ISO-10303-21;
HEADER;
FILE_DESCRIPTION (('STEP AP214'),
    '1' );
FILE_NAME ('hex flange bolt_din_DIN 6921 - M8 x 30 x 30-S.step',
    '2026-10-09T14:04:53',
    ( '' ),
    ( '' ),
    'SwSTEP 2.0',
    'SolidWorks 2021',
    '' );
FILE_SCHEMA (( 'AUTOMOTIVE_DESIGN' ));
ENDSEC;

DATA;
#5=ORIENTED_EDGE ( 'NONE', *, *, #56749, .T. ) ;
#25=VECTOR ( 'NONE', #75300, 1000.000000000000000 ) ;
#28=CARTESIAN_POINT ( 'NONE',  ( 13.09999999999999787, 1.533819458162526451E-15, 0.000000000000000000 ) ) ;
#100=DIRECTION ( 'NONE',  ( 0.000000000000000000, -1.000000000000000000, 0.000000000000000000 ) ) ;
#184=CARTESIAN_POINT ( 'NONE',  ( 0.000000000000000000, 0.000000000000000000, 0.000000000000000000 ) ) ;
#200=CARTESIAN_POINT ( 'NONE',  ( 37.40949999999997289, 0.000000000000000000, 0.000000000000000000 ) ) ;
#228=DIRECTION ( 'NONE',  ( 0.000000000000000000, -1.000000000000000000, 0.000000000000000000 ) ) ;
#251=DIRECTION ( 'NONE',  ( 0.000000000000000000, -1.000000000000000000, 0.000000000000000000 ) ) ;
#256=CARTESIAN_POINT ( 'NONE',  ( 0.000000000000000000, 0.000000000000000000, 0.000000000000000000 ) ) ;
#258=EDGE_CURVE ( 'NONE', #42466, #63078, #68595, .T. ) ;
#279=CONICAL_SURFACE ( 'NONE', #70939, 3.309500000000001663, 0.9599310885968770357 ) ;
#284=CARTESIAN_POINT ( 'NONE',  ( 36.08349330513379982, 1.593028355512270962E-15, 0.000000000000000000 ) ) ;
#296=ORIENTED_EDGE ( 'NONE', *, *, #75581, .T. ) ;
#338=ORIENTED_EDGE ( 'NONE', *, *, #17693, .T. ) ;
#368=CIRCLE ( 'NONE', #53762, 4.000000000000000888 ) ;
#374=ORIENTED_EDGE ( 'NONE', *, *, #93282, .F. ) ;
#387=CARTESIAN_POINT ( 'NONE',  ( 0.5805565836007605673, 3.752776749732565253, 6.499999999999997335 ) ) ;
#388=CARTESIAN_POINT ( 'NONE',  ( 23.58349330513380337, 1.593028355512270962E-15, 0.000000000000000000 ) ) ;
#389=DIRECTION ( 'NONE',  ( 0.000000000000000000, -1.000000000000000000, 0.000000000000000000 ) ) ;
#421=ORIENTED_EDGE ( 'NONE', *, *, #82408, .T. ) ;
#455=CARTESIAN_POINT ( 'NONE',  ( 27.33349330513380693, -4.000000000000000888, 4.898587196589416773E-16 ) ) ;
#501=CARTESIAN_POINT ( 'NONE',  ( 6.162888688655347558, 7.505553499465140277, 0.000000000000000000 ) ) ;
#503=VECTOR ( 'NONE', #36456, 1000.000000000000341 ) ;
#522=VECTOR ( 'NONE', #46039, 1000.000000000000341 ) ;
#545=ORIENTED_EDGE ( 'NONE', *, *, #45539, .T. ) ;
#559=B_SPLINE_CURVE_WITH_KNOTS ( 'NONE', 3,
 ( #3751, #4273, #36682, #21544, #20521 ),
 .UNSPECIFIED., .F., .F.,
 ( 4, 1, 4 ),
 ( 0.000000000000000000, 0.003752776749732568331, 0.007505553499465136662 ),
 .UNSPECIFIED. ) ;
#568=VECTOR ( 'NONE', #12370, 1000.000000000000000 ) ;
#601=DIRECTION ( 'NONE',  ( 0.000000000000000000, -1.000000000000000000, 0.000000000000000000 ) ) ;
#615=FACE_OUTER_BOUND ( 'NONE', #63502, .T. ) ;
#623=ORIENTED_EDGE ( 'NONE', *, *, #98570, .T. ) ;
#685=DIRECTION ( 'NONE',  ( 1.000000000000000000, 1.224606353822377258E-16, 0.000000000000000000 ) ) ;
#694=DIRECTION ( 'NONE',  ( -1.000000000000000000, -1.224606353822377258E-16, -0.000000000000000000 ) ) ;
#706=CARTESIAN_POINT ( 'NONE',  ( 6.643884894376897776, 3.901062859471661870, -6.756839076126022192 ) ) ;
#707=LINE ( 'NONE', #50883, #95053 ) ;
#718=EDGE_CURVE ( 'NONE', #102768, #42192, #99703, .T. ) ;
#753=CARTESIAN_POINT ( 'NONE',  ( 6.936184427528457874, 1.053834543709838281E-15, 8.605212085995399107 ) ) ;
#786=LINE ( 'NONE', #100056, #81311 ) ;
#815=DIRECTION ( 'NONE',  ( 0.000000000000000000, 0.000000000000000000, 1.000000000000000000 ) ) ;
#826=VERTEX_POINT ( 'NONE', #2592 ) ;
#849=CARTESIAN_POINT ( 'NONE',  ( 6.326592304916277776, 6.579439845142157850, 2.267162479624766025 ) ) ;
#876=VERTEX_POINT ( 'NONE', #36085 ) ;
#900=CARTESIAN_POINT ( 'NONE',  ( 36.84999999999999432, 3.309500000000003439, 4.052968581778167743E-16 ) ) ;
#922=DIRECTION ( 'NONE',  ( -1.000000000000000000, -1.224606353822377258E-16, -0.000000000000000000 ) ) ;
#952=ORIENTED_EDGE ( 'NONE', *, *, #4809, .T. ) ;
#953=AXIS2_PLACEMENT_3D ( 'NONE', #83715, #26602, #27131 ) ;
#1013=EDGE_CURVE ( 'NONE', #83206, #68858, #73785, .T. ) ;
#1027=ADVANCED_FACE ( 'NONE', ( #79675 ), #26616, .F. ) ;
#1046=EDGE_CURVE ( 'NONE', #86797, #45061, #95974, .T. ) ;
#1091=FACE_OUTER_BOUND ( 'NONE', #64944, .T. ) ;
#1124=CARTESIAN_POINT ( 'NONE',  ( 17.33349330513380693, 4.898587196589411843E-16, -4.000000000000001776 ) ) ;
#1134=CARTESIAN_POINT ( 'NONE',  ( 0.000000000000000000, 0.000000000000000000, 0.000000000000000000 ) ) ;
#1144=FACE_OUTER_BOUND ( 'NONE', #89371, .T. ) ;
#1187=LINE ( 'NONE', #2266, #66386 ) ;
#1191=DIRECTION ( 'NONE',  ( 0.000000000000000000, -1.000000000000000000, 0.000000000000000000 ) ) ;
#1199=ORIENTED_EDGE ( 'NONE', *, *, #79459, .F. ) ;
#1203=ORIENTED_EDGE ( 'NONE', *, *, #98674, .F. ) ;
#1214=CONICAL_SURFACE ( 'NONE', #70171, 4.000000000000001776, 0.9599310885968774798 ) ;
#1243=AXIS2_PLACEMENT_3D ( 'NONE', #40069, #39022, #100 ) ;
#1282=DIRECTION ( 'NONE',  ( 0.000000000000000000, -1.000000000000000000, 0.000000000000000000 ) ) ;
#1315=VECTOR ( 'NONE', #44030, 1000.000000000000000 ) ;
#1323=CARTESIAN_POINT ( 'NONE',  ( 36.36650669486618881, 0.000000000000000000, 4.000000000000000888 ) ) ;
#1336=CONICAL_SURFACE ( 'NONE', #85774, 3.309500000000001663, 0.9599310885968770357 ) ;
#1348=AXIS2_PLACEMENT_3D ( 'NONE', #8861, #84364, #26692 ) ;
#1355=EDGE_CURVE ( 'NONE', #7599, #17049, #34025, .T. ) ;
#1362=DIRECTION ( 'NONE',  ( 0.000000000000000000, -1.000000000000000000, 0.000000000000000000 ) ) ;
#1370=ORIENTED_EDGE ( 'NONE', *, *, #98570, .F. ) ;
#1377=CARTESIAN_POINT ( 'NONE',  ( 6.562934840145643101, -7.579717272840337472, 0.5631738335430738207 ) ) ;
#1386=VECTOR ( 'NONE', #70885, 1000.000000000000000 ) ;
#1401=CARTESIAN_POINT ( 'NONE',  ( 8.099999999999999645, 1.041268927496807532E-15, -8.400000000000000355 ) ) ;
#1420=VERTEX_POINT ( 'NONE', #3554 ) ;
#1434=ORIENTED_EDGE ( 'NONE', *, *, #1046, .T. ) ;
#1485=VERTEX_POINT ( 'NONE', #106327 ) ;
#1512=ORIENTED_EDGE ( 'NONE', *, *, #55924, .F. ) ;
#1528=LINE ( 'NONE', #2066, #52976 ) ;
#1543=DIRECTION ( 'NONE',  ( 1.000000000000000000, 1.224606353822377258E-16, 0.000000000000000000 ) ) ;
#1564=DIRECTION ( 'NONE',  ( -1.000000000000000000, -0.000000000000000000, -0.000000000000000000 ) ) ;
#1578=CONICAL_SURFACE ( 'NONE', #5076, 4.000000000000001776, 0.9599310885968774798 ) ;
#1585=ORIENTED_EDGE ( 'NONE', *, *, #7579, .T. ) ;
#1593=VECTOR ( 'NONE', #4066, 1000.000000000000000 ) ;
#1595=CIRCLE ( 'NONE', #82536, 4.000000000000001776 ) ;
#1600=AXIS2_PLACEMENT_3D ( 'NONE', #2844, #83238, #34731 ) ;
#1619=ADVANCED_FACE ( 'NONE', ( #74503 ), #18535, .T. ) ;
#1650=AXIS2_PLACEMENT_3D ( 'NONE', #82261, #57440, #81191 ) ;
#1712=CARTESIAN_POINT ( 'NONE',  ( 35.11650669486618170, 0.000000000000000000, 4.000000000000000888 ) ) ;
#1716=EDGE_CURVE ( 'NONE', #56185, #45991, #15032, .T. ) ;
#1764=AXIS2_PLACEMENT_3D ( 'NONE', #100011, #42843, #84374 ) ;
#1776=CARTESIAN_POINT ( 'NONE',  ( 29.34999999999999787, 1.533819458162526451E-15, 0.000000000000000000 ) ) ;
#1799=CARTESIAN_POINT ( 'NONE',  ( 0.000000000000000000, 4.898587196589413815E-16, -4.000000000000000888 ) ) ;
#1815=FACE_OUTER_BOUND ( 'NONE', #62603, .T. ) ;
#1823=DIRECTION ( 'NONE',  ( -1.000000000000000000, -1.224606353822377258E-16, -0.000000000000000000 ) ) ;
#1825=EDGE_CURVE ( 'NONE', #84857, #42272, #85672, .T. ) ;
#1828=ORIENTED_EDGE ( 'NONE', *, *, #21149, .T. ) ;
#1851=PLANE ( 'NONE',  #78548 ) ;
#1856=CIRCLE ( 'NONE', #32845, 4.000000000000000888 ) ;
#1867=DIRECTION ( 'NONE',  ( -1.000000000000000000, -1.224606353822377258E-16, -0.000000000000000000 ) ) ;
#1883=EDGE_CURVE ( 'NONE', #14833, #62772, #28132, .T. ) ;
#1893=CARTESIAN_POINT ( 'NONE',  ( 0.000000000000000000, -5.629165124598847214, 3.250000000000005329 ) ) ;
#1899=ORIENTED_EDGE ( 'NONE', *, *, #66860, .T. ) ;
#1904=CARTESIAN_POINT ( 'NONE',  ( 17.61650669486618881, 4.000000000000003553, 4.898587196589414801E-16 ) ) ;
#1932=ORIENTED_EDGE ( 'NONE', *, *, #62858, .F. ) ;
#1962=ORIENTED_EDGE ( 'NONE', *, *, #105947, .T. ) ;
#2003=VECTOR ( 'NONE', #11800, 1000.000000000000000 ) ;
#2013=CARTESIAN_POINT ( 'NONE',  ( 28.86650669486618881, -3.999999999999998224, 0.000000000000000000 ) ) ;
#2031=CYLINDRICAL_SURFACE ( 'NONE', #65535, 4.000000000000000888 ) ;
#2044=DIRECTION ( 'NONE',  ( 0.000000000000000000, -1.000000000000000000, 0.000000000000000000 ) ) ;
#2047=EDGE_CURVE ( 'NONE', #21783, #81794, #10699, .T. ) ;
#2066=CARTESIAN_POINT ( 'NONE',  ( 30.59999999999999787, -3.309499999999999886, 0.000000000000000000 ) ) ;
#2074=AXIS2_PLACEMENT_3D ( 'NONE', #105346, #64371, #90221 ) ;
#2082=ORIENTED_EDGE ( 'NONE', *, *, #7579, .F. ) ;
#2086=ADVANCED_FACE ( 'NONE', ( #26415 ), #26941, .T. ) ;
#2087=AXIS2_PLACEMENT_3D ( 'NONE', #68907, #19856, #37626 ) ;
#2088=ORIENTED_EDGE ( 'NONE', *, *, #81317, .F. ) ;
#2121=DIRECTION ( 'NONE',  ( -1.000000000000000000, -1.224606353822377258E-16, -0.000000000000000000 ) ) ;
#2135=FACE_OUTER_BOUND ( 'NONE', #14476, .T. ) ;
#2145=DIRECTION ( 'NONE',  ( -0.5735764363510497121, 0.8191520442889892450, 1.003171929053521665E-16 ) ) ;
#2159=DIRECTION ( 'NONE',  ( -1.000000000000000000, -1.224606353822377258E-16, -0.000000000000000000 ) ) ;
#2165=ORIENTED_EDGE ( 'NONE', *, *, #91155, .T. ) ;
#2173=CARTESIAN_POINT ( 'NONE',  ( 0.06682554136337941209, 6.264794173742279426, 2.149058192116896748 ) ) ;
#2252=CARTESIAN_POINT ( 'NONE',  ( 33.58349330513380693, 4.000000000000002665, 0.000000000000000000 ) ) ;
#2266=CARTESIAN_POINT ( 'NONE',  ( 14.34999999999999787, 3.309500000000003439, 4.052968581778167743E-16 ) ) ;
#2323=CARTESIAN_POINT ( 'NONE',  ( 8.099999999999999645, 7.505553499465140277, -3.755786496842903002E-16 ) ) ;
#2389=ORIENTED_EDGE ( 'NONE', *, *, #58737, .F. ) ;
#2401=DIRECTION ( 'NONE',  ( -1.000000000000000000, -1.224606353822377258E-16, -0.000000000000000000 ) ) ;
#2440=AXIS2_PLACEMENT_3D ( 'NONE', #99860, #26032, #16283 ) ;
#2446=EDGE_CURVE ( 'NONE', #46570, #11369, #59159, .T. ) ;
#2468=EDGE_LOOP ( 'NONE', ( #92470, #16063, #88334, #3572, #27114 ) ) ;
#2503=DIRECTION ( 'NONE',  ( 0.000000000000000000, 0.000000000000000000, -1.000000000000000000 ) ) ;
#2531=AXIS2_PLACEMENT_3D ( 'NONE', #10388, #3381, #10910 ) ;
#2537=AXIS2_PLACEMENT_3D ( 'NONE', #38078, #60218, #68831 ) ;
#2557=CARTESIAN_POINT ( 'NONE',  ( 6.222742520105473574, -7.673830019007163550, 0.2914634815676374613 ) ) ;
#2582=ORIENTED_EDGE ( 'NONE', *, *, #56675, .F. ) ;
#2585=DIRECTION ( 'NONE',  ( 0.000000000000000000, 1.000000000000000000, 0.000000000000000000 ) ) ;
#2586=EDGE_LOOP ( 'NONE', ( #29695, #56583, #5994, #83844, #105918, #100891 ) ) ;
#2592=CARTESIAN_POINT ( 'NONE',  ( 23.58349330513380337, -3.851859888774471706E-31, 4.000000000000001776 ) ) ;
#2625=EDGE_CURVE ( 'NONE', #4198, #6482, #47723, .T. ) ;
#2658=DIRECTION ( 'NONE',  ( -1.000000000000000000, -0.000000000000000000, -0.000000000000000000 ) ) ;
#2659=ORIENTED_EDGE ( 'NONE', *, *, #20483, .T. ) ;
#2687=CARTESIAN_POINT ( 'NONE',  ( 24.83349330513380693, 4.000000000000003553, 0.000000000000000000 ) ) ;
#2692=EDGE_LOOP ( 'NONE', ( #80303, #952, #87603, #34761, #102068 ) ) ;
#2716=CARTESIAN_POINT ( 'NONE',  ( 0.2578475836320712200, 6.890627091270371096, 1.065083781909173410 ) ) ;
#2728=ORIENTED_EDGE ( 'NONE', *, *, #33471, .T. ) ;
#2739=CARTESIAN_POINT ( 'NONE',  ( 0.000000000000000000, 0.000000000000000000, 0.000000000000000000 ) ) ;
#2742=CARTESIAN_POINT ( 'NONE',  ( 8.099999999999999645, 0.000000000000000000, 8.400000000000000355 ) ) ;
#2775=ORIENTED_EDGE ( 'NONE', *, *, #92848, .T. ) ;
#2779=CARTESIAN_POINT ( 'NONE',  ( 5.947762761376476526, -6.880090707843042885, 1.083333333333332593 ) ) ;
#2844=CARTESIAN_POINT ( 'NONE',  ( 18.58349330513380693, 1.593028355512270962E-15, 0.000000000000000000 ) ) ;
#2855=DIRECTION ( 'NONE',  ( 0.5735764363510490460, 0.8191520442889896891, 0.000000000000000000 ) ) ;
#2859=AXIS2_PLACEMENT_3D ( 'NONE', #60601, #11472, #28790 ) ;
#2872=ORIENTED_EDGE ( 'NONE', *, *, #35904, .F. ) ;
#2873=CARTESIAN_POINT ( 'NONE',  ( 20.59999999999999787, 3.309500000000003439, 0.000000000000000000 ) ) ;
#2898=CARTESIAN_POINT ( 'NONE',  ( 0.000000000000000000, 0.000000000000000000, 0.000000000000000000 ) ) ;
#2900=DIRECTION ( 'NONE',  ( 0.000000000000000000, -1.000000000000000000, 0.000000000000000000 ) ) ;
#2902=CIRCLE ( 'NONE', #87312, 4.000000000000000888 ) ;
#2915=CONICAL_SURFACE ( 'NONE', #63217, 4.000000000000001776, 0.9599310885968774798 ) ;
#2975=CARTESIAN_POINT ( 'NONE',  ( 11.36650669486618881, 1.474610560812782335E-15, 0.000000000000000000 ) ) ;
#2986=ORIENTED_EDGE ( 'NONE', *, *, #75474, .F. ) ;
#2998=VERTEX_POINT ( 'NONE', #46553 ) ;
#3039=VERTEX_POINT ( 'NONE', #78385 ) ;
#3057=DIRECTION ( 'NONE',  ( -1.000000000000000000, -1.224606353822377258E-16, -0.000000000000000000 ) ) ;
#3058=CONICAL_SURFACE ( 'NONE', #106358, 3.309500000000001663, 0.9599310885968770357 ) ;
#3065=VERTEX_POINT ( 'NONE', #63280 ) ;
#3125=CARTESIAN_POINT ( 'NONE',  ( 35.11650669486618170, -3.999999999999998224, 0.000000000000000000 ) ) ;
#3128=VERTEX_POINT ( 'NONE', #34124 ) ;
#3131=DIRECTION ( 'NONE',  ( -1.000000000000000000, -1.224606353822377258E-16, -0.000000000000000000 ) ) ;
#3132=DIRECTION ( 'NONE',  ( 1.000000000000000000, 1.224606353822377258E-16, 0.000000000000000000 ) ) ;
#3252=DIRECTION ( 'NONE',  ( 0.000000000000000000, 1.000000000000000000, 0.000000000000000000 ) ) ;
#3255=AXIS2_PLACEMENT_3D ( 'NONE', #62065, #21089, #28642 ) ;
#3272=CARTESIAN_POINT ( 'NONE',  ( 36.08349330513379982, 1.593028355512270962E-15, 0.000000000000000000 ) ) ;
#3300=B_SPLINE_CURVE_WITH_KNOTS ( 'NONE', 3,
 ( #3988, #13649, #4510, #36400, #86524, #69266 ),
 .UNSPECIFIED., .F., .F.,
 ( 4, 2, 4 ),
 ( 0.000000000000000000, 0.0003491763592121695367, 0.0006983527184243390733 ),
 .UNSPECIFIED. ) ;
#3323=CARTESIAN_POINT ( 'NONE',  ( 6.162888688655344893, -3.752776749732565253, 6.499999999999999112 ) ) ;
#3332=DIRECTION ( 'NONE',  ( -1.000000000000000000, -1.224606353822377258E-16, -0.000000000000000000 ) ) ;
#3338=EDGE_CURVE ( 'NONE', #14833, #87241, #63216, .T. ) ;
#3381=DIRECTION ( 'NONE',  ( -1.000000000000000000, -1.224606353822377258E-16, -0.000000000000000000 ) ) ;
#3461=ORIENTED_EDGE ( 'NONE', *, *, #33936, .F. ) ;
#3552=DIRECTION ( 'NONE',  ( 0.5735764363510491570, -0.8191520442889895781, 1.003171929053522035E-16 ) ) ;
#3554=CARTESIAN_POINT ( 'NONE',  ( 12.33349330513380693, 4.000000000000002665, 0.000000000000000000 ) ) ;
#3569=CARTESIAN_POINT ( 'NONE',  ( 0.000000000000000000, -5.629165124598850767, -3.249999999999999556 ) ) ;
#3572=ORIENTED_EDGE ( 'NONE', *, *, #16347, .F. ) ;
#3579=( BOUNDED_SURFACE ( )  B_SPLINE_SURFACE ( 3, 2, ( 
 ( #34118, #98278, #9254 ),
 ( #41640, #42164, #73454 ),
 ( #57802, #8732, #75045 ),
 ( #90726, #23897, #106352 ),
 ( #99321, #7655, #31972 ),
 ( #97207, #74523, #90190 ),
 ( #32514, #15232, #25495 ),
 ( #82082, #81530, #72920 ) ),
 .UNSPECIFIED., .F., .F., .F. ) 
 B_SPLINE_SURFACE_WITH_KNOTS ( ( 4, 2, 2, 4 ),
 ( 3, 3 ),
 ( 0.03205733154476830132, 0.03606343422293256662, 0.03806648556201470274, 0.04006953690109683885 ),
 ( 0.000000000000000000, 1.000000000000000000 ),
 .UNSPECIFIED. ) 
 GEOMETRIC_REPRESENTATION_ITEM ( )  RATIONAL_B_SPLINE_SURFACE ( (
 ( 1.000000000000000000, 0.8047781205924506853, 1.000000000000000000),
 ( 1.000000000000000000, 0.8123783054473237009, 1.000000000000000000),
 ( 1.000000000000000000, 0.8190665327891030190, 1.000000000000000000),
 ( 1.000000000000000000, 0.8191934993920665375, 1.000000000000000000),
 ( 1.000000000000000000, 0.8176088856299312813, 1.000000000000000000),
 ( 1.000000000000000000, 0.8122958243108089338, 1.000000000000000000),
 ( 1.000000000000000000, 0.8086309198479199045, 1.000000000000000000),
 ( 1.000000000000000000, 0.8047712443299024354, 1.000000000000000000) ) ) 
 REPRESENTATION_ITEM ( '' )  SURFACE ( )  );
#3584=ORIENTED_EDGE ( 'NONE', *, *, #57707, .F. ) ;
#3600=FACE_OUTER_BOUND ( 'NONE', #74002, .T. ) ;
#3641=EDGE_CURVE ( 'NONE', #2998, #88621, #90904, .T. ) ;
#3645=ORIENTED_EDGE ( 'NONE', *, *, #44250, .F. ) ;
#3652=EDGE_CURVE ( 'NONE', #30663, #11120, #78738, .T. ) ;
#3689=AXIS2_PLACEMENT_3D ( 'NONE', #66062, #24577, #228 ) ;
#3710=CIRCLE ( 'NONE', #101855, 4.000000000000000888 ) ;
#3751=CARTESIAN_POINT ( 'NONE',  ( 6.162888688655344893, 3.752776749732562589, -6.500000000000000888 ) ) ;
#3767=CARTESIAN_POINT ( 'NONE',  ( 6.169949891408088583, 6.308465495018137581, -2.073417244832098216 ) ) ;
#3780=ORIENTED_EDGE ( 'NONE', *, *, #59664, .F. ) ;
#3812=ORIENTED_EDGE ( 'NONE', *, *, #32330, .T. ) ;
#3824=CARTESIAN_POINT ( 'NONE',  ( 16.08349330513380337, 1.593028355512270962E-15, 0.000000000000000000 ) ) ;
#3861=DIRECTION ( 'NONE',  ( 0.5735764363510490460, 0.8191520442889896891, 0.000000000000000000 ) ) ;
#3872=DIRECTION ( 'NONE',  ( -1.000000000000000000, -1.224606353822377258E-16, -0.000000000000000000 ) ) ;
#3877=DIRECTION ( 'NONE',  ( 1.000000000000000000, 0.000000000000000000, 0.000000000000000000 ) ) ;
#3887=CARTESIAN_POINT ( 'NONE',  ( 22.33349330513380693, 1.593028355512270962E-15, 0.000000000000000000 ) ) ;
#3940=FACE_BOUND ( 'NONE', #47503, .T. ) ;
#3975=DIRECTION ( 'NONE',  ( 0.000000000000000000, -1.000000000000000000, 0.000000000000000000 ) ) ;
#3988=CARTESIAN_POINT ( 'NONE',  ( 6.162888688655347558, 7.505553499465140277, 0.000000000000000000 ) ) ;
#4006=VERTEX_POINT ( 'NONE', #23169 ) ;
#4013=CARTESIAN_POINT ( 'NONE',  ( 0.000000000000000000, 0.000000000000000000, 0.000000000000000000 ) ) ;
#4015=DIRECTION ( 'NONE',  ( -1.000000000000000000, -1.224606353822377258E-16, -0.000000000000000000 ) ) ;
#4035=DIRECTION ( 'NONE',  ( -1.000000000000000000, -1.224606353822377258E-16, -0.000000000000000000 ) ) ;
#4052=FACE_OUTER_BOUND ( 'NONE', #78060, .T. ) ;
#4055=AXIS2_PLACEMENT_3D ( 'NONE', #10868, #3872, #52945 ) ;
#4058=DIRECTION ( 'NONE',  ( 1.000000000000000000, 1.224606353822377258E-16, 0.000000000000000000 ) ) ;
#4059=ADVANCED_FACE ( 'NONE', ( #97028 ), #28923, .T. ) ;
#4062=ADVANCED_FACE ( 'NONE', ( #72229 ), #37247, .T. ) ;
#4066=DIRECTION ( 'NONE',  ( -1.000000000000000000, -0.000000000000000000, -0.000000000000000000 ) ) ;
#4071=CARTESIAN_POINT ( 'NONE',  ( 25.59999999999999787, 1.533819458162526451E-15, 0.000000000000000000 ) ) ;
#4077=ORIENTED_EDGE ( 'NONE', *, *, #103276, .T. ) ;
#4078=DIRECTION ( 'NONE',  ( -1.000000000000000000, -0.000000000000000000, -0.000000000000000000 ) ) ;
#4114=CARTESIAN_POINT ( 'NONE',  ( 0.000000000000000000, 5.629165124598848102, -3.250000000000007105 ) ) ;
#4132=ORIENTED_EDGE ( 'NONE', *, *, #19874, .T. ) ;
#4140=AXIS2_PLACEMENT_3D ( 'NONE', #37323, #70184, #103090 ) ;
#4151=EDGE_CURVE ( 'NONE', #10937, #90401, #27218, .T. ) ;
#4159=AXIS2_PLACEMENT_3D ( 'NONE', #99423, #50345, #25602 ) ;
#4178=DIRECTION ( 'NONE',  ( -1.000000000000000000, -1.224606353822377258E-16, -0.000000000000000000 ) ) ;
#4198=VERTEX_POINT ( 'NONE', #16647 ) ;
#4215=DIRECTION ( 'NONE',  ( -1.000000000000000000, -1.224606353822377258E-16, -0.000000000000000000 ) ) ;
#4218=ORIENTED_EDGE ( 'NONE', *, *, #29825, .T. ) ;
#4237=VERTEX_POINT ( 'NONE', #24241 ) ;
#4273=CARTESIAN_POINT ( 'NONE',  ( 5.947762761376473861, 2.501851166488373579, -6.500000000000000000 ) ) ;
#4276=AXIS2_PLACEMENT_3D ( 'NONE', #58801, #2121, #25392 ) ;
#4302=CARTESIAN_POINT ( 'NONE',  ( 6.445370176741822554, 4.584736124523701939, 5.738941594274445279 ) ) ;
#4308=DIRECTION ( 'NONE',  ( 1.000000000000000000, 1.224606353822377258E-16, 0.000000000000000000 ) ) ;
#4316=VERTEX_POINT ( 'NONE', #3125 ) ;
#4318=ORIENTED_EDGE ( 'NONE', *, *, #75224, .T. ) ;
#4355=ORIENTED_EDGE ( 'NONE', *, *, #51750, .F. ) ;
#4368=DIRECTION ( 'NONE',  ( -1.000000000000000000, -1.224606353822377258E-16, -0.000000000000000000 ) ) ;
#4387=AXIS2_PLACEMENT_3D ( 'NONE', #77555, #45205, #11731 ) ;
#4409=EDGE_CURVE ( 'NONE', #21060, #4006, #29052, .T. ) ;
#4414=CARTESIAN_POINT ( 'NONE',  ( 20.11650669486618881, 4.898587196589413815E-16, -4.000000000000000888 ) ) ;
#4468=CARTESIAN_POINT ( 'NONE',  ( 32.61650669486618881, 1.474610560812782335E-15, 0.000000000000000000 ) ) ;
#4510=CARTESIAN_POINT ( 'NONE',  ( 6.394343112843833943, 7.552705921139272860, 1.203258575478541822E-16 ) ) ;
#4533=VECTOR ( 'NONE', #67586, 1000.000000000000341 ) ;
#4537=VECTOR ( 'NONE', #48646, 1000.000000000000000 ) ;
#4564=DIRECTION ( 'NONE',  ( -1.000000000000000000, -0.000000000000000000, -0.000000000000000000 ) ) ;
#4567=DIRECTION ( 'NONE',  ( 0.000000000000000000, -1.000000000000000000, 0.000000000000000000 ) ) ;
#4596=ORIENTED_EDGE ( 'NONE', *, *, #85346, .F. ) ;
#4606=CIRCLE ( 'NONE', #8042, 4.000000000000000888 ) ;
#4636=CARTESIAN_POINT ( 'NONE',  ( 0.2578475836320734405, -6.890627091270379090, -1.065083781909172078 ) ) ;
#4690=EDGE_CURVE ( 'NONE', #63779, #48529, #61465, .T. ) ;
#4714=EDGE_CURVE ( 'NONE', #99250, #60578, #26567, .T. ) ;
#4765=DIRECTION ( 'NONE',  ( 0.000000000000000000, -1.000000000000000000, 0.000000000000000000 ) ) ;
#4768=ORIENTED_EDGE ( 'NONE', *, *, #81492, .F. ) ;
#4809=EDGE_CURVE ( 'NONE', #42350, #35708, #11068, .T. ) ;
#4823=AXIS2_PLACEMENT_3D ( 'NONE', #26729, #76292, #59600 ) ;
#4833=CONICAL_SURFACE ( 'NONE', #44497, 4.000000000000001776, 0.9599310885968774798 ) ;
#4883=DIRECTION ( 'NONE',  ( 0.000000000000000000, -1.000000000000000000, 0.000000000000000000 ) ) ;
#4895=ORIENTED_EDGE ( 'NONE', *, *, #40959, .F. ) ;
#4923=VECTOR ( 'NONE', #18019, 1000.000000000000000 ) ;
#4951=AXIS2_PLACEMENT_3D ( 'NONE', #31511, #65441, #49234 ) ;
#5020=ORIENTED_EDGE ( 'NONE', *, *, #63900, .F. ) ;
#5021=CARTESIAN_POINT ( 'NONE',  ( 36.84999999999999432, -3.309499999999999886, 0.000000000000000000 ) ) ;
#5041=CARTESIAN_POINT ( 'NONE',  ( 15.11650669486618881, 4.898587196589413815E-16, -4.000000000000000888 ) ) ;
#5046=VECTOR ( 'NONE', #42331, 1000.000000000000000 ) ;
#5076=AXIS2_PLACEMENT_3D ( 'NONE', #79368, #45953, #70754 ) ;
#5078=AXIS2_PLACEMENT_3D ( 'NONE', #65250, #37438, #70833 ) ;
#5097=CARTESIAN_POINT ( 'NONE',  ( 0.000000000000000000, 0.000000000000000000, 4.000000000000000888 ) ) ;
#5103=CARTESIAN_POINT ( 'NONE',  ( 12.33349330513380693, 1.593028355512270962E-15, 0.000000000000000000 ) ) ;
#5104=DIRECTION ( 'NONE',  ( 0.000000000000000000, 1.000000000000000000, 0.000000000000000000 ) ) ;
#5112=CARTESIAN_POINT ( 'NONE',  ( 26.84999999999999787, 1.533819458162526451E-15, 0.000000000000000000 ) ) ;
#5116=AXIS2_PLACEMENT_3D ( 'NONE', #31498, #81064, #64378 ) ;
#5128=FACE_OUTER_BOUND ( 'NONE', #49651, .T. ) ;
#5155=EDGE_CURVE ( 'NONE', #87702, #101426, #75054, .T. ) ;
#5183=CIRCLE ( 'NONE', #65451, 4.000000000000001776 ) ;
#5186=ORIENTED_EDGE ( 'NONE', *, *, #38471, .F. ) ;
#5203=CIRCLE ( 'NONE', #41371, 3.309500000000001663 ) ;
#5206=EDGE_CURVE ( 'NONE', #87241, #99736, #27183, .T. ) ;
#5230=CARTESIAN_POINT ( 'NONE',  ( 26.84999999999999787, 1.533819458162526451E-15, 0.000000000000000000 ) ) ;
#5241=ORIENTED_EDGE ( 'NONE', *, *, #61476, .T. ) ;
#5332=CARTESIAN_POINT ( 'NONE',  ( 28.86650669486618881, 1.474610560812782335E-15, 0.000000000000000000 ) ) ;
#5368=ORIENTED_EDGE ( 'NONE', *, *, #66094, .T. ) ;
#5372=CARTESIAN_POINT ( 'NONE',  ( 6.169949891409287623, 4.949864754176874548, 4.426582755168845473 ) ) ;
#5394=EDGE_CURVE ( 'NONE', #15029, #87062, #33836, .T. ) ;
#5454=AXIS2_PLACEMENT_3D ( 'NONE', #33192, #99477, #26190 ) ;
#5475=CARTESIAN_POINT ( 'NONE',  ( 13.58349330513380515, 1.593028355512270962E-15, 0.000000000000000000 ) ) ;
#5489=EDGE_LOOP ( 'NONE', ( #20882, #40346, #66456, #7647, #64585 ) ) ;
#5521=ORIENTED_EDGE ( 'NONE', *, *, #5155, .T. ) ;
#5522=DIRECTION ( 'NONE',  ( 0.000000000000000000, -1.000000000000000000, 0.000000000000000000 ) ) ;
#5531=CARTESIAN_POINT ( 'NONE',  ( 0.000000000000000000, 0.000000000000000000, 0.000000000000000000 ) ) ;
#5553=CYLINDRICAL_SURFACE ( 'NONE', #29779, 4.000000000000000888 ) ;
#5561=ORIENTED_EDGE ( 'NONE', *, *, #37468, .T. ) ;
#5613=ORIENTED_EDGE ( 'NONE', *, *, #67276, .F. ) ;
#5623=CIRCLE ( 'NONE', #11008, 4.000000000000001776 ) ;
#5625=DIRECTION ( 'NONE',  ( 1.000000000000000000, 1.224606353822377258E-16, 0.000000000000000000 ) ) ;
#5629=ORIENTED_EDGE ( 'NONE', *, *, #28525, .T. ) ;
#5635=DIRECTION ( 'NONE',  ( 0.000000000000000000, -1.000000000000000000, 0.000000000000000000 ) ) ;
#5645=ORIENTED_EDGE ( 'NONE', *, *, #28115, .F. ) ;
#5665=DIRECTION ( 'NONE',  ( -1.000000000000000000, -1.224606353822377258E-16, -0.000000000000000000 ) ) ;
#5669=CARTESIAN_POINT ( 'NONE',  ( 0.4053525175236804001, 3.145852061456247739, 6.499999999999998224 ) ) ;
#5693=CARTESIAN_POINT ( 'NONE',  ( 0.000000000000000000, 0.000000000000000000, 0.000000000000000000 ) ) ;
#5739=FACE_OUTER_BOUND ( 'NONE', #16993, .T. ) ;
#5743=ADVANCED_FACE ( 'NONE', ( #82538 ), #16204, .T. ) ;
#5751=ADVANCED_FACE ( 'NONE', ( #31883 ), #82460, .T. ) ;
#5795=ORIENTED_EDGE ( 'NONE', *, *, #63676, .T. ) ;
#5815=DIRECTION ( 'NONE',  ( -0.5735764363510494901, -0.8191520442889894671, 0.000000000000000000 ) ) ;
#5816=CARTESIAN_POINT ( 'NONE',  ( 0.000000000000000000, 0.000000000000000000, 4.000000000000000888 ) ) ;
#5884=DIRECTION ( 'NONE',  ( 1.000000000000000000, 1.224606353822377258E-16, 0.000000000000000000 ) ) ;
#5910=ORIENTED_EDGE ( 'NONE', *, *, #77334, .T. ) ;
#5948=AXIS2_PLACEMENT_3D ( 'NONE', #72062, #96360, #251 ) ;
#5950=FACE_OUTER_BOUND ( 'NONE', #18334, .T. ) ;
#5979=VECTOR ( 'NONE', #5815, 1000.000000000000000 ) ;
#5986=EDGE_CURVE ( 'NONE', #87241, #14833, #56574, .T. ) ;
#5991=CONICAL_SURFACE ( 'NONE', #14602, 4.000000000000001776, 0.9599310885968774798 ) ;
#5992=AXIS2_PLACEMENT_3D ( 'NONE', #9461, #65057, #34324 ) ;
#5994=ORIENTED_EDGE ( 'NONE', *, *, #73101, .T. ) ;
#6030=EDGE_CURVE ( 'NONE', #30663, #30305, #6921, .T. ) ;
#6058=ORIENTED_EDGE ( 'NONE', *, *, #93557, .T. ) ;
#6073=AXIS2_PLACEMENT_3D ( 'NONE', #16419, #38599, #14285 ) ;
#6085=AXIS2_PLACEMENT_3D ( 'NONE', #49084, #106258, #48022 ) ;
#6096=DIRECTION ( 'NONE',  ( -1.000000000000000000, -0.000000000000000000, -0.000000000000000000 ) ) ;
#6097=EDGE_LOOP ( 'NONE', ( #48390, #1585, #34799, #105861, #73605, #45556 ) ) ;
#6144=CARTESIAN_POINT ( 'NONE',  ( 19.34999999999999787, 1.533819458162526451E-15, 0.000000000000000000 ) ) ;
#6160=CARTESIAN_POINT ( 'NONE',  ( 9.349999999999997868, -3.309499999999999886, 0.000000000000000000 ) ) ;
#6170=FACE_OUTER_BOUND ( 'NONE', #17710, .T. ) ;
#6183=CARTESIAN_POINT ( 'NONE',  ( 36.08349330513379982, 1.593028355512270962E-15, 0.000000000000000000 ) ) ;
#6193=CARTESIAN_POINT ( 'NONE',  ( 26.08349330513380693, 1.593028355512270962E-15, 0.000000000000000000 ) ) ;
#6203=EDGE_CURVE ( 'NONE', #59582, #48784, #1595, .T. ) ;
#6214=ADVANCED_FACE ( 'NONE', ( #99107 ), #58441, .T. ) ;
#6220=FACE_OUTER_BOUND ( 'NONE', #95538, .T. ) ;
#6226=ADVANCED_FACE ( 'NONE', ( #16614 ), #92091, .F. ) ;
#6251=EDGE_CURVE ( 'NONE', #98662, #78892, #18233, .T. ) ;
#6300=CARTESIAN_POINT ( 'NONE',  ( 5.821900211247815982, 1.420906337213440507, -6.500000000000000888 ) ) ;
#6306=DIRECTION ( 'NONE',  ( 0.000000000000000000, -1.000000000000000000, 0.000000000000000000 ) ) ;
#6312=DIRECTION ( 'NONE',  ( 0.000000000000000000, 0.5000000000000008882, -0.8660254037844381525 ) ) ;
#6383=DIRECTION ( 'NONE',  ( 0.000000000000000000, -1.000000000000000000, 0.000000000000000000 ) ) ;
#6395=CARTESIAN_POINT ( 'NONE',  ( 5.975663821521748353, -7.000939006314043311, -0.8740179403733212560 ) ) ;
#6435=CARTESIAN_POINT ( 'NONE',  ( 26.36650669486618881, 1.474610560812782335E-15, 0.000000000000000000 ) ) ;
#6437=EDGE_LOOP ( 'NONE', ( #77921, #93869, #44205, #16902, #36277 ) ) ;
#6452=CARTESIAN_POINT ( 'NONE',  ( 0.2565376335216121295, -2.516992571280029178, 6.499999999999999112 ) ) ;
#6465=AXIS2_PLACEMENT_3D ( 'NONE', #92433, #58497, #27767 ) ;
#6466=EDGE_LOOP ( 'NONE', ( #82489, #72996, #80241, #28099, #21796, #20538 ) ) ;
#6482=VERTEX_POINT ( 'NONE', #32147 ) ;
#6505=VERTEX_POINT ( 'NONE', #48819 ) ;
#6506=EDGE_CURVE ( 'NONE', #91829, #44978, #36159, .T. ) ;
#6520=ORIENTED_EDGE ( 'NONE', *, *, #104754, .F. ) ;
#6538=DIRECTION ( 'NONE',  ( -0.5735764363510497121, 0.8191520442889892450, 1.003171929053521665E-16 ) ) ;
#6572=ORIENTED_EDGE ( 'NONE', *, *, #42271, .T. ) ;
#6590=AXIS2_PLACEMENT_3D ( 'NONE', #80066, #46130, #11203 ) ;
#6599=ORIENTED_EDGE ( 'NONE', *, *, #102807, .T. ) ;
#6614=CARTESIAN_POINT ( 'NONE',  ( 0.000000000000000000, 0.000000000000000000, 0.000000000000000000 ) ) ;
#6616=ORIENTED_EDGE ( 'NONE', *, *, #81398, .F. ) ;
#6632=AXIS2_PLACEMENT_3D ( 'NONE', #51803, #82583, #16790 ) ;
#6656=FACE_OUTER_BOUND ( 'NONE', #52972, .T. ) ;
#6666=DIRECTION ( 'NONE',  ( 0.000000000000000000, -1.000000000000000000, -1.155626614413199331E-16 ) ) ;
#6672=VECTOR ( 'NONE', #93209, 1000.000000000000000 ) ;
#6710=CARTESIAN_POINT ( 'NONE',  ( 31.36650669486618881, -3.999999999999998224, 0.000000000000000000 ) ) ;
#6726=CIRCLE ( 'NONE', #60120, 4.000000000000000888 ) ;
#6734=ORIENTED_EDGE ( 'NONE', *, *, #70596, .F. ) ;
#6739=ORIENTED_EDGE ( 'NONE', *, *, #103409, .T. ) ;
#6749=ORIENTED_EDGE ( 'NONE', *, *, #37385, .T. ) ;
#6840=CIRCLE ( 'NONE', #44836, 4.000000000000000888 ) ;
#6844=FACE_OUTER_BOUND ( 'NONE', #54156, .T. ) ;
#6859=DIRECTION ( 'NONE',  ( 0.000000000000000000, -1.000000000000000000, 0.000000000000000000 ) ) ;
#6875=DIRECTION ( 'NONE',  ( 1.000000000000000000, 1.224606353822377258E-16, 0.000000000000000000 ) ) ;
#6879=EDGE_LOOP ( 'NONE', ( #11834, #99440, #14654, #42399, #81650 ) ) ;
#6880=FACE_OUTER_BOUND ( 'NONE', #23165, .T. ) ;
#6891=CARTESIAN_POINT ( 'NONE',  ( 0.2573354458087852015, -4.368923434677197903, -5.432802636760778903 ) ) ;
#6921=LINE ( 'NONE', #71649, #80761 ) ;
#6932=CARTESIAN_POINT ( 'NONE',  ( 6.169949891408690767, -4.949864754179316151, -4.426582755168344541 ) ) ;
#6939=CIRCLE ( 'NONE', #62885, 4.000000000000001776 ) ;
#6943=VECTOR ( 'NONE', #45505, 1000.000000000000227 ) ;
#6996=EDGE_CURVE ( 'NONE', #68693, #40430, #97648, .T. ) ;
#7061=VECTOR ( 'NONE', #10181, 1000.000000000000341 ) ;
#7068=CARTESIAN_POINT ( 'NONE',  ( 23.09999999999999432, 1.533819458162526451E-15, 0.000000000000000000 ) ) ;
#7103=DIRECTION ( 'NONE',  ( 0.000000000000000000, -1.000000000000000000, 0.000000000000000000 ) ) ;
#7161=VERTEX_POINT ( 'NONE', #4414 ) ;
#7167=CIRCLE ( 'NONE', #81217, 4.000000000000000888 ) ;
#7254=DIRECTION ( 'NONE',  ( 0.000000000000000000, -1.000000000000000000, 0.000000000000000000 ) ) ;
#7278=CARTESIAN_POINT ( 'NONE',  ( 0.000000000000000000, 7.511572993685796142E-16, -6.500000000000000888 ) ) ;
#7345=CYLINDRICAL_SURFACE ( 'NONE', #46709, 4.000000000000000888 ) ;
#7366=CARTESIAN_POINT ( 'NONE',  ( 23.58349330513380337, 1.593028355512270962E-15, 0.000000000000000000 ) ) ;
#7440=LINE ( 'NONE', #106134, #43050 ) ;
#7471=ORIENTED_EDGE ( 'NONE', *, *, #15064, .T. ) ;
#7479=EDGE_LOOP ( 'NONE', ( #101320, #88875, #64650, #37692, #101755 ) ) ;
#7480=CARTESIAN_POINT ( 'NONE',  ( 33.58349330513380693, 1.593028355512270962E-15, 0.000000000000000000 ) ) ;
#7531=CONICAL_SURFACE ( 'NONE', #102261, 4.000000000000001776, 0.9599310885968774798 ) ;
#7546=DIRECTION ( 'NONE',  ( -1.000000000000000000, -1.224606353822377258E-16, -0.000000000000000000 ) ) ;
#7555=LINE ( 'NONE', #50154, #45415 ) ;
#7558=VECTOR ( 'NONE', #91947, 1000.000000000000227 ) ;
#7567=CARTESIAN_POINT ( 'NONE',  ( 27.33349330513380693, 1.593028355512270962E-15, 0.000000000000000000 ) ) ;
#7572=LINE ( 'NONE', #32432, #39716 ) ;
#7579=EDGE_CURVE ( 'NONE', #81756, #94819, #47760, .T. ) ;
#7585=ORIENTED_EDGE ( 'NONE', *, *, #12565, .T. ) ;
#7595=CARTESIAN_POINT ( 'NONE',  ( 6.936184427528457874, 0.000000000000000000, 0.000000000000000000 ) ) ;
#7599=VERTEX_POINT ( 'NONE', #76314 ) ;
#7627=AXIS2_PLACEMENT_3D ( 'NONE', #8507, #23135, #99100 ) ;
#7628=CARTESIAN_POINT ( 'NONE',  ( 30.59999999999999787, 3.309500000000003439, 0.000000000000000000 ) ) ;
#7636=CARTESIAN_POINT ( 'NONE',  ( 16.08349330513380337, 1.593028355512270962E-15, 0.000000000000000000 ) ) ;
#7640=CARTESIAN_POINT ( 'NONE',  ( 29.34999999999999787, 3.309500000000003439, 0.000000000000000000 ) ) ;
#7647=ORIENTED_EDGE ( 'NONE', *, *, #27581, .F. ) ;
#7655=CARTESIAN_POINT ( 'NONE',  ( 6.207999833770000642, 1.336757187206258024, 6.499999999999995559 ) ) ;
#7676=ORIENTED_EDGE ( 'NONE', *, *, #85240, .T. ) ;
#7687=CARTESIAN_POINT ( 'NONE',  ( 0.000000000000000000, 0.000000000000000000, 4.000000000000000888 ) ) ;
#7689=EDGE_CURVE ( 'NONE', #83796, #78825, #39833, .T. ) ;
#7719=CARTESIAN_POINT ( 'NONE',  ( 31.08349330513380693, 4.000000000000002665, 0.000000000000000000 ) ) ;
#7722=ORIENTED_EDGE ( 'NONE', *, *, #5394, .F. ) ;
#7729=CARTESIAN_POINT ( 'NONE',  ( 32.33349330513380693, 4.000000000000003553, 0.000000000000000000 ) ) ;
#7740=EDGE_CURVE ( 'NONE', #78219, #23042, #74587, .T. ) ;
#7760=ORIENTED_EDGE ( 'NONE', *, *, #99351, .F. ) ;
#7772=DIRECTION ( 'NONE',  ( -1.000000000000000000, -1.224606353822377258E-16, -0.000000000000000000 ) ) ;
#7792=CARTESIAN_POINT ( 'NONE',  ( 6.563035550597769330, -3.302680408004405432, 6.845819698387219709 ) ) ;
#7824=VECTOR ( 'NONE', #51059, 1000.000000000000000 ) ;
#7837=AXIS2_PLACEMENT_3D ( 'NONE', #27361, #60240, #52108 ) ;
#7880=DIRECTION ( 'NONE',  ( -1.000000000000000000, -1.224606353822377258E-16, -0.000000000000000000 ) ) ;
#7885=DIRECTION ( 'NONE',  ( 0.000000000000000000, -1.000000000000000000, 0.000000000000000000 ) ) ;
#7909=ORIENTED_EDGE ( 'NONE', *, *, #91862, .T. ) ;
#7917=CARTESIAN_POINT ( 'NONE',  ( 6.683837171061806082, 7.911893696991936231, -4.595687358162529387E-16 ) ) ;
#7940=DIRECTION ( 'NONE',  ( -1.000000000000000000, -1.224606353822377258E-16, -0.000000000000000000 ) ) ;
#7960=FACE_OUTER_BOUND ( 'NONE', #50183, .T. ) ;
#7989=CONICAL_SURFACE ( 'NONE', #32125, 3.309500000000001663, 0.9599310885968770357 ) ;
#8001=EDGE_LOOP ( 'NONE', ( #11212, #6616, #75140, #85150 ) ) ;
#8002=CARTESIAN_POINT ( 'NONE',  ( 0.5805565836007617886, -3.752776749732566142, 6.499999999999999112 ) ) ;
#8032=DIRECTION ( 'NONE',  ( -1.000000000000000000, -1.224606353822377258E-16, -0.000000000000000000 ) ) ;
#8034=VERTEX_POINT ( 'NONE', #72857 ) ;
#8042=AXIS2_PLACEMENT_3D ( 'NONE', #47746, #80645, #23520 ) ;
#8054=VERTEX_POINT ( 'NONE', #57732 ) ;
#8070=VECTOR ( 'NONE', #26884, 1000.000000000000000 ) ;
#8078=EDGE_CURVE ( 'NONE', #6505, #72376, #17314, .T. ) ;
#8090=CARTESIAN_POINT ( 'NONE',  ( 32.33349330513380693, 4.898587196589411843E-16, -4.000000000000001776 ) ) ;
#8120=EDGE_CURVE ( 'NONE', #52389, #93666, #55347, .T. ) ;
#8152=EDGE_CURVE ( 'NONE', #63779, #74653, #101928, .T. ) ;
#8201=CARTESIAN_POINT ( 'NONE',  ( 18.09999999999999787, 3.309500000000003439, 4.052968581778167743E-16 ) ) ;
#8217=CARTESIAN_POINT ( 'NONE',  ( 15.59999999999999787, 1.533819458162526451E-15, 0.000000000000000000 ) ) ;
#8241=DIRECTION ( 'NONE',  ( 0.000000000000000000, -1.000000000000000000, 0.000000000000000000 ) ) ;
#8243=EDGE_CURVE ( 'NONE', #59988, #65549, #36187, .T. ) ;
#8278=DIRECTION ( 'NONE',  ( -1.000000000000000000, -1.224606353822377258E-16, -0.000000000000000000 ) ) ;
#8297=VERTEX_POINT ( 'NONE', #21065 ) ;
#8303=DIRECTION ( 'NONE',  ( 0.000000000000000000, 0.000000000000000000, 1.000000000000000000 ) ) ;
#8332=CARTESIAN_POINT ( 'NONE',  ( 6.289692432696784685, 1.244853941008388061E-13, 6.828989928337166226 ) ) ;
#8349=VERTEX_POINT ( 'NONE', #45307 ) ;
#8383=ADVANCED_FACE ( 'NONE', ( #29677 ), #53358, .F. ) ;
#8425=CARTESIAN_POINT ( 'NONE',  ( 6.463481858019718196, -7.246446802359425732, 1.128819432756289265 ) ) ;
#8428=EDGE_CURVE ( 'NONE', #9982, #49600, #73654, .T. ) ;
#8464=CARTESIAN_POINT ( 'NONE',  ( 25.59999999999999787, 1.533819458162526451E-15, 0.000000000000000000 ) ) ;
#8484=CARTESIAN_POINT ( 'NONE',  ( 0.05533025579362397389, -4.993776679985862721, -4.350525068611871049 ) ) ;
#8485=DIRECTION ( 'NONE',  ( 1.000000000000000000, 0.000000000000000000, 0.000000000000000000 ) ) ;
#8487=DIRECTION ( 'NONE',  ( 0.000000000000000000, -1.000000000000000000, 0.000000000000000000 ) ) ;
#8491=CIRCLE ( 'NONE', #22316, 4.000000000000001776 ) ;
#8507=CARTESIAN_POINT ( 'NONE',  ( 37.33349330513379982, 1.593028355512270962E-15, 0.000000000000000000 ) ) ;
#8514=CARTESIAN_POINT ( 'NONE',  ( 0.05533025579362068486, 4.993776679985853839, 4.350525068611871049 ) ) ;
#8517=DIRECTION ( 'NONE',  ( 0.000000000000000000, -1.000000000000000000, 0.000000000000000000 ) ) ;
#8523=CARTESIAN_POINT ( 'NONE',  ( 33.09999999999999432, 1.533819458162526451E-15, 0.000000000000000000 ) ) ;
#8525=DIRECTION ( 'NONE',  ( 0.000000000000000000, -1.000000000000000000, 0.000000000000000000 ) ) ;
#8536=AXIS2_PLACEMENT_3D ( 'NONE', #25827, #40892, #75915 ) ;
#8576=ORIENTED_EDGE ( 'NONE', *, *, #61439, .F. ) ;
#8588=EDGE_LOOP ( 'NONE', ( #31358, #421, #38366, #28637, #12046, #37330 ) ) ;
#8589=EDGE_LOOP ( 'NONE', ( #27059, #102351, #73348, #102889, #66390 ) ) ;
#8595=ORIENTED_EDGE ( 'NONE', *, *, #29745, .F. ) ;
#8606=ADVANCED_FACE ( 'NONE', ( #4052 ), #49500, .T. ) ;
#8620=CARTESIAN_POINT ( 'NONE',  ( 0.000000000000000000, 0.000000000000000000, 0.000000000000000000 ) ) ;
#8628=EDGE_CURVE ( 'NONE', #45785, #49640, #35930, .T. ) ;
#8650=AXIS2_PLACEMENT_3D ( 'NONE', #48877, #41330, #81767 ) ;
#8656=ORIENTED_EDGE ( 'NONE', *, *, #3338, .F. ) ;
#8666=AXIS2_PLACEMENT_3D ( 'NONE', #81814, #16040, #97475 ) ;
#8679=EDGE_CURVE ( 'NONE', #21783, #36385, #1528, .T. ) ;
#8691=DIRECTION ( 'NONE',  ( 0.000000000000000000, -1.000000000000000000, 0.000000000000000000 ) ) ;
#8703=ORIENTED_EDGE ( 'NONE', *, *, #22621, .F. ) ;
#8719=CIRCLE ( 'NONE', #24312, 3.309500000000001663 ) ;
#8732=CARTESIAN_POINT ( 'NONE',  ( 6.172110426325241761, -1.395451528107193750, 6.499999999999999112 ) ) ;
#8740=EDGE_CURVE ( 'NONE', #20995, #90030, #77034, .T. ) ;
#8808=EDGE_LOOP ( 'NONE', ( #8576, #36368, #52052, #61773, #84999, #42351 ) ) ;
#8810=ADVANCED_FACE ( 'NONE', ( #44146 ), #40885, .T. ) ;
#8815=FACE_OUTER_BOUND ( 'NONE', #24146, .T. ) ;
#8828=VERTEX_POINT ( 'NONE', #12818 ) ;
#8830=DIRECTION ( 'NONE',  ( 0.000000000000000000, -1.000000000000000000, 0.000000000000000000 ) ) ;
#8848=EDGE_CURVE ( 'NONE', #66028, #81895, #34062, .T. ) ;
#8859=CIRCLE ( 'NONE', #32987, 4.000000000000000888 ) ;
#8861=CARTESIAN_POINT ( 'NONE',  ( 29.34999999999999787, 1.533819458162526451E-15, 0.000000000000000000 ) ) ;
#8866=CONICAL_SURFACE ( 'NONE', #82702, 6.500000000000000000, 1.047197551196600296 ) ;
#8907=ORIENTED_EDGE ( 'NONE', *, *, #6251, .T. ) ;
#8920=FACE_OUTER_BOUND ( 'NONE', #21393, .T. ) ;
#8931=AXIS2_PLACEMENT_3D ( 'NONE', #58109, #73759, #57561 ) ;
#8933=DIRECTION ( 'NONE',  ( 0.000000000000000000, 0.000000000000000000, 1.000000000000000000 ) ) ;
#8935=EDGE_CURVE ( 'NONE', #44704, #23042, #75367, .T. ) ;
#8951=CARTESIAN_POINT ( 'NONE',  ( 35.11650669486618170, 4.000000000000003553, 4.898587196589414801E-16 ) ) ;
#8952=CARTESIAN_POINT ( 'NONE',  ( 6.683837171061806970, -7.911893696991936231, 5.688671339918660213E-17 ) ) ;
#8965=CIRCLE ( 'NONE', #22784, 4.000000000000000888 ) ;
#9021=CIRCLE ( 'NONE', #38318, 4.000000000000001776 ) ;
#9028=ORIENTED_EDGE ( 'NONE', *, *, #17009, .F. ) ;
#9040=CARTESIAN_POINT ( 'NONE',  ( 29.34999999999999787, -3.309499999999999886, 0.000000000000000000 ) ) ;
#9084=CARTESIAN_POINT ( 'NONE',  ( 32.33349330513380693, 1.593028355512270962E-15, 0.000000000000000000 ) ) ;
#9118=VERTEX_POINT ( 'NONE', #34896 ) ;
#9148=VERTEX_POINT ( 'NONE', #1401 ) ;
#9204=EDGE_CURVE ( 'NONE', #94380, #96401, #85373, .T. ) ;
#9246=ORIENTED_EDGE ( 'NONE', *, *, #73938, .T. ) ;
#9254=CARTESIAN_POINT ( 'NONE',  ( 6.692428679880671361, -4.002209756868625234, 6.852332176615682613 ) ) ;
#9323=ORIENTED_EDGE ( 'NONE', *, *, #97404, .T. ) ;
#9332=CARTESIAN_POINT ( 'NONE',  ( 6.463344223170839342, 4.601472318010338292, -5.710032555828796319 ) ) ;
#9343=ORIENTED_EDGE ( 'NONE', *, *, #64885, .T. ) ;
#9356=CARTESIAN_POINT ( 'NONE',  ( 28.09999999999999787, 1.533819458162526451E-15, 0.000000000000000000 ) ) ;
#9371=CIRCLE ( 'NONE', #5992, 3.309500000000001663 ) ;
#9385=DIRECTION ( 'NONE',  ( 0.000000000000000000, 0.000000000000000000, 1.000000000000000000 ) ) ;
#9386=CARTESIAN_POINT ( 'NONE',  ( 0.000000000000000000, 4.898587196589413815E-16, -4.000000000000000888 ) ) ;
#9405=CIRCLE ( 'NONE', #69717, 4.000000000000001776 ) ;
#9461=CARTESIAN_POINT ( 'NONE',  ( 30.59999999999999787, 1.533819458162526451E-15, 0.000000000000000000 ) ) ;
#9503=CARTESIAN_POINT ( 'NONE',  ( 6.562934840145638660, 4.277581483015135966, 6.282640795011893431 ) ) ;
#9538=AXIS2_PLACEMENT_3D ( 'NONE', #56489, #105581, #96449 ) ;
#9553=EDGE_CURVE ( 'NONE', #90138, #30441, #22575, .T. ) ;
#9567=CARTESIAN_POINT ( 'NONE',  ( 0.000000000000000000, 7.505553499465140277, -3.755786496842903002E-16 ) ) ;
#9596=AXIS2_PLACEMENT_3D ( 'NONE', #10151, #58720, #99694 ) ;
#9601=ORIENTED_EDGE ( 'NONE', *, *, #53684, .F. ) ;
#9631=DIRECTION ( 'NONE',  ( -1.000000000000000000, -0.000000000000000000, -0.000000000000000000 ) ) ;
#9656=LINE ( 'NONE', #42568, #28868 ) ;
#9691=ADVANCED_FACE ( 'NONE', ( #52372 ), #21575, .T. ) ;
#9693=AXIS2_PLACEMENT_3D ( 'NONE', #97083, #47988, #73323 ) ;
#9703=DIRECTION ( 'NONE',  ( 0.000000000000000000, -1.155626614413199331E-16, 1.000000000000000000 ) ) ;
#9715=CARTESIAN_POINT ( 'NONE',  ( 0.000000000000000000, 0.000000000000000000, 0.000000000000000000 ) ) ;
#9756=ORIENTED_EDGE ( 'NONE', *, *, #62642, .F. ) ;
#9782=CARTESIAN_POINT ( 'NONE',  ( 37.33349330513379982, -4.000000000000000000, 4.898587196589415787E-16 ) ) ;
#9808=ORIENTED_EDGE ( 'NONE', *, *, #98751, .T. ) ;
#9811=CONICAL_SURFACE ( 'NONE', #87298, 3.309500000000001663, 0.9599310885968770357 ) ;
#9816=CARTESIAN_POINT ( 'NONE',  ( 6.289692432696784685, 1.244853941008388061E-13, 6.828989928337166226 ) ) ;
#9822=CIRCLE ( 'NONE', #87384, 6.500000000000000888 ) ;
#9842=CARTESIAN_POINT ( 'NONE',  ( 21.84999999999999787, -3.309499999999999886, 0.000000000000000000 ) ) ;
#9843=ORIENTED_EDGE ( 'NONE', *, *, #16347, .T. ) ;
#9869=CARTESIAN_POINT ( 'NONE',  ( 30.11650669486618881, 1.474610560812782335E-15, 0.000000000000000000 ) ) ;
#9872=DIRECTION ( 'NONE',  ( -1.000000000000000000, -1.224606353822377258E-16, -0.000000000000000000 ) ) ;
#9908=ORIENTED_EDGE ( 'NONE', *, *, #104404, .F. ) ;
#9955=CARTESIAN_POINT ( 'NONE',  ( 8.099999999999999645, -7.505553499465142053, -3.129864801432410934E-16 ) ) ;
#9982=VERTEX_POINT ( 'NONE', #4114 ) ;
#10015=AXIS2_PLACEMENT_3D ( 'NONE', #28407, #1543, #37031 ) ;
#10028=EDGE_CURVE ( 'NONE', #78219, #90250, #102553, .T. ) ;
#10067=CIRCLE ( 'NONE', #60059, 4.000000000000000888 ) ;
#10112=CARTESIAN_POINT ( 'NONE',  ( 8.099999999999999645, 3.752776749732562589, -6.500000000000000888 ) ) ;
#10151=CARTESIAN_POINT ( 'NONE',  ( 31.08349330513380693, 1.593028355512270962E-15, 0.000000000000000000 ) ) ;
#10181=DIRECTION ( 'NONE',  ( 0.5735764363510490460, 0.8191520442889896891, 0.000000000000000000 ) ) ;
#10229=ADVANCED_FACE ( 'NONE', ( #79582 ), #36521, .T. ) ;
#10241=DIRECTION ( 'NONE',  ( 0.000000000000000000, -1.000000000000000000, 0.000000000000000000 ) ) ;
#10321=CARTESIAN_POINT ( 'NONE',  ( 17.61650669486618881, 0.000000000000000000, 4.000000000000000888 ) ) ;
#10326=DIRECTION ( 'NONE',  ( -1.000000000000000000, -1.224606353822377258E-16, -0.000000000000000000 ) ) ;
#10330=CARTESIAN_POINT ( 'NONE',  ( 13.58349330513380515, 4.000000000000002665, 0.000000000000000000 ) ) ;
#10348=VECTOR ( 'NONE', #71420, 1000.000000000000341 ) ;
#10388=CARTESIAN_POINT ( 'NONE',  ( 33.09999999999999432, 1.533819458162526451E-15, 0.000000000000000000 ) ) ;
#10400=B_SPLINE_CURVE_WITH_KNOTS ( 'NONE', 3,
 ( #96735, #105867, #14726, #97771, #47096, #55703, #80526, #72960, #72445, #105349 ),
 .UNSPECIFIED., .F., .F.,
 ( 4, 2, 2, 2, 4 ),
 ( 0.000000000000000000, 0.001993803085173303461, 0.003987606170346606922, 0.005981409255519910817, 0.007975212340693213844 ),
 .UNSPECIFIED. ) ;
#10451=ORIENTED_EDGE ( 'NONE', *, *, #49462, .F. ) ;
#10487=ORIENTED_EDGE ( 'NONE', *, *, #55753, .F. ) ;
#10544=ORIENTED_EDGE ( 'NONE', *, *, #84423, .F. ) ;
#10545=CARTESIAN_POINT ( 'NONE',  ( 16.08349330513380337, 4.000000000000002665, 0.000000000000000000 ) ) ;
#10549=DIRECTION ( 'NONE',  ( -1.000000000000000000, -1.224606353822377258E-16, -0.000000000000000000 ) ) ;
#10550=ORIENTED_EDGE ( 'NONE', *, *, #61861, .F. ) ;
#10568=CARTESIAN_POINT ( 'NONE',  ( 0.000000000000000000, 0.000000000000000000, 0.000000000000000000 ) ) ;
#10573=ORIENTED_EDGE ( 'NONE', *, *, #45932, .F. ) ;
#10589=ORIENTED_EDGE ( 'NONE', *, *, #80650, .F. ) ;
#10592=DIRECTION ( 'NONE',  ( -1.000000000000000000, -1.224606353822377258E-16, -0.000000000000000000 ) ) ;
#10606=CARTESIAN_POINT ( 'NONE',  ( 17.61650669486618881, 1.474610560812782335E-15, 0.000000000000000000 ) ) ;
#10629=FACE_OUTER_BOUND ( 'NONE', #97010, .T. ) ;
#10645=CARTESIAN_POINT ( 'NONE',  ( 6.692588830498428898, -7.935834885954430540, 0.04058884017440032160 ) ) ;
#10681=DIRECTION ( 'NONE',  ( -0.5735764363510497121, 0.8191520442889892450, 1.003171929053521665E-16 ) ) ;
#10699=LINE ( 'NONE', #83011, #28978 ) ;
#10705=EDGE_LOOP ( 'NONE', ( #24940, #73315, #57812, #55537, #103982, #31203 ) ) ;
#10725=EDGE_LOOP ( 'NONE', ( #38492, #67256, #14380, #73212, #92357, #83629, #98527 ) ) ;
#10728=AXIS2_PLACEMENT_3D ( 'NONE', #14983, #57033, #47878 ) ;
#10731=CARTESIAN_POINT ( 'NONE',  ( 27.33349330513380693, -3.851859888774471706E-31, 4.000000000000001776 ) ) ;
#10760=ADVANCED_FACE ( 'NONE', ( #615 ), #87257, .T. ) ;
#10815=DIRECTION ( 'NONE',  ( 1.000000000000000000, 1.224606353822377258E-16, 0.000000000000000000 ) ) ;
#10868=CARTESIAN_POINT ( 'NONE',  ( 36.36650669486618881, 1.474610560812782335E-15, 0.000000000000000000 ) ) ;
#10901=ADVANCED_FACE ( 'NONE', ( #62118 ), #82072, .T. ) ;
#10910=DIRECTION ( 'NONE',  ( 0.000000000000000000, -1.000000000000000000, 0.000000000000000000 ) ) ;
#10922=FACE_OUTER_BOUND ( 'NONE', #64720, .T. ) ;
#10937=VERTEX_POINT ( 'NONE', #36790 ) ;
#10939=EDGE_LOOP ( 'NONE', ( #40120, #69321, #18396, #3461, #35198, #12468 ) ) ;
#10972=EDGE_CURVE ( 'NONE', #47749, #49640, #37322, .T. ) ;
#10997=DIRECTION ( 'NONE',  ( -1.000000000000000000, -0.000000000000000000, -0.000000000000000000 ) ) ;
#11008=AXIS2_PLACEMENT_3D ( 'NONE', #99832, #85255, #69087 ) ;
#11031=CIRCLE ( 'NONE', #23086, 3.309500000000001663 ) ;
#11068=LINE ( 'NONE', #43991, #40795 ) ;
#11071=CIRCLE ( 'NONE', #71369, 4.000000000000001776 ) ;
#11081=LINE ( 'NONE', #95225, #100697 ) ;
#11120=VERTEX_POINT ( 'NONE', #51190 ) ;
#11179=VERTEX_POINT ( 'NONE', #10731 ) ;
#11194=ORIENTED_EDGE ( 'NONE', *, *, #31479, .T. ) ;
#11203=DIRECTION ( 'NONE',  ( 0.000000000000000000, -1.000000000000000000, 0.000000000000000000 ) ) ;
#11212=ORIENTED_EDGE ( 'NONE', *, *, #67044, .F. ) ;
#11216=AXIS2_PLACEMENT_3D ( 'NONE', #49970, #59683, #82879 ) ;
#11217=DIRECTION ( 'NONE',  ( 0.000000000000000000, 1.000000000000000000, 0.000000000000000000 ) ) ;
#11269=CARTESIAN_POINT ( 'NONE',  ( 10.11650669486618881, 4.898587196589413815E-16, -4.000000000000000888 ) ) ;
#11273=CARTESIAN_POINT ( 'NONE',  ( 26.36650669486618881, 1.474610560812782335E-15, 0.000000000000000000 ) ) ;
#11281=CARTESIAN_POINT ( 'NONE',  ( 35.59999999999999432, 3.309500000000003439, 4.052968581778167743E-16 ) ) ;
#11290=CARTESIAN_POINT ( 'NONE',  ( 6.333820801330769967, 6.982605850970919903, -0.9057718968924614034 ) ) ;
#11332=FACE_OUTER_BOUND ( 'NONE', #75251, .T. ) ;
#11350=DIRECTION ( 'NONE',  ( -1.000000000000000000, -1.224606353822377258E-16, -0.000000000000000000 ) ) ;
#11359=CIRCLE ( 'NONE', #28667, 4.000000000000001776 ) ;
#11369=VERTEX_POINT ( 'NONE', #14982 ) ;
#11403=AXIS2_PLACEMENT_3D ( 'NONE', #4071, #10549, #43468 ) ;
#11418=DIRECTION ( 'NONE',  ( -1.000000000000000000, -1.224606353822377258E-16, -0.000000000000000000 ) ) ;
#11423=ADVANCED_FACE ( 'NONE', ( #59592 ), #1851, .F. ) ;
#11443=AXIS2_PLACEMENT_3D ( 'NONE', #16616, #49509, #389 ) ;
#11446=CONICAL_SURFACE ( 'NONE', #97604, 4.000000000000001776, 0.9599310885968774798 ) ;
#11447=CARTESIAN_POINT ( 'NONE',  ( 6.326416241096633364, 1.324101276589543907, 6.831531844319973068 ) ) ;
#11448=DIRECTION ( 'NONE',  ( 0.000000000000000000, 0.000000000000000000, 1.000000000000000000 ) ) ;
#11472=DIRECTION ( 'NONE',  ( -1.000000000000000000, -1.224606353822377258E-16, -0.000000000000000000 ) ) ;
#11490=EDGE_LOOP ( 'NONE', ( #41850, #99313, #52370, #96284, #2775 ) ) ;
#11506=ORIENTED_EDGE ( 'NONE', *, *, #98674, .T. ) ;
#11538=ORIENTED_EDGE ( 'NONE', *, *, #14486, .F. ) ;
#11545=( NAMED_UNIT ( * ) SI_UNIT ( $, .STERADIAN. ) SOLID_ANGLE_UNIT ( ) );
#11561=DIRECTION ( 'NONE',  ( 0.5735764363510491570, -0.8191520442889895781, 1.003171929053522035E-16 ) ) ;
#11572=AXIS2_PLACEMENT_3D ( 'NONE', #76629, #68570, #101455 ) ;
#11586=DIRECTION ( 'NONE',  ( -1.000000000000000000, -1.224606353822377258E-16, -0.000000000000000000 ) ) ;
#11592=AXIS2_PLACEMENT_3D ( 'NONE', #1776, #9872, #42785 ) ;
#11601=DIRECTION ( 'NONE',  ( -1.000000000000000000, -1.224606353822377258E-16, -0.000000000000000000 ) ) ;
#11603=AXIS2_PLACEMENT_3D ( 'NONE', #105719, #47480, #80378 ) ;
#11676=CARTESIAN_POINT ( 'NONE',  ( 23.86650669486618881, 4.898587196589413815E-16, -4.000000000000000888 ) ) ;
#11708=EDGE_LOOP ( 'NONE', ( #31154, #14243, #48133, #97883, #6739 ) ) ;
#11714=VECTOR ( 'NONE', #91454, 1000.000000000000227 ) ;
#11722=DIRECTION ( 'NONE',  ( -1.000000000000000000, -1.224606353822377258E-16, -0.000000000000000000 ) ) ;
#11731=DIRECTION ( 'NONE',  ( 0.000000000000000000, -1.000000000000000000, 0.000000000000000000 ) ) ;
#11752=DIRECTION ( 'NONE',  ( 0.5735764363510491570, -0.8191520442889895781, 1.003171929053522035E-16 ) ) ;
#11759=LINE ( 'NONE', #28005, #83784 ) ;
#11781=ORIENTED_EDGE ( 'NONE', *, *, #52348, .F. ) ;
#11789=CARTESIAN_POINT ( 'NONE',  ( 34.35000000000000142, -3.309499999999999886, 4.475777889183790779E-16 ) ) ;
#11800=DIRECTION ( 'NONE',  ( -1.000000000000000000, -0.000000000000000000, -0.000000000000000000 ) ) ;
#11833=CARTESIAN_POINT ( 'NONE',  ( 6.692588830498428898, 7.935834885954428763, 0.04058884017440190367 ) ) ;
#11834=ORIENTED_EDGE ( 'NONE', *, *, #18357, .F. ) ;
#11863=AXIS2_PLACEMENT_3D ( 'NONE', #33566, #91273, #601 ) ;
#11885=VERTEX_POINT ( 'NONE', #60756 ) ;
#11895=FACE_OUTER_BOUND ( 'NONE', #85593, .T. ) ;
#11909=ORIENTED_EDGE ( 'NONE', *, *, #26014, .F. ) ;
#11914=ORIENTED_EDGE ( 'NONE', *, *, #1883, .T. ) ;
#11955=FACE_OUTER_BOUND ( 'NONE', #43102, .T. ) ;
#11961=AXIS2_PLACEMENT_3D ( 'NONE', #5531, #102643, #21231 ) ;
#11974=ORIENTED_EDGE ( 'NONE', *, *, #41169, .T. ) ;
#11988=DIRECTION ( 'NONE',  ( -1.000000000000000000, -1.224606353822377258E-16, -0.000000000000000000 ) ) ;
#11995=VECTOR ( 'NONE', #105669, 1000.000000000000000 ) ;
#12018=FACE_OUTER_BOUND ( 'NONE', #31574, .T. ) ;
#12041=DIRECTION ( 'NONE',  ( 0.000000000000000000, 1.000000000000000000, 0.000000000000000000 ) ) ;
#12046=ORIENTED_EDGE ( 'NONE', *, *, #84386, .F. ) ;
#12048=AXIS2_PLACEMENT_3D ( 'NONE', #16375, #81620, #89752 ) ;
#12056=EDGE_LOOP ( 'NONE', ( #13839, #104149, #99801, #24516, #13960, #69049 ) ) ;
#12061=CARTESIAN_POINT ( 'NONE',  ( 0.000000000000000000, 0.000000000000000000, 0.000000000000000000 ) ) ;
#12131=ORIENTED_EDGE ( 'NONE', *, *, #4690, .T. ) ;
#12165=ORIENTED_EDGE ( 'NONE', *, *, #64885, .F. ) ;
#12209=CARTESIAN_POINT ( 'NONE',  ( 29.83349330513380693, 1.593028355512270962E-15, 0.000000000000000000 ) ) ;
#12263=ORIENTED_EDGE ( 'NONE', *, *, #77116, .F. ) ;
#12274=DIRECTION ( 'NONE',  ( -1.000000000000000000, -1.224606353822377258E-16, -0.000000000000000000 ) ) ;
#12279=AXIS2_PLACEMENT_3D ( 'NONE', #73128, #82303, #815 ) ;
#12289=AXIS2_PLACEMENT_3D ( 'NONE', #97268, #9703, #6666 ) ;
#12329=ORIENTED_EDGE ( 'NONE', *, *, #81028, .T. ) ;
#12353=ADVANCED_FACE ( 'NONE', ( #1815 ), #17065, .T. ) ;
#12365=LINE ( 'NONE', #27545, #17312 ) ;
#12370=DIRECTION ( 'NONE',  ( -1.000000000000000000, -0.000000000000000000, -0.000000000000000000 ) ) ;
#12422=DIRECTION ( 'NONE',  ( -1.000000000000000000, -1.224606353822377258E-16, -0.000000000000000000 ) ) ;
#12431=AXIS2_PLACEMENT_3D ( 'NONE', #79678, #64052, #62978 ) ;
#12434=CARTESIAN_POINT ( 'NONE',  ( 6.162888688655344005, 3.752776749732565253, 6.499999999999997335 ) ) ;
#12450=EDGE_CURVE ( 'NONE', #61515, #68693, #57932, .T. ) ;
#12454=DIRECTION ( 'NONE',  ( -1.000000000000000000, -0.000000000000000000, -0.000000000000000000 ) ) ;
#12468=ORIENTED_EDGE ( 'NONE', *, *, #17693, .F. ) ;
#12473=VECTOR ( 'NONE', #88406, 1000.000000000000000 ) ;
#12511=DIRECTION ( 'NONE',  ( -1.000000000000000000, -1.224606353822377258E-16, -0.000000000000000000 ) ) ;
#12541=CYLINDRICAL_SURFACE ( 'NONE', #56201, 4.000000000000000888 ) ;
#12559=AXIS2_PLACEMENT_3D ( 'NONE', #84232, #10326, #35173 ) ;
#12565=EDGE_CURVE ( 'NONE', #21060, #70045, #16293, .T. ) ;
#12604=PRESENTATION_STYLE_ASSIGNMENT (( #103234 ) ) ;
#12616=CIRCLE ( 'NONE', #98691, 4.000000000000001776 ) ;
#12626=EDGE_CURVE ( 'NONE', #60578, #48387, #43797, .T. ) ;
#12679=CYLINDRICAL_SURFACE ( 'NONE', #75616, 4.000000000000000888 ) ;
#12755=CARTESIAN_POINT ( 'NONE',  ( 6.162888688655344893, -3.752776749732565253, 6.499999999999999112 ) ) ;
#12758=EDGE_CURVE ( 'NONE', #87964, #54573, #58379, .T. ) ;
#12761=DIRECTION ( 'NONE',  ( -1.000000000000000000, -1.224606353822377258E-16, -0.000000000000000000 ) ) ;
#12766=DIRECTION ( 'NONE',  ( -1.000000000000000000, -0.000000000000000000, -0.000000000000000000 ) ) ;
#12777=ADVANCED_FACE ( 'NONE', ( #1144 ), #61876, .T. ) ;
#12814=LINE ( 'NONE', #78092, #70608 ) ;
#12816=LINE ( 'NONE', #71064, #31524 ) ;
#12818=CARTESIAN_POINT ( 'NONE',  ( 38.09999999999998721, 4.475777889183789793E-16, -3.309499999999999886 ) ) ;
#12821=VERTEX_POINT ( 'NONE', #58354 ) ;
#12835=LINE ( 'NONE', #21506, #52487 ) ;
#12849=AXIS2_PLACEMENT_3D ( 'NONE', #65467, #8278, #16372 ) ;
#12881=EDGE_CURVE ( 'NONE', #51129, #84766, #37325, .T. ) ;
#12897=CIRCLE ( 'NONE', #54243, 4.000000000000001776 ) ;
#12911=LINE ( 'NONE', #29682, #26460 ) ;
#12919=VECTOR ( 'NONE', #9631, 1000.000000000000000 ) ;
#12927=ORIENTED_EDGE ( 'NONE', *, *, #43625, .F. ) ;
#12929=DIRECTION ( 'NONE',  ( 0.000000000000000000, -1.000000000000000000, 0.000000000000000000 ) ) ;
#13038=CARTESIAN_POINT ( 'NONE',  ( 18.09999999999999787, 1.533819458162526451E-15, 0.000000000000000000 ) ) ;
#13044=DIRECTION ( 'NONE',  ( 1.000000000000000000, 1.224606353822377258E-16, 0.000000000000000000 ) ) ;
#13095=DIRECTION ( 'NONE',  ( 1.000000000000000000, 1.224606353822377258E-16, 0.000000000000000000 ) ) ;
#13096=CARTESIAN_POINT ( 'NONE',  ( 8.099999999999999645, 0.000000000000000000, 4.000000000000000888 ) ) ;
#13113=CARTESIAN_POINT ( 'NONE',  ( 30.11650669486618881, 4.898587196589413815E-16, -4.000000000000000888 ) ) ;
#13178=EDGE_CURVE ( 'NONE', #66028, #83796, #99471, .T. ) ;
#13206=DIRECTION ( 'NONE',  ( 0.000000000000000000, -1.000000000000000000, 0.000000000000000000 ) ) ;
#13227=LINE ( 'NONE', #47715, #27565 ) ;
#13293=CIRCLE ( 'NONE', #71901, 8.400000000000000355 ) ;
#13305=AXIS2_PLACEMENT_3D ( 'NONE', #67882, #85130, #11217 ) ;
#13306=EDGE_CURVE ( 'NONE', #55271, #77629, #61159, .T. ) ;
#13320=AXIS2_PLACEMENT_3D ( 'NONE', #54579, #104744, #7103 ) ;
#13360=ORIENTED_EDGE ( 'NONE', *, *, #8628, .F. ) ;
#13388=ORIENTED_EDGE ( 'NONE', *, *, #17425, .T. ) ;
#13408=VECTOR ( 'NONE', #89731, 1000.000000000000000 ) ;
#13446=CARTESIAN_POINT ( 'NONE',  ( 16.08349330513380337, 1.593028355512270962E-15, 0.000000000000000000 ) ) ;
#13538=FACE_OUTER_BOUND ( 'NONE', #89932, .T. ) ;
#13633=DIRECTION ( 'NONE',  ( 0.000000000000000000, 0.000000000000000000, 1.000000000000000000 ) ) ;
#13649=CARTESIAN_POINT ( 'NONE',  ( 6.281178480976150169, 7.505553499465141165, 5.007024290797836712E-17 ) ) ;
#13693=CIRCLE ( 'NONE', #22368, 4.000000000000001776 ) ;
#13697=LINE ( 'NONE', #5097, #101644 ) ;
#13698=EDGE_CURVE ( 'NONE', #39211, #64041, #56020, .T. ) ;
#13705=DIRECTION ( 'NONE',  ( -1.000000000000000000, -1.224606353822377258E-16, -0.000000000000000000 ) ) ;
#13724=CARTESIAN_POINT ( 'NONE',  ( -3.294958164819228319E-15, 5.948846446048902337, -2.696295709017757503 ) ) ;
#13744=DIRECTION ( 'NONE',  ( 0.000000000000000000, 0.000000000000000000, 1.000000000000000000 ) ) ;
#13825=AXIS2_PLACEMENT_3D ( 'NONE', #88876, #106639, #95911 ) ;
#13839=ORIENTED_EDGE ( 'NONE', *, *, #41645, .T. ) ;
#13841=CARTESIAN_POINT ( 'NONE',  ( 9.833493305133805151, -4.000000000000000888, 4.898587196589416773E-16 ) ) ;
#13849=CARTESIAN_POINT ( 'NONE',  ( 27.33349330513380693, 1.593028355512270962E-15, 0.000000000000000000 ) ) ;
#13859=VECTOR ( 'NONE', #90855, 1000.000000000000227 ) ;
#13893=DIRECTION ( 'NONE',  ( -0.5735764363510497121, 0.8191520442889892450, 1.003171929053521665E-16 ) ) ;
#13897=ORIENTED_EDGE ( 'NONE', *, *, #97311, .F. ) ;
#13900=CIRCLE ( 'NONE', #29438, 4.000000000000001776 ) ;
#13930=CARTESIAN_POINT ( 'NONE',  ( 6.394337469123806628, -7.552703473009533042, -1.902911509106785533E-15 ) ) ;
#13946=CARTESIAN_POINT ( 'NONE',  ( 0.000000000000000000, 4.898587196589413815E-16, -4.000000000000000888 ) ) ;
#13960=ORIENTED_EDGE ( 'NONE', *, *, #40811, .F. ) ;
#13974=DIRECTION ( 'NONE',  ( 0.000000000000000000, 1.000000000000000000, 0.000000000000000000 ) ) ;
#13979=EDGE_LOOP ( 'NONE', ( #33977, #16376, #57665, #81588, #95670 ) ) ;
#14184=ORIENTED_EDGE ( 'NONE', *, *, #27581, .T. ) ;
#14243=ORIENTED_EDGE ( 'NONE', *, *, #81063, .F. ) ;
#14244=CIRCLE ( 'NONE', #74542, 8.605212085995399107 ) ;
#14248=ADVANCED_FACE ( 'NONE', ( #18490 ), #51353, .T. ) ;
#14285=DIRECTION ( 'NONE',  ( 0.000000000000000000, -1.000000000000000000, 0.000000000000000000 ) ) ;
#14293=CARTESIAN_POINT ( 'NONE',  ( 6.463647488011506681, -2.646730816809992781, 6.840026438643557860 ) ) ;
#14298=ORIENTED_EDGE ( 'NONE', *, *, #718, .F. ) ;
#14307=EDGE_CURVE ( 'NONE', #27343, #55436, #19044, .T. ) ;
#14317=AXIS2_PLACEMENT_3D ( 'NONE', #58544, #34828, #17560 ) ;
#14319=LINE ( 'NONE', #21401, #51333 ) ;
#14372=FACE_OUTER_BOUND ( 'NONE', #78226, .T. ) ;
#14375=CARTESIAN_POINT ( 'NONE',  ( 18.58349330513380693, 4.000000000000003553, 0.000000000000000000 ) ) ;
#14380=ORIENTED_EDGE ( 'NONE', *, *, #28397, .T. ) ;
#14399=CARTESIAN_POINT ( 'NONE',  ( 19.83349330513380693, 1.593028355512270962E-15, 0.000000000000000000 ) ) ;
#14400=DIRECTION ( 'NONE',  ( 0.000000000000000000, -0.8660254037844381525, -0.5000000000000008882 ) ) ;
#14440=DIRECTION ( 'NONE',  ( 0.000000000000000000, 1.000000000000000000, 0.000000000000000000 ) ) ;
#14445=VERTEX_POINT ( 'NONE', #74579 ) ;
#14465=CARTESIAN_POINT ( 'NONE',  ( 14.34999999999999787, 1.533819458162526451E-15, 0.000000000000000000 ) ) ;
#14476=EDGE_LOOP ( 'NONE', ( #21508, #35453, #44270, #38876, #26831 ) ) ;
#14477=LINE ( 'NONE', #15021, #70312 ) ;
#14483=VERTEX_POINT ( 'NONE', #32032 ) ;
#14486=EDGE_CURVE ( 'NONE', #96401, #94380, #50880, .T. ) ;
#14530=AXIS2_PLACEMENT_3D ( 'NONE', #54073, #63796, #96682 ) ;
#14593=ORIENTED_EDGE ( 'NONE', *, *, #58413, .T. ) ;
#14602=AXIS2_PLACEMENT_3D ( 'NONE', #6193, #72531, #80086 ) ;
#14604=CIRCLE ( 'NONE', #18038, 4.000000000000001776 ) ;
#14616=ORIENTED_EDGE ( 'NONE', *, *, #98751, .F. ) ;
#14629=EDGE_CURVE ( 'NONE', #45991, #64739, #106082, .T. ) ;
#14637=EDGE_CURVE ( 'NONE', #78219, #59152, #27553, .T. ) ;
#14653=DIRECTION ( 'NONE',  ( -1.000000000000000000, -1.224606353822377258E-16, -0.000000000000000000 ) ) ;
#14654=ORIENTED_EDGE ( 'NONE', *, *, #62858, .T. ) ;
#14726=CARTESIAN_POINT ( 'NONE',  ( 6.463344223170843783, -7.245769408789100474, -1.129975644293425230 ) ) ;
#14752=DIRECTION ( 'NONE',  ( 0.5735764363510490460, 0.8191520442889896891, 0.000000000000000000 ) ) ;
#14785=CARTESIAN_POINT ( 'NONE',  ( 0.000000000000000000, 5.629165124598848102, -3.250000000000007105 ) ) ;
#14790=( LENGTH_UNIT ( ) NAMED_UNIT ( * ) SI_UNIT ( .MILLI., .METRE. ) );
#14792=B_SPLINE_CURVE_WITH_KNOTS ( 'NONE', 3,
 ( #91352, #16931, #9332, #65473, #23450, #97830, #98872, #90276, #15320, #65997 ),
 .UNSPECIFIED., .F., .F.,
 ( 4, 2, 2, 2, 4 ),
 ( 0.000000000000000000, 0.001993803085173305196, 0.003987606170346610392, 0.005981409255519916021, 0.007975212340693220783 ),
 .UNSPECIFIED. ) ;
#14818=FACE_OUTER_BOUND ( 'NONE', #20256, .T. ) ;
#14833=VERTEX_POINT ( 'NONE', #44770 ) ;
#14853=CARTESIAN_POINT ( 'NONE',  ( 22.33349330513380693, 4.000000000000002665, 0.000000000000000000 ) ) ;
#14897=AXIS2_PLACEMENT_3D ( 'NONE', #63466, #89317, #40749 ) ;
#14902=CIRCLE ( 'NONE', #92442, 4.000000000000000888 ) ;
#14928=DIRECTION ( 'NONE',  ( 0.000000000000000000, -1.000000000000000000, 0.000000000000000000 ) ) ;
#14943=CARTESIAN_POINT ( 'NONE',  ( 35.11650669486618170, 1.474610560812782335E-15, 0.000000000000000000 ) ) ;
#14954=DIRECTION ( 'NONE',  ( -1.000000000000000000, -1.224606353822377258E-16, -0.000000000000000000 ) ) ;
#14977=EDGE_LOOP ( 'NONE', ( #52526, #36663, #9323, #96752, #105690 ) ) ;
#14978=ADVANCED_FACE ( 'NONE', ( #88673 ), #26995, .T. ) ;
#14982=CARTESIAN_POINT ( 'NONE',  ( 0.5805565836007650082, -3.752776749732574135, -6.500000000000001776 ) ) ;
#14983=CARTESIAN_POINT ( 'NONE',  ( 0.000000000000000000, 0.000000000000000000, 0.000000000000000000 ) ) ;
#14990=CONICAL_SURFACE ( 'NONE', #64964, 3.309500000000001663, 0.9599310885968770357 ) ;
#15009=CARTESIAN_POINT ( 'NONE',  ( 12.61650669486618881, 4.898587196589413815E-16, -4.000000000000000888 ) ) ;
#15021=CARTESIAN_POINT ( 'NONE',  ( 13.58349330513380515, 4.000000000000003553, 0.000000000000000000 ) ) ;
#15027=EDGE_CURVE ( 'NONE', #87378, #14445, #94182, .T. ) ;
#15029=VERTEX_POINT ( 'NONE', #21846 ) ;
#15032=CIRCLE ( 'NONE', #40912, 4.000000000000001776 ) ;
#15064=EDGE_CURVE ( 'NONE', #90250, #78219, #87245, .T. ) ;
#15083=CARTESIAN_POINT ( 'NONE',  ( 0.4042117618284674085, -3.141900367810040784, 6.500000000000000000 ) ) ;
#15161=FACE_OUTER_BOUND ( 'NONE', #78617, .T. ) ;
#15164=EDGE_CURVE ( 'NONE', #16434, #73038, #90707, .T. ) ;
#15172=DIRECTION ( 'NONE',  ( 0.000000000000000000, -1.000000000000000000, 0.000000000000000000 ) ) ;
#15174=CARTESIAN_POINT ( 'NONE',  ( 6.575925811255156184, 3.850887307289501571, 6.669932470447524686 ) ) ;
#15182=CARTESIAN_POINT ( 'NONE',  ( 14.83349330513380693, 1.593028355512270962E-15, 0.000000000000000000 ) ) ;
#15223=AXIS2_PLACEMENT_3D ( 'NONE', #101690, #36470, #61791 ) ;
#15228=ORIENTED_EDGE ( 'NONE', *, *, #22492, .T. ) ;
#15232=CARTESIAN_POINT ( 'NONE',  ( 6.458251213448418682, 3.357560920637083779, 6.499999999999997335 ) ) ;
#15237=DIRECTION ( 'NONE',  ( -1.000000000000000000, -0.000000000000000000, -0.000000000000000000 ) ) ;
#15250=DIRECTION ( 'NONE',  ( 0.000000000000000000, -1.000000000000000000, 0.000000000000000000 ) ) ;
#15277=DIRECTION ( 'NONE',  ( -1.000000000000000000, -1.224606353822377258E-16, -0.000000000000000000 ) ) ;
#15287=PRODUCT_CONTEXT ( 'NONE', #49301, 'mechanical' ) ;
#15320=CARTESIAN_POINT ( 'NONE',  ( 6.562934840145643101, 7.579717272840337472, -0.5631738335430729325 ) ) ;
#15355=DIRECTION ( 'NONE',  ( -1.000000000000000000, -0.000000000000000000, -0.000000000000000000 ) ) ;
#15358=DIRECTION ( 'NONE',  ( -0.5735764363510497121, 0.8191520442889892450, 1.003171929053521665E-16 ) ) ;
#15371=ORIENTED_EDGE ( 'NONE', *, *, #56373, .T. ) ;
#15388=AXIS2_PLACEMENT_3D ( 'NONE', #105245, #71276, #104170 ) ;
#15389=CIRCLE ( 'NONE', #5078, 3.309500000000001663 ) ;
#15392=ORIENTED_EDGE ( 'NONE', *, *, #45945, .T. ) ;
#15435=CARTESIAN_POINT ( 'NONE',  ( 21.36650669486618881, 0.000000000000000000, 4.000000000000000888 ) ) ;
#15442=CYLINDRICAL_SURFACE ( 'NONE', #12279, 4.000000000000000888 ) ;
#15465=CARTESIAN_POINT ( 'NONE',  ( 24.83349330513380693, 1.593028355512270962E-15, 0.000000000000000000 ) ) ;
#15466=AXIS2_PLACEMENT_3D ( 'NONE', #81714, #25678, #58542 ) ;
#15468=DIRECTION ( 'NONE',  ( 1.000000000000000000, 1.224606353822377258E-16, 0.000000000000000000 ) ) ;
#15473=PRODUCT_DEFINITION_CONTEXT ( 'detailed design', #100980, 'design' ) ;
#15480=EDGE_LOOP ( 'NONE', ( #34083, #13388, #22135, #30857, #27596 ) ) ;
#15517=ADVANCED_FACE ( 'NONE', ( #101543 ), #67591, .T. ) ;
#15518=CARTESIAN_POINT ( 'NONE',  ( 18.09999999999999787, -3.309499999999999886, 4.475777889183790779E-16 ) ) ;
#15538=CARTESIAN_POINT ( 'NONE',  ( 8.099999999999999645, -3.752776749732565253, 6.499999999999999112 ) ) ;
#15561=AXIS2_PLACEMENT_3D ( 'NONE', #62617, #4368, #63687 ) ;
#15600=ORIENTED_EDGE ( 'NONE', *, *, #87532, .T. ) ;
#15618=ORIENTED_EDGE ( 'NONE', *, *, #78564, .T. ) ;
#15635=CIRCLE ( 'NONE', #31234, 4.000000000000001776 ) ;
#15644=ORIENTED_EDGE ( 'NONE', *, *, #55924, .T. ) ;
#15648=DIRECTION ( 'NONE',  ( 0.000000000000000000, 0.000000000000000000, 1.000000000000000000 ) ) ;
#15689=DIRECTION ( 'NONE',  ( 0.000000000000000000, -1.000000000000000000, 0.000000000000000000 ) ) ;
#15705=ORIENTED_EDGE ( 'NONE', *, *, #99020, .F. ) ;
#15712=CARTESIAN_POINT ( 'NONE',  ( 26.84999999999999787, 1.533819458162526451E-15, 0.000000000000000000 ) ) ;
#15713=EDGE_CURVE ( 'NONE', #89211, #59582, #52899, .T. ) ;
#15721=AXIS2_PLACEMENT_3D ( 'NONE', #54304, #12274, #60853 ) ;
#15772=DIRECTION ( 'NONE',  ( 1.000000000000000000, 1.224606353822377258E-16, 0.000000000000000000 ) ) ;
#15775=EDGE_CURVE ( 'NONE', #86058, #36198, #44283, .T. ) ;
#15793=DIRECTION ( 'NONE',  ( 0.000000000000000000, -1.000000000000000000, 0.000000000000000000 ) ) ;
#15801=EDGE_CURVE ( 'NONE', #51255, #47192, #42570, .T. ) ;
#15816=DIRECTION ( 'NONE',  ( -1.000000000000000000, -1.224606353822377258E-16, -0.000000000000000000 ) ) ;
#15869=AXIS2_PLACEMENT_3D ( 'NONE', #77764, #3877, #29772 ) ;
#15874=EDGE_CURVE ( 'NONE', #94695, #826, #20014, .T. ) ;
#15889=DIRECTION ( 'NONE',  ( 0.000000000000000000, -1.000000000000000000, 0.000000000000000000 ) ) ;
#15948=CARTESIAN_POINT ( 'NONE',  ( 0.5805565836007605673, 3.752776749732565253, 6.499999999999997335 ) ) ;
#15992=CARTESIAN_POINT ( 'NONE',  ( 21.84999999999999787, -3.309499999999999886, 4.475777889183790779E-16 ) ) ;
#15993=ORIENTED_EDGE ( 'NONE', *, *, #68214, .F. ) ;
#16018=CARTESIAN_POINT ( 'NONE',  ( 6.463481858019713755, 4.600809706232195317, 5.711197301637621848 ) ) ;
#16040=DIRECTION ( 'NONE',  ( -1.000000000000000000, -1.224606353822377258E-16, -0.000000000000000000 ) ) ;
#16050=CYLINDRICAL_SURFACE ( 'NONE', #56636, 4.000000000000000888 ) ;
#16052=ORIENTED_EDGE ( 'NONE', *, *, #44622, .F. ) ;
#16061=CARTESIAN_POINT ( 'NONE',  ( 32.33349330513380693, 1.593028355512270962E-15, 0.000000000000000000 ) ) ;
#16063=ORIENTED_EDGE ( 'NONE', *, *, #81063, .T. ) ;
#16080=DIRECTION ( 'NONE',  ( -1.000000000000000000, -1.224606353822377258E-16, -0.000000000000000000 ) ) ;
#16120=CIRCLE ( 'NONE', #102209, 4.000000000000001776 ) ;
#16193=CONICAL_SURFACE ( 'NONE', #90263, 4.000000000000001776, 0.9599310885968774798 ) ;
#16204=CYLINDRICAL_SURFACE ( 'NONE', #18763, 4.000000000000000888 ) ;
#16221=VERTEX_POINT ( 'NONE', #1712 ) ;
#16224=VECTOR ( 'NONE', #48274, 1000.000000000000000 ) ;
#16245=CARTESIAN_POINT ( 'NONE',  ( 0.000000000000000000, 0.000000000000000000, 4.000000000000000888 ) ) ;
#16250=EDGE_CURVE ( 'NONE', #16689, #26284, #67538, .T. ) ;
#16258=ORIENTED_EDGE ( 'NONE', *, *, #50420, .T. ) ;
#16283=DIRECTION ( 'NONE',  ( 0.000000000000000000, -1.000000000000000000, 0.000000000000000000 ) ) ;
#16293=LINE ( 'NONE', #8201, #4537 ) ;
#16347=EDGE_CURVE ( 'NONE', #78006, #55436, #30024, .T. ) ;
#16370=ADVANCED_FACE ( 'NONE', ( #53977 ), #102294, .T. ) ;
#16372=DIRECTION ( 'NONE',  ( 0.000000000000000000, -1.000000000000000000, 0.000000000000000000 ) ) ;
#16375=CARTESIAN_POINT ( 'NONE',  ( 0.000000000000000000, 0.000000000000000000, 0.000000000000000000 ) ) ;
#16376=ORIENTED_EDGE ( 'NONE', *, *, #38291, .F. ) ;
#16391=CONICAL_SURFACE ( 'NONE', #76674, 3.309500000000001663, 0.9599310885968770357 ) ;
#16399=FACE_OUTER_BOUND ( 'NONE', #70062, .T. ) ;
#16405=DIRECTION ( 'NONE',  ( -1.000000000000000000, -0.000000000000000000, -0.000000000000000000 ) ) ;
#16419=CARTESIAN_POINT ( 'NONE',  ( 31.36650669486618881, 1.474610560812782335E-15, 0.000000000000000000 ) ) ;
#16420=CARTESIAN_POINT ( 'NONE',  ( 35.59999999999999432, -3.309499999999999886, 4.475777889183790779E-16 ) ) ;
#16434=VERTEX_POINT ( 'NONE', #8090 ) ;
#16458=VERTEX_POINT ( 'NONE', #23244 ) ;
#16466=CARTESIAN_POINT ( 'NONE',  ( 34.35000000000000142, -3.309499999999999886, 0.000000000000000000 ) ) ;
#16469=CIRCLE ( 'NONE', #37146, 4.000000000000001776 ) ;
#16492=DIRECTION ( 'NONE',  ( 0.000000000000000000, -1.000000000000000000, 0.000000000000000000 ) ) ;
#16503=VERTEX_POINT ( 'NONE', #39423 ) ;
#16508=FACE_OUTER_BOUND ( 'NONE', #2586, .T. ) ;
#16542=ADVANCED_FACE ( 'NONE', ( #41523 ), #82517, .T. ) ;
#16544=DIRECTION ( 'NONE',  ( -1.000000000000000000, -1.224606353822377258E-16, -0.000000000000000000 ) ) ;
#16558=VERTEX_POINT ( 'NONE', #48541 ) ;
#16563=AXIS2_PLACEMENT_3D ( 'NONE', #55727, #98336, #57327 ) ;
#16595=DIRECTION ( 'NONE',  ( -1.000000000000000000, -1.224606353822377258E-16, -0.000000000000000000 ) ) ;
#16598=EDGE_CURVE ( 'NONE', #31318, #7161, #36959, .T. ) ;
#16614=FACE_OUTER_BOUND ( 'NONE', #50930, .T. ) ;
#16616=CARTESIAN_POINT ( 'NONE',  ( 30.11650669486618881, 1.474610560812782335E-15, 0.000000000000000000 ) ) ;
#16628=CARTESIAN_POINT ( 'NONE',  ( 6.289692432696854851, -5.239086202715443896, -4.583616368338468305 ) ) ;
#16636=ORIENTED_EDGE ( 'NONE', *, *, #68160, .F. ) ;
#16647=CARTESIAN_POINT ( 'NONE',  ( 18.86650669486618881, 0.000000000000000000, 4.000000000000000888 ) ) ;
#16689=VERTEX_POINT ( 'NONE', #50648 ) ;
#16693=CIRCLE ( 'NONE', #85618, 4.000000000000000888 ) ;
#16703=AXIS2_PLACEMENT_3D ( 'NONE', #50772, #18458, #83684 ) ;
#16746=DIRECTION ( 'NONE',  ( -1.000000000000000000, -1.224606353822377258E-16, -0.000000000000000000 ) ) ;
#16766=CIRCLE ( 'NONE', #11603, 3.309500000000001663 ) ;
#16781=DIRECTION ( 'NONE',  ( -1.000000000000000000, -1.224606353822377258E-16, -0.000000000000000000 ) ) ;
#16790=DIRECTION ( 'NONE',  ( 0.000000000000000000, 0.000000000000000000, 1.000000000000000000 ) ) ;
#16866=AXIS2_PLACEMENT_3D ( 'NONE', #95443, #46366, #98614 ) ;
#16901=EDGE_CURVE ( 'NONE', #6505, #1485, #81701, .T. ) ;
#16902=ORIENTED_EDGE ( 'NONE', *, *, #18140, .T. ) ;
#16931=CARTESIAN_POINT ( 'NONE',  ( 6.562974947121711367, 4.277474787035885129, -6.282829635893498299 ) ) ;
#16942=ORIENTED_EDGE ( 'NONE', *, *, #92199, .T. ) ;
#16961=ORIENTED_EDGE ( 'NONE', *, *, #83587, .F. ) ;
#16966=CARTESIAN_POINT ( 'NONE',  ( 10.59999999999999609, 1.533819458162526451E-15, 0.000000000000000000 ) ) ;
#16993=EDGE_LOOP ( 'NONE', ( #80122, #65507, #32173, #1434, #68175 ) ) ;
#17009=EDGE_CURVE ( 'NONE', #88573, #36200, #22605, .T. ) ;
#17029=VECTOR ( 'NONE', #6538, 1000.000000000000000 ) ;
#17049=VERTEX_POINT ( 'NONE', #47363 ) ;
#17056=DIRECTION ( 'NONE',  ( 0.000000000000000000, 0.000000000000000000, 1.000000000000000000 ) ) ;
#17065=TOROIDAL_SURFACE ( 'NONE', #60136, 8.400000000000000355, 0.5999999999999978684 ) ;
#17069=CARTESIAN_POINT ( 'NONE',  ( 6.683837171061803417, -3.955946848495962787, 6.851900933636989599 ) ) ;
#17175=ORIENTED_EDGE ( 'NONE', *, *, #68885, .T. ) ;
#17182=ORIENTED_EDGE ( 'NONE', *, *, #72214, .T. ) ;
#17183=VECTOR ( 'NONE', #92000, 1000.000000000000000 ) ;
#17187=CARTESIAN_POINT ( 'NONE',  ( 0.01372220897661740636, -5.309964801958117597, 3.802871176606131609 ) ) ;
#17216=EDGE_CURVE ( 'NONE', #66061, #10937, #50534, .T. ) ;
#17260=ORIENTED_EDGE ( 'NONE', *, *, #71006, .T. ) ;
#17312=VECTOR ( 'NONE', #101394, 1000.000000000000000 ) ;
#17314=LINE ( 'NONE', #74455, #79466 ) ;
#17329=DIRECTION ( 'NONE',  ( 1.000000000000000000, 1.224606353822377258E-16, 0.000000000000000000 ) ) ;
#17373=DIRECTION ( 'NONE',  ( -1.000000000000000000, -0.000000000000000000, -0.000000000000000000 ) ) ;
#17384=CARTESIAN_POINT ( 'NONE',  ( 11.08349330513380515, 1.593028355512270962E-15, 0.000000000000000000 ) ) ;
#17390=DIRECTION ( 'NONE',  ( 0.000000000000000000, 0.000000000000000000, -1.000000000000000000 ) ) ;
#17393=VERTEX_POINT ( 'NONE', #11676 ) ;
#17399=AXIS2_PLACEMENT_3D ( 'NONE', #55255, #54189, #38071 ) ;
#17425=EDGE_CURVE ( 'NONE', #46183, #876, #53744, .T. ) ;
#17430=AXIS2_PLACEMENT_3D ( 'NONE', #70367, #103262, #29411 ) ;
#17465=AXIS2_PLACEMENT_3D ( 'NONE', #73846, #57120, #24794 ) ;
#17476=CARTESIAN_POINT ( 'NONE',  ( 18.58349330513380693, 1.593028355512270962E-15, 0.000000000000000000 ) ) ;
#17483=FACE_OUTER_BOUND ( 'NONE', #102714, .T. ) ;
#17488=CARTESIAN_POINT ( 'NONE',  ( 6.575918192882433289, 3.850883087735903043, -6.669925161966314242 ) ) ;
#17489=FACE_OUTER_BOUND ( 'NONE', #93097, .T. ) ;
#17503=ORIENTED_EDGE ( 'NONE', *, *, #68160, .T. ) ;
#17519=ORIENTED_EDGE ( 'NONE', *, *, #9553, .T. ) ;
#17523=DIRECTION ( 'NONE',  ( 0.5735764363510491570, -0.8191520442889895781, 1.003171929053522035E-16 ) ) ;
#17554=CARTESIAN_POINT ( 'NONE',  ( 12.33349330513380693, 4.000000000000003553, 0.000000000000000000 ) ) ;
#17557=DIRECTION ( 'NONE',  ( 0.000000000000000000, -1.000000000000000000, 0.000000000000000000 ) ) ;
#17560=DIRECTION ( 'NONE',  ( 0.000000000000000000, -1.000000000000000000, 0.000000000000000000 ) ) ;
#17566=EDGE_LOOP ( 'NONE', ( #21990, #10550, #18968, #36637, #31902 ) ) ;
#17589=EDGE_LOOP ( 'NONE', ( #94029, #69736 ) ) ;
#17605=CARTESIAN_POINT ( 'NONE',  ( 6.289812543865804351, -5.581224740283311725, 3.991031161979334385 ) ) ;
#17612=EDGE_CURVE ( 'NONE', #16558, #45991, #34815, .T. ) ;
#17628=ORIENTED_EDGE ( 'NONE', *, *, #13178, .F. ) ;
#17693=EDGE_CURVE ( 'NONE', #47749, #96624, #82795, .T. ) ;
#17701=CARTESIAN_POINT ( 'NONE',  ( 26.36650669486618881, 1.474610560812782335E-15, 0.000000000000000000 ) ) ;
#17703=EDGE_LOOP ( 'NONE', ( #70524, #54562, #90879, #19165, #94118, #99473 ) ) ;
#17704=CARTESIAN_POINT ( 'NONE',  ( 6.585468679846623097, -7.640532685286896886, 0.2337908078075559004 ) ) ;
#17708=DIRECTION ( 'NONE',  ( 0.000000000000000000, 1.000000000000000000, 0.000000000000000000 ) ) ;
#17710=EDGE_LOOP ( 'NONE', ( #60220, #1962, #545, #45402, #90755, #50711 ) ) ;
#17716=VERTEX_POINT ( 'NONE', #43407 ) ;
#17752=LINE ( 'NONE', #83525, #45158 ) ;
#17763=CARTESIAN_POINT ( 'NONE',  ( 27.33349330513380693, 1.593028355512270962E-15, 0.000000000000000000 ) ) ;
#17789=ORIENTED_EDGE ( 'NONE', *, *, #35904, .T. ) ;
#17844=ORIENTED_EDGE ( 'NONE', *, *, #25730, .T. ) ;
#17894=CIRCLE ( 'NONE', #90245, 4.000000000000001776 ) ;
#17942=LINE ( 'NONE', #35200, #62800 ) ;
#17978=DIRECTION ( 'NONE',  ( -1.000000000000000000, -0.000000000000000000, -0.000000000000000000 ) ) ;
#17981=CIRCLE ( 'NONE', #92040, 3.309500000000001663 ) ;
#18006=EDGE_LOOP ( 'NONE', ( #81141, #86298, #40585, #35604, #58156, #40823 ) ) ;
#18008=CARTESIAN_POINT ( 'NONE',  ( 0.000000000000000000, 0.000000000000000000, 0.000000000000000000 ) ) ;
#18019=DIRECTION ( 'NONE',  ( -0.5735764363510494901, -0.8191520442889894671, 0.000000000000000000 ) ) ;
#18038=AXIS2_PLACEMENT_3D ( 'NONE', #40679, #73565, #88716 ) ;
#18060=DIRECTION ( 'NONE',  ( -0.5735764363510497121, 0.8191520442889892450, 1.003171929053521665E-16 ) ) ;
#18081=DIRECTION ( 'NONE',  ( -1.000000000000000000, -1.224606353822377258E-16, -0.000000000000000000 ) ) ;
#18096=ADVANCED_FACE ( 'NONE', ( #32818 ), #104032, .T. ) ;
#18108=DIRECTION ( 'NONE',  ( -1.000000000000000000, -0.000000000000000000, -0.000000000000000000 ) ) ;
#18140=EDGE_CURVE ( 'NONE', #100701, #34409, #71318, .T. ) ;
#18141=CARTESIAN_POINT ( 'NONE',  ( 6.289572920342627604, -6.243622107253693265, 2.843693100100563420 ) ) ;
#18182=ORIENTED_EDGE ( 'NONE', *, *, #87129, .T. ) ;
#18194=DIRECTION ( 'NONE',  ( 0.000000000000000000, -1.000000000000000000, 0.000000000000000000 ) ) ;
#18233=LINE ( 'NONE', #9040, #91184 ) ;
#18260=AXIS2_PLACEMENT_3D ( 'NONE', #75408, #52192, #2044 ) ;
#18281=LINE ( 'NONE', #33396, #6672 ) ;
#18282=CARTESIAN_POINT ( 'NONE',  ( 37.33349330513379982, 4.898587196589411843E-16, -4.000000000000001776 ) ) ;
#18294=CARTESIAN_POINT ( 'NONE',  ( 33.09999999999999432, -3.309499999999999886, 0.000000000000000000 ) ) ;
#18314=ADVANCED_FACE ( 'NONE', ( #10629 ), #16193, .T. ) ;
#18326=VECTOR ( 'NONE', #20371, 1000.000000000000341 ) ;
#18334=EDGE_LOOP ( 'NONE', ( #99148, #62887, #14184, #67297, #99997, #23622 ) ) ;
#18349=CARTESIAN_POINT ( 'NONE',  ( 0.000000000000000000, 0.000000000000000000, 0.000000000000000000 ) ) ;
#18350=ORIENTED_EDGE ( 'NONE', *, *, #45887, .T. ) ;
#18357=EDGE_CURVE ( 'NONE', #81895, #66028, #17981, .T. ) ;
#18367=CARTESIAN_POINT ( 'NONE',  ( 31.84999999999999787, 1.533819458162526451E-15, 0.000000000000000000 ) ) ;
#18396=ORIENTED_EDGE ( 'NONE', *, *, #104173, .T. ) ;
#18403=DIRECTION ( 'NONE',  ( 0.000000000000000000, 0.000000000000000000, -1.000000000000000000 ) ) ;
#18406=DIRECTION ( 'NONE',  ( -1.000000000000000000, -1.224606353822377258E-16, -0.000000000000000000 ) ) ;
#18458=DIRECTION ( 'NONE',  ( -1.000000000000000000, -1.224606353822377258E-16, -0.000000000000000000 ) ) ;
#18471=DIRECTION ( 'NONE',  ( -1.000000000000000000, -1.224606353822377258E-16, -0.000000000000000000 ) ) ;
#18487=EDGE_CURVE ( 'NONE', #51009, #2998, #67449, .T. ) ;
#18490=FACE_OUTER_BOUND ( 'NONE', #60071, .T. ) ;
#18515=DIRECTION ( 'NONE',  ( -1.000000000000000000, -1.224606353822377258E-16, -0.000000000000000000 ) ) ;
#18535=CONICAL_SURFACE ( 'NONE', #11572, 8.605212085995399107, 1.221730476396037490 ) ;
#18553=CARTESIAN_POINT ( 'NONE',  ( 0.000000000000000000, 0.000000000000000000, 0.000000000000000000 ) ) ;
#18584=ORIENTED_EDGE ( 'NONE', *, *, #18625, .F. ) ;
#18591=ORIENTED_EDGE ( 'NONE', *, *, #57590, .F. ) ;
#18605=CYLINDRICAL_SURFACE ( 'NONE', #54589, 4.000000000000000888 ) ;
#18613=EDGE_LOOP ( 'NONE', ( #13360, #88594, #54488, #31370, #54443 ) ) ;
#18621=AXIS2_PLACEMENT_3D ( 'NONE', #52035, #84419, #91969 ) ;
#18625=EDGE_CURVE ( 'NONE', #71083, #58745, #104115, .T. ) ;
#18626=CARTESIAN_POINT ( 'NONE',  ( 27.33349330513380693, 1.593028355512270962E-15, 0.000000000000000000 ) ) ;
#18630=AXIS2_PLACEMENT_3D ( 'NONE', #33521, #18406, #24901 ) ;
#18641=EDGE_CURVE ( 'NONE', #88306, #29177, #104971, .T. ) ;
#18678=CONICAL_SURFACE ( 'NONE', #10015, 4.000000000000001776, 0.9599310885968774798 ) ;
#18689=ORIENTED_EDGE ( 'NONE', *, *, #81171, .F. ) ;
#18709=VERTEX_POINT ( 'NONE', #63465 ) ;
#18734=EDGE_LOOP ( 'NONE', ( #37082, #81278, #35987, #67741, #9028 ) ) ;
#18763=AXIS2_PLACEMENT_3D ( 'NONE', #56108, #98702, #24857 ) ;
#18816=CIRCLE ( 'NONE', #79071, 3.309500000000001663 ) ;
#18844=CIRCLE ( 'NONE', #46367, 3.309499999999999886 ) ;
#18904=EDGE_CURVE ( 'NONE', #99736, #8297, #16120, .T. ) ;
#18954=DIRECTION ( 'NONE',  ( 0.000000000000000000, -1.000000000000000000, 0.000000000000000000 ) ) ;
#18960=CYLINDRICAL_SURFACE ( 'NONE', #6632, 4.000000000000000888 ) ;
#18968=ORIENTED_EDGE ( 'NONE', *, *, #4409, .T. ) ;
#18992=CARTESIAN_POINT ( 'NONE',  ( 5.947762761376478302, 6.880090707843046438, 1.083333333333333481 ) ) ;
#19038=CARTESIAN_POINT ( 'NONE',  ( 33.86650669486618881, -3.999999999999998224, 0.000000000000000000 ) ) ;
#19044=LINE ( 'NONE', #92878, #90542 ) ;
#19045=CIRCLE ( 'NONE', #72344, 3.309500000000001663 ) ;
#19060=CONICAL_SURFACE ( 'NONE', #51727, 3.309500000000001663, 0.9599310885968770357 ) ;
#19097=ORIENTED_EDGE ( 'NONE', *, *, #71252, .T. ) ;
#19101=FACE_OUTER_BOUND ( 'NONE', #17589, .T. ) ;
#19140=DIRECTION ( 'NONE',  ( -1.000000000000000000, -1.224606353822377258E-16, -0.000000000000000000 ) ) ;
#19159=CARTESIAN_POINT ( 'NONE',  ( 0.000000000000000000, 0.000000000000000000, 0.000000000000000000 ) ) ;
#19163=EDGE_CURVE ( 'NONE', #104988, #94131, #77641, .T. ) ;
#19165=ORIENTED_EDGE ( 'NONE', *, *, #6203, .F. ) ;
#19214=VERTEX_POINT ( 'NONE', #59791 ) ;
#19260=DIRECTION ( 'NONE',  ( -1.000000000000000000, -0.000000000000000000, -0.000000000000000000 ) ) ;
#19293=AXIS2_PLACEMENT_3D ( 'NONE', #49570, #73299, #81391 ) ;
#19309=CARTESIAN_POINT ( 'NONE',  ( 35.59999999999999432, -3.309499999999999886, 0.000000000000000000 ) ) ;
#19316=CARTESIAN_POINT ( 'NONE',  ( 21.84999999999999787, 3.309500000000003439, 4.052968581778167743E-16 ) ) ;
#19338=ADVANCED_FACE ( 'NONE', ( #86728 ), #29555, .T. ) ;
#19349=EDGE_CURVE ( 'NONE', #11179, #67595, #89811, .T. ) ;
#19436=LINE ( 'NONE', #92734, #62192 ) ;
#19485=ORIENTED_EDGE ( 'NONE', *, *, #9204, .F. ) ;
#19489=CIRCLE ( 'NONE', #62564, 4.000000000000000888 ) ;
#19548=ORIENTED_EDGE ( 'NONE', *, *, #72802, .F. ) ;
#19590=CARTESIAN_POINT ( 'NONE',  ( 16.08349330513380337, 1.593028355512270962E-15, 0.000000000000000000 ) ) ;
#19593=ORIENTED_EDGE ( 'NONE', *, *, #2047, .T. ) ;
#19596=DIRECTION ( 'NONE',  ( -1.000000000000000000, -1.224606353822377258E-16, -0.000000000000000000 ) ) ;
#19617=EDGE_LOOP ( 'NONE', ( #52323, #74745, #71035, #73224, #20201 ) ) ;
#19638=DIRECTION ( 'NONE',  ( -1.000000000000000000, -1.224606353822377258E-16, -0.000000000000000000 ) ) ;
#19669=VERTEX_POINT ( 'NONE', #50475 ) ;
#19721=DIRECTION ( 'NONE',  ( -1.000000000000000000, -1.224606353822377258E-16, -0.000000000000000000 ) ) ;
#19733=DIRECTION ( 'NONE',  ( 0.000000000000000000, -1.000000000000000000, 0.000000000000000000 ) ) ;
#19761=CONICAL_SURFACE ( 'NONE', #79984, 3.309500000000001663, 0.9599310885968770357 ) ;
#19767=AXIS2_PLACEMENT_3D ( 'NONE', #7068, #63743, #96629 ) ;
#19769=CARTESIAN_POINT ( 'NONE',  ( 6.562874270078300043, -3.301808241302750080, -6.845811579416826831 ) ) ;
#19782=EDGE_LOOP ( 'NONE', ( #19869, #23699, #58552, #95624, #1932, #56352 ) ) ;
#19829=ADVANCED_FACE ( 'NONE', ( #80073 ), #59003, .T. ) ;
#19844=CIRCLE ( 'NONE', #2537, 4.000000000000000888 ) ;
#19850=DIRECTION ( 'NONE',  ( -1.000000000000000000, -0.000000000000000000, -0.000000000000000000 ) ) ;
#19856=DIRECTION ( 'NONE',  ( 1.000000000000000000, 1.224606353822377258E-16, 0.000000000000000000 ) ) ;
#19861=ADVANCED_FACE ( 'NONE', ( #17489 ), #279, .T. ) ;
#19866=LINE ( 'NONE', #28474, #68377 ) ;
#19869=ORIENTED_EDGE ( 'NONE', *, *, #78532, .F. ) ;
#19874=EDGE_CURVE ( 'NONE', #91446, #53134, #707, .T. ) ;
#19919=ORIENTED_EDGE ( 'NONE', *, *, #47799, .T. ) ;
#19930=ORIENTED_EDGE ( 'NONE', *, *, #24353, .T. ) ;
#19939=ORIENTED_EDGE ( 'NONE', *, *, #74472, .F. ) ;
#19941=EDGE_CURVE ( 'NONE', #97355, #14483, #26147, .T. ) ;
#19989=CIRCLE ( 'NONE', #47489, 3.309500000000001663 ) ;
#20002=ADVANCED_FACE ( 'NONE', ( #95098 ), #84717, .T. ) ;
#20014=LINE ( 'NONE', #52858, #27144 ) ;
#20026=DIRECTION ( 'NONE',  ( -1.000000000000000000, -1.224606353822377258E-16, -0.000000000000000000 ) ) ;
#20088=CARTESIAN_POINT ( 'NONE',  ( 17.33349330513380693, 4.000000000000003553, 0.000000000000000000 ) ) ;
#20094=PRODUCT_DEFINITION_SHAPE ( 'NONE', 'NONE',  #76584 ) ;
#20113=DIRECTION ( 'NONE',  ( 0.000000000000000000, -1.000000000000000000, 0.000000000000000000 ) ) ;
#20147=ORIENTED_EDGE ( 'NONE', *, *, #88714, .T. ) ;
#20179=LINE ( 'NONE', #102099, #34420 ) ;
#20182=CARTESIAN_POINT ( 'NONE',  ( 28.58349330513380337, -4.000000000000000888, 4.898587196589416773E-16 ) ) ;
#20201=ORIENTED_EDGE ( 'NONE', *, *, #15164, .T. ) ;
#20211=B_SPLINE_CURVE_WITH_KNOTS ( 'NONE', 3,
 ( #50715, #83628, #42648, #2173, #34600, #2716, #92246, #51254 ),
 .UNSPECIFIED., .F., .F.,
 ( 4, 2, 2, 4 ),
 ( 0.003797433802554431997, 0.004743183970586231819, 0.005688934138618031641, 0.007580434474681628683 ),
 .UNSPECIFIED. ) ;
#20216=DIRECTION ( 'NONE',  ( -1.000000000000000000, -0.000000000000000000, -0.000000000000000000 ) ) ;
#20249=DIRECTION ( 'NONE',  ( -1.000000000000000000, -0.000000000000000000, -0.000000000000000000 ) ) ;
#20256=EDGE_LOOP ( 'NONE', ( #46826, #71166, #21765, #84031, #47579 ) ) ;
#20286=DIRECTION ( 'NONE',  ( -0.5735764363510497121, 0.8191520442889892450, 1.003171929053521665E-16 ) ) ;
#20296=LINE ( 'NONE', #44527, #37611 ) ;
#20313=EDGE_CURVE ( 'NONE', #94433, #91201, #9021, .T. ) ;
#20342=FACE_OUTER_BOUND ( 'NONE', #35292, .T. ) ;
#20349=DIRECTION ( 'NONE',  ( -1.000000000000000000, -1.224606353822377258E-16, -0.000000000000000000 ) ) ;
#20351=EDGE_CURVE ( 'NONE', #36441, #99443, #368, .T. ) ;
#20371=DIRECTION ( 'NONE',  ( 0.5735764363510490460, 0.8191520442889896891, 0.000000000000000000 ) ) ;
#20393=DIRECTION ( 'NONE',  ( 0.000000000000000000, 0.000000000000000000, 1.000000000000000000 ) ) ;
#20420=AXIS2_PLACEMENT_3D ( 'NONE', #256, #58554, #25137 ) ;
#20451=AXIS2_PLACEMENT_3D ( 'NONE', #102999, #62032, #94924 ) ;
#20483=EDGE_CURVE ( 'NONE', #93666, #32543, #36543, .T. ) ;
#20485=ORIENTED_EDGE ( 'NONE', *, *, #93507, .F. ) ;
#20506=CARTESIAN_POINT ( 'NONE',  ( 31.08349330513380693, -4.000000000000000888, 4.898587196589416773E-16 ) ) ;
#20521=CARTESIAN_POINT ( 'NONE',  ( 6.162888688655347558, -3.752776749732574135, -6.500000000000001776 ) ) ;
#20538=ORIENTED_EDGE ( 'NONE', *, *, #70856, .F. ) ;
#20541=ORIENTED_EDGE ( 'NONE', *, *, #75555, .F. ) ;
#20548=VERTEX_POINT ( 'NONE', #56332 ) ;
#20580=DIRECTION ( 'NONE',  ( 0.000000000000000000, -1.000000000000000000, 0.000000000000000000 ) ) ;
#20590=VECTOR ( 'NONE', #43886, 1000.000000000000341 ) ;
#20647=CARTESIAN_POINT ( 'NONE',  ( 0.5805565836007658964, 7.505553499465141165, -3.996997974842411264E-16 ) ) ;
#20658=CARTESIAN_POINT ( 'NONE',  ( 9.833493305133805151, 1.593028355512270962E-15, 0.000000000000000000 ) ) ;
#20790=EDGE_CURVE ( 'NONE', #81895, #4237, #76252, .T. ) ;
#20800=ORIENTED_EDGE ( 'NONE', *, *, #28665, .T. ) ;
#20805=VECTOR ( 'NONE', #91605, 1000.000000000000341 ) ;
#20827=CIRCLE ( 'NONE', #34667, 4.000000000000000888 ) ;
#20830=CARTESIAN_POINT ( 'NONE',  ( 34.83349330513380693, 1.593028355512270962E-15, 0.000000000000000000 ) ) ;
#20837=CARTESIAN_POINT ( 'NONE',  ( 24.34999999999999787, 1.533819458162526451E-15, 0.000000000000000000 ) ) ;
#20882=ORIENTED_EDGE ( 'NONE', *, *, #82735, .T. ) ;
#20901=ORIENTED_EDGE ( 'NONE', *, *, #54618, .T. ) ;
#20906=ADVANCED_FACE ( 'NONE', ( #31978 ), #5553, .T. ) ;
#20960=ORIENTED_EDGE ( 'NONE', *, *, #15164, .F. ) ;
#20987=ORIENTED_EDGE ( 'NONE', *, *, #44870, .T. ) ;
#20995=VERTEX_POINT ( 'NONE', #49727 ) ;
#21018=ORIENTED_EDGE ( 'NONE', *, *, #59625, .T. ) ;
#21049=DIRECTION ( 'NONE',  ( 0.000000000000000000, -1.000000000000000000, 0.000000000000000000 ) ) ;
#21060=VERTEX_POINT ( 'NONE', #76655 ) ;
#21062=ORIENTED_EDGE ( 'NONE', *, *, #93507, .T. ) ;
#21065=CARTESIAN_POINT ( 'NONE',  ( 14.83349330513380693, 4.898587196589411843E-16, -4.000000000000001776 ) ) ;
#21069=CARTESIAN_POINT ( 'NONE',  ( 13.86650669486618881, 4.898587196589413815E-16, -4.000000000000000888 ) ) ;
#21083=EDGE_CURVE ( 'NONE', #36198, #86058, #14244, .T. ) ;
#21089=DIRECTION ( 'NONE',  ( 1.000000000000000000, 1.224606353822377258E-16, 0.000000000000000000 ) ) ;
#21118=CIRCLE ( 'NONE', #12431, 4.000000000000001776 ) ;
#21119=ORIENTED_EDGE ( 'NONE', *, *, #99020, .T. ) ;
#21145=DIRECTION ( 'NONE',  ( -1.000000000000000000, -1.224606353822377258E-16, -0.000000000000000000 ) ) ;
#21149=EDGE_CURVE ( 'NONE', #84857, #77950, #59981, .T. ) ;
#21155=ADVANCED_FACE ( 'NONE', ( #51309 ), #59083, .T. ) ;
#21168=ORIENTED_EDGE ( 'NONE', *, *, #75417, .F. ) ;
#21226=AXIS2_PLACEMENT_3D ( 'NONE', #52685, #19850, #20393 ) ;
#21231=DIRECTION ( 'NONE',  ( 0.000000000000000000, 0.000000000000000000, 1.000000000000000000 ) ) ;
#21234=DIRECTION ( 'NONE',  ( -1.000000000000000000, -1.224606353822377258E-16, -0.000000000000000000 ) ) ;
#21284=( NAMED_UNIT ( * ) PLANE_ANGLE_UNIT ( ) SI_UNIT ( $, .RADIAN. ) );
#21330=LINE ( 'NONE', #39088, #10348 ) ;
#21339=DIRECTION ( 'NONE',  ( -1.000000000000000000, -1.224606353822377258E-16, -0.000000000000000000 ) ) ;
#21373=ORIENTED_EDGE ( 'NONE', *, *, #70412, .T. ) ;
#21382=ORIENTED_EDGE ( 'NONE', *, *, #41169, .F. ) ;
#21393=EDGE_LOOP ( 'NONE', ( #65544, #78137, #80168, #25293, #23870, #60961 ) ) ;
#21401=CARTESIAN_POINT ( 'NONE',  ( 0.000000000000000000, 4.898587196589413815E-16, -4.000000000000000888 ) ) ;
#21428=CARTESIAN_POINT ( 'NONE',  ( 22.61650669486618526, 1.474610560812782335E-15, 0.000000000000000000 ) ) ;
#21438=CARTESIAN_POINT ( 'NONE',  ( 26.08349330513380693, 1.593028355512270962E-15, 0.000000000000000000 ) ) ;
#21463=ORIENTED_EDGE ( 'NONE', *, *, #83714, .T. ) ;
#21492=B_SPLINE_CURVE_WITH_KNOTS ( 'NONE', 3,
 ( #17069, #92006, #66672, #75281, #17605, #18141, #50997, #8425, #1377, #8952 ),
 .UNSPECIFIED., .F., .F.,
 ( 4, 2, 2, 2, 4 ),
 ( 0.000000000000000000, 0.001993803085173304762, 0.003987606170346609524, 0.005981409255519914286, 0.007975212340693219049 ),
 .UNSPECIFIED. ) ;
#21506=CARTESIAN_POINT ( 'NONE',  ( 29.34999999999999787, 3.309500000000003439, 4.052968581778167743E-16 ) ) ;
#21508=ORIENTED_EDGE ( 'NONE', *, *, #95673, .T. ) ;
#21544=CARTESIAN_POINT ( 'NONE',  ( 5.947762761376478302, -2.501851166488387346, -6.500000000000002665 ) ) ;
#21569=CIRCLE ( 'NONE', #42235, 4.000000000000001776 ) ;
#21574=EDGE_LOOP ( 'NONE', ( #40666, #88295, #83170, #95130, #95720, #4596 ) ) ;
#21575=CONICAL_SURFACE ( 'NONE', #52566, 4.000000000000001776, 0.9599310885968774798 ) ;
#21579=VECTOR ( 'NONE', #42115, 1000.000000000000000 ) ;
#21581=ORIENTED_EDGE ( 'NONE', *, *, #85346, .T. ) ;
#21613=ORIENTED_EDGE ( 'NONE', *, *, #44870, .F. ) ;
#21668=DIRECTION ( 'NONE',  ( -1.000000000000000000, -0.000000000000000000, -0.000000000000000000 ) ) ;
#21680=CARTESIAN_POINT ( 'NONE',  ( 34.35000000000000142, 1.533819458162526451E-15, 0.000000000000000000 ) ) ;
#21734=ORIENTED_EDGE ( 'NONE', *, *, #48186, .F. ) ;
#21761=DIRECTION ( 'NONE',  ( 0.000000000000000000, 0.000000000000000000, 1.000000000000000000 ) ) ;
#21765=ORIENTED_EDGE ( 'NONE', *, *, #47265, .T. ) ;
#21783=VERTEX_POINT ( 'NONE', #84909 ) ;
#21796=ORIENTED_EDGE ( 'NONE', *, *, #1013, .F. ) ;
#21801=AXIS2_PLACEMENT_3D ( 'NONE', #60266, #77487, #83437 ) ;
#21842=DIRECTION ( 'NONE',  ( -1.000000000000000000, -1.224606353822377258E-16, -0.000000000000000000 ) ) ;
#21846=CARTESIAN_POINT ( 'NONE',  ( 32.61650669486618881, 4.000000000000003553, 4.898587196589414801E-16 ) ) ;
#21857=PLANE ( 'NONE',  #106209 ) ;
#21883=CARTESIAN_POINT ( 'NONE',  ( 9.349999999999997868, 3.309500000000003439, 0.000000000000000000 ) ) ;
#21890=FACE_OUTER_BOUND ( 'NONE', #57544, .T. ) ;
#21918=CARTESIAN_POINT ( 'NONE',  ( 0.2595206531158521512, 2.531175536751804067, -6.500000000000002665 ) ) ;
#21925=LINE ( 'NONE', #30543, #16224 ) ;
#21946=AXIS2_PLACEMENT_3D ( 'NONE', #16061, #24717, #65145 ) ;
#21964=AXIS2_PLACEMENT_3D ( 'NONE', #53641, #21842, #4567 ) ;
#21990=ORIENTED_EDGE ( 'NONE', *, *, #54014, .F. ) ;
#21995=ORIENTED_EDGE ( 'NONE', *, *, #66345, .F. ) ;
#22017=VECTOR ( 'NONE', #93151, 1000.000000000000000 ) ;
#22088=VECTOR ( 'NONE', #27538, 1000.000000000000000 ) ;
#22104=ORIENTED_EDGE ( 'NONE', *, *, #100591, .F. ) ;
#22117=ADVANCED_FACE ( 'NONE', ( #80208 ), #66156, .F. ) ;
#22135=ORIENTED_EDGE ( 'NONE', *, *, #87583, .T. ) ;
#22153=AXIS2_PLACEMENT_3D ( 'NONE', #59900, #92771, #53390 ) ;
#22176=CARTESIAN_POINT ( 'NONE',  ( 0.000000000000000000, 0.000000000000000000, 0.000000000000000000 ) ) ;
#22191=AXIS2_PLACEMENT_3D ( 'NONE', #56496, #23111, #14440 ) ;
#22207=ORIENTED_EDGE ( 'NONE', *, *, #49462, .T. ) ;
#22249=EDGE_CURVE ( 'NONE', #48784, #35708, #98982, .T. ) ;
#22252=DIRECTION ( 'NONE',  ( 0.000000000000000000, -1.000000000000000000, 0.000000000000000000 ) ) ;
#22262=ORIENTED_EDGE ( 'NONE', *, *, #54425, .T. ) ;
#22295=CARTESIAN_POINT ( 'NONE',  ( 6.289692432696756264, -5.239086202715468765, 4.583616368337883884 ) ) ;
#22316=AXIS2_PLACEMENT_3D ( 'NONE', #18626, #18081, #25671 ) ;
#22368=AXIS2_PLACEMENT_3D ( 'NONE', #28919, #21339, #79008 ) ;
#22379=CARTESIAN_POINT ( 'NONE',  ( 34.83349330513380693, 1.593028355512270962E-15, 0.000000000000000000 ) ) ;
#22395=DIRECTION ( 'NONE',  ( 0.000000000000000000, 1.000000000000000000, 0.000000000000000000 ) ) ;
#22396=ADVANCED_FACE ( 'NONE', ( #14818 ), #5991, .T. ) ;
#22414=PLANE ( 'NONE',  #46389 ) ;
#22421=CARTESIAN_POINT ( 'NONE',  ( 0.5805565836007605673, 3.752776749732565253, 6.499999999999997335 ) ) ;
#22435=ADVANCED_FACE ( 'NONE', ( #48769 ), #33587, .T. ) ;
#22452=CARTESIAN_POINT ( 'NONE',  ( 13.86650669486618881, -3.999999999999998224, 0.000000000000000000 ) ) ;
#22459=EDGE_LOOP ( 'NONE', ( #24246, #21018, #1828, #88207, #66665 ) ) ;
#22492=EDGE_CURVE ( 'NONE', #28856, #87378, #97374, .T. ) ;
#22499=DIRECTION ( 'NONE',  ( -1.000000000000000000, -1.224606353822377258E-16, -0.000000000000000000 ) ) ;
#22538=ORIENTED_EDGE ( 'NONE', *, *, #91659, .F. ) ;
#22557=CARTESIAN_POINT ( 'NONE',  ( 8.099999999999999645, 7.505553499465140277, 0.000000000000000000 ) ) ;
#22573=EDGE_LOOP ( 'NONE', ( #44779, #70757, #54051, #60016 ) ) ;
#22575=LINE ( 'NONE', #105056, #47399 ) ;
#22594=VERTEX_POINT ( 'NONE', #26680 ) ;
#22605=LINE ( 'NONE', #106113, #71165 ) ;
#22621=EDGE_CURVE ( 'NONE', #21783, #61515, #78447, .T. ) ;
#22641=VERTEX_POINT ( 'NONE', #51966 ) ;
#22667=SHAPE_REPRESENTATION ( 'hex flange bolt_din_DIN 6921 - M8 x 30 x 30-S', ( #10728 ), #57385 ) ;
#22712=DIRECTION ( 'NONE',  ( 0.000000000000000000, 0.000000000000000000, 1.000000000000000000 ) ) ;
#22717=AXIS2_PLACEMENT_3D ( 'NONE', #97690, #24904, #8691 ) ;
#22741=EDGE_CURVE ( 'NONE', #90030, #37979, #16469, .T. ) ;
#22761=FACE_OUTER_BOUND ( 'NONE', #28101, .T. ) ;
#22771=CARTESIAN_POINT ( 'NONE',  ( 12.33349330513380693, 1.593028355512270962E-15, 0.000000000000000000 ) ) ;
#22784=AXIS2_PLACEMENT_3D ( 'NONE', #36248, #92834, #69640 ) ;
#22803=CARTESIAN_POINT ( 'NONE',  ( 13.86650669486618881, 1.474610560812782335E-15, 0.000000000000000000 ) ) ;
#22804=DIRECTION ( 'NONE',  ( -1.000000000000000000, -1.224606353822377258E-16, -0.000000000000000000 ) ) ;
#22825=CARTESIAN_POINT ( 'NONE',  ( 5.819846122303831137, -4.937269551422891034, 4.448398286272754909 ) ) ;
#22859=CARTESIAN_POINT ( 'NONE',  ( 37.33349330513379982, 4.000000000000003553, 0.000000000000000000 ) ) ;
#22860=EDGE_LOOP ( 'NONE', ( #17628, #91222, #18350, #62927, #26244 ) ) ;
#22867=ADVANCED_FACE ( 'NONE', ( #70825 ), #33661, .T. ) ;
#22879=CARTESIAN_POINT ( 'NONE',  ( 31.08349330513380693, -3.851859888774471706E-31, 4.000000000000001776 ) ) ;
#22946=VECTOR ( 'NONE', #12454, 1000.000000000000000 ) ;
#22964=CARTESIAN_POINT ( 'NONE',  ( 6.289692432696780244, -0.6618655008720331079, 6.828989928337167115 ) ) ;
#22979=ORIENTED_EDGE ( 'NONE', *, *, #1883, .F. ) ;
#22983=VECTOR ( 'NONE', #95104, 1000.000000000000000 ) ;
#22984=LINE ( 'NONE', #97361, #80406 ) ;
#23042=VERTEX_POINT ( 'NONE', #31971 ) ;
#23051=AXIS2_PLACEMENT_3D ( 'NONE', #33256, #66667, #66129 ) ;
#23077=FACE_OUTER_BOUND ( 'NONE', #80910, .T. ) ;
#23086=AXIS2_PLACEMENT_3D ( 'NONE', #68339, #75341, #83440 ) ;
#23111=DIRECTION ( 'NONE',  ( 1.000000000000000000, 1.224606353822377258E-16, 0.000000000000000000 ) ) ;
#23135=DIRECTION ( 'NONE',  ( -1.000000000000000000, -1.224606353822377258E-16, -0.000000000000000000 ) ) ;
#23165=EDGE_LOOP ( 'NONE', ( #12927, #94759, #77427, #3584, #77461 ) ) ;
#23169=CARTESIAN_POINT ( 'NONE',  ( 18.58349330513380693, 4.000000000000002665, 0.000000000000000000 ) ) ;
#23176=ORIENTED_EDGE ( 'NONE', *, *, #81317, .T. ) ;
#23216=VERTEX_POINT ( 'NONE', #10321 ) ;
#23234=EDGE_LOOP ( 'NONE', ( #94194, #34806, #43045, #57069, #3780, #57153 ) ) ;
#23244=CARTESIAN_POINT ( 'NONE',  ( 0.000000000000000000, 7.511572993685796142E-16, -6.500000000000000888 ) ) ;
#23262=AXIS2_PLACEMENT_3D ( 'NONE', #105838, #15772, #97739 ) ;
#23277=ORIENTED_EDGE ( 'NONE', *, *, #12450, .F. ) ;
#23305=CARTESIAN_POINT ( 'NONE',  ( 29.83349330513380693, 1.593028355512270962E-15, 0.000000000000000000 ) ) ;
#23318=ORIENTED_EDGE ( 'NONE', *, *, #73101, .F. ) ;
#23325=DIRECTION ( 'NONE',  ( -1.000000000000000000, -1.224606353822377258E-16, -0.000000000000000000 ) ) ;
#23341=ORIENTED_EDGE ( 'NONE', *, *, #50288, .T. ) ;
#23356=AXIS2_PLACEMENT_3D ( 'NONE', #42518, #3131, #26391 ) ;
#23403=CARTESIAN_POINT ( 'NONE',  ( 0.000000000000000000, 0.000000000000000000, 0.000000000000000000 ) ) ;
#23450=CARTESIAN_POINT ( 'NONE',  ( 6.289812543865803462, 5.581224740283310837, -3.991031161979335273 ) ) ;
#23453=DIRECTION ( 'NONE',  ( -1.000000000000000000, -1.224606353822377258E-16, -0.000000000000000000 ) ) ;
#23488=ADVANCED_FACE ( 'NONE', ( #85030 ), #7989, .T. ) ;
#23515=AXIS2_PLACEMENT_3D ( 'NONE', #17763, #75981, #35565 ) ;
#23520=DIRECTION ( 'NONE',  ( 0.000000000000000000, -1.000000000000000000, 0.000000000000000000 ) ) ;
#23558=ADVANCED_FACE ( 'NONE', ( #91536 ), #69980, .T. ) ;
#23566=ORIENTED_EDGE ( 'NONE', *, *, #80750, .F. ) ;
#23595=CARTESIAN_POINT ( 'NONE',  ( 6.222802839579465228, -4.089658325571345898, -6.500000000000002665 ) ) ;
#23622=ORIENTED_EDGE ( 'NONE', *, *, #92848, .F. ) ;
#23637=CARTESIAN_POINT ( 'NONE',  ( 0.4033376246892511618, -4.059728990630809164, -5.968343123267135120 ) ) ;
#23639=LINE ( 'NONE', #19309, #7824 ) ;
#23652=CIRCLE ( 'NONE', #90841, 4.000000000000001776 ) ;
#23668=CARTESIAN_POINT ( 'NONE',  ( 11.36650669486618881, 0.000000000000000000, 4.000000000000000888 ) ) ;
#23678=AXIS2_PLACEMENT_3D ( 'NONE', #75183, #19140, #1282 ) ;
#23688=FACE_OUTER_BOUND ( 'NONE', #91978, .T. ) ;
#23699=ORIENTED_EDGE ( 'NONE', *, *, #26014, .T. ) ;
#23722=DIRECTION ( 'NONE',  ( 0.5735764363510490460, 0.8191520442889896891, 0.000000000000000000 ) ) ;
#23734=AXIS2_PLACEMENT_3D ( 'NONE', #13446, #5884, #13974 ) ;
#23830=CARTESIAN_POINT ( 'NONE',  ( 28.09999999999999787, 1.533819458162526451E-15, 0.000000000000000000 ) ) ;
#23839=DIRECTION ( 'NONE',  ( -1.000000000000000000, -1.224606353822377258E-16, -0.000000000000000000 ) ) ;
#23856=ADVANCED_FACE ( 'NONE', ( #59037 ), #34253, .T. ) ;
#23870=ORIENTED_EDGE ( 'NONE', *, *, #71006, .F. ) ;
#23894=FACE_OUTER_BOUND ( 'NONE', #104200, .T. ) ;
#23897=CARTESIAN_POINT ( 'NONE',  ( 6.168902648239645181, 0.6556005035803867953, 6.499999999999999112 ) ) ;
#23907=CARTESIAN_POINT ( 'NONE',  ( 6.683837171061803417, 3.955946848495959234, -6.851900933636991375 ) ) ;
#23967=CIRCLE ( 'NONE', #97987, 4.000000000000001776 ) ;
#24014=CARTESIAN_POINT ( 'NONE',  ( 28.58349330513380337, 1.593028355512270962E-15, 0.000000000000000000 ) ) ;
#24023=DIRECTION ( 'NONE',  ( 1.000000000000000000, 1.224606353822377258E-16, 0.000000000000000000 ) ) ;
#24036=VERTEX_POINT ( 'NONE', #42177 ) ;
#24053=DIRECTION ( 'NONE',  ( 0.3420201433256622736, 1.150791560227853228E-16, 0.9396926207859106484 ) ) ;
#24089=CARTESIAN_POINT ( 'NONE',  ( 11.36650669486618881, 1.474610560812782335E-15, 0.000000000000000000 ) ) ;
#24146=EDGE_LOOP ( 'NONE', ( #20485, #37850, #79563, #89633, #82590 ) ) ;
#24181=CARTESIAN_POINT ( 'NONE',  ( 13.09999999999999787, 3.309500000000003439, 0.000000000000000000 ) ) ;
#24204=EDGE_CURVE ( 'NONE', #91446, #67548, #69136, .T. ) ;
#24221=CARTESIAN_POINT ( 'NONE',  ( 6.222742520105472686, -3.584500230190552639, -6.791463481567640237 ) ) ;
#24241=CARTESIAN_POINT ( 'NONE',  ( 13.58349330513380515, -4.000000000000000888, 4.898587196589416773E-16 ) ) ;
#24246=ORIENTED_EDGE ( 'NONE', *, *, #16901, .T. ) ;
#24261=CARTESIAN_POINT ( 'NONE',  ( 30.11650669486618881, 1.474610560812782335E-15, 0.000000000000000000 ) ) ;
#24303=AXIS2_PLACEMENT_3D ( 'NONE', #65401, #98293, #15250 ) ;
#24312=AXIS2_PLACEMENT_3D ( 'NONE', #53765, #12761, #38661 ) ;
#24319=CARTESIAN_POINT ( 'NONE',  ( 11.08349330513380515, -3.851859888774471706E-31, 4.000000000000001776 ) ) ;
#24325=CARTESIAN_POINT ( 'NONE',  ( 0.000000000000000000, 0.000000000000000000, 4.000000000000000888 ) ) ;
#24336=CONICAL_SURFACE ( 'NONE', #62223, 4.000000000000001776, 0.9599310885968774798 ) ;
#24353=EDGE_CURVE ( 'NONE', #102768, #88573, #16766, .T. ) ;
#24355=ORIENTED_EDGE ( 'NONE', *, *, #37468, .F. ) ;
#24377=ORIENTED_EDGE ( 'NONE', *, *, #70596, .T. ) ;
#24390=CIRCLE ( 'NONE', #53615, 4.000000000000000888 ) ;
#24400=EDGE_LOOP ( 'NONE', ( #18689, #56233, #25292, #28862, #99186 ) ) ;
#24402=EDGE_LOOP ( 'NONE', ( #68391, #14616, #85393, #35409, #29965 ) ) ;
#24415=EDGE_CURVE ( 'NONE', #38226, #9148, #13293, .T. ) ;
#24422=CIRCLE ( 'NONE', #17465, 4.000000000000001776 ) ;
#24460=DIRECTION ( 'NONE',  ( -1.000000000000000000, -1.224606353822377258E-16, -0.000000000000000000 ) ) ;
#24501=CARTESIAN_POINT ( 'NONE',  ( 6.683837171061806082, 7.911893696991936231, -4.595687358162529387E-16 ) ) ;
#24515=DIRECTION ( 'NONE',  ( -1.000000000000000000, -0.000000000000000000, -0.000000000000000000 ) ) ;
#24516=ORIENTED_EDGE ( 'NONE', *, *, #46803, .F. ) ;
#24529=DIRECTION ( 'NONE',  ( -1.000000000000000000, -1.224606353822377258E-16, -0.000000000000000000 ) ) ;
#24560=CARTESIAN_POINT ( 'NONE',  ( 30.59999999999999787, 1.533819458162526451E-15, 0.000000000000000000 ) ) ;
#24577=DIRECTION ( 'NONE',  ( -1.000000000000000000, -1.224606353822377258E-16, -0.000000000000000000 ) ) ;
#24579=DIRECTION ( 'NONE',  ( 0.000000000000000000, -1.000000000000000000, 0.000000000000000000 ) ) ;
#24717=DIRECTION ( 'NONE',  ( -1.000000000000000000, -1.224606353822377258E-16, -0.000000000000000000 ) ) ;
#24745=CARTESIAN_POINT ( 'NONE',  ( 5.975663821521703056, -4.257391242883674209, -5.625982059626680076 ) ) ;
#24755=CARTESIAN_POINT ( 'NONE',  ( 0.000000000000000000, -5.629165124598847214, 3.250000000000005329 ) ) ;
#24766=VECTOR ( 'NONE', #41270, 1000.000000000000000 ) ;
#24776=DIRECTION ( 'NONE',  ( -1.000000000000000000, -1.224606353822377258E-16, -0.000000000000000000 ) ) ;
#24794=DIRECTION ( 'NONE',  ( 0.000000000000000000, -1.000000000000000000, 0.000000000000000000 ) ) ;
#24823=( GEOMETRIC_REPRESENTATION_CONTEXT ( 3 ) GLOBAL_UNCERTAINTY_ASSIGNED_CONTEXT ( ( #70761 ) ) GLOBAL_UNIT_ASSIGNED_CONTEXT ( ( #14790, #80583, #46123 ) ) REPRESENTATION_CONTEXT ( 'NONE', 'WORKASPACE' ) );
#24838=EDGE_CURVE ( 'NONE', #20995, #78892, #73406, .T. ) ;
#24857=DIRECTION ( 'NONE',  ( 0.000000000000000000, 0.000000000000000000, 1.000000000000000000 ) ) ;
#24869=CARTESIAN_POINT ( 'NONE',  ( 31.84999999999999787, 3.309500000000003439, 4.052968581778167743E-16 ) ) ;
#24901=DIRECTION ( 'NONE',  ( 0.000000000000000000, -1.000000000000000000, 0.000000000000000000 ) ) ;
#24902=DIRECTION ( 'NONE',  ( -1.000000000000000000, -1.224606353822377258E-16, -0.000000000000000000 ) ) ;
#24904=DIRECTION ( 'NONE',  ( -1.000000000000000000, -1.224606353822377258E-16, -0.000000000000000000 ) ) ;
#24940=ORIENTED_EDGE ( 'NONE', *, *, #46512, .F. ) ;
#24944=ORIENTED_EDGE ( 'NONE', *, *, #7740, .T. ) ;
#24976=VECTOR ( 'NONE', #79270, 1000.000000000000000 ) ;
#24999=EDGE_LOOP ( 'NONE', ( #105560, #4318, #53197, #5521, #42298 ) ) ;
#25003=CIRCLE ( 'NONE', #40449, 4.000000000000000888 ) ;
#25037=DIRECTION ( 'NONE',  ( -1.000000000000000000, -0.000000000000000000, -0.000000000000000000 ) ) ;
#25041=VERTEX_POINT ( 'NONE', #82693 ) ;
#25067=EDGE_CURVE ( 'NONE', #7599, #26910, #34712, .T. ) ;
#25087=ORIENTED_EDGE ( 'NONE', *, *, #92182, .T. ) ;
#25091=CARTESIAN_POINT ( 'NONE',  ( 0.000000000000000000, 0.000000000000000000, 0.000000000000000000 ) ) ;
#25099=VERTEX_POINT ( 'NONE', #24501 ) ;
#25123=CONICAL_SURFACE ( 'NONE', #88851, 4.000000000000001776, 0.9599310885968774798 ) ;
#25131=AXIS2_PLACEMENT_3D ( 'NONE', #65486, #57902, #98375 ) ;
#25137=DIRECTION ( 'NONE',  ( 0.000000000000000000, 0.000000000000000000, 1.000000000000000000 ) ) ;
#25233=DIRECTION ( 'NONE',  ( -1.000000000000000000, -1.224606353822377258E-16, -0.000000000000000000 ) ) ;
#25238=ADVANCED_FACE ( 'NONE', ( #76714 ), #80267, .T. ) ;
#25258=ORIENTED_EDGE ( 'NONE', *, *, #39843, .T. ) ;
#25267=PLANE ( 'NONE',  #72618 ) ;
#25269=CARTESIAN_POINT ( 'NONE',  ( 21.84999999999999787, 1.533819458162526451E-15, 0.000000000000000000 ) ) ;
#25292=ORIENTED_EDGE ( 'NONE', *, *, #14629, .T. ) ;
#25293=ORIENTED_EDGE ( 'NONE', *, *, #48512, .T. ) ;
#25294=CARTESIAN_POINT ( 'NONE',  ( 0.2578475836320698322, -4.367703157927332214, 5.434916218090831030 ) ) ;
#25319=LINE ( 'NONE', #33946, #46778 ) ;
#25392=DIRECTION ( 'NONE',  ( 0.000000000000000000, -1.000000000000000000, 0.000000000000000000 ) ) ;
#25412=DIRECTION ( 'NONE',  ( -1.000000000000000000, -1.224606353822377258E-16, -0.000000000000000000 ) ) ;
#25422=EDGE_CURVE ( 'NONE', #57770, #82322, #14902, .T. ) ;
#25423=DIRECTION ( 'NONE',  ( 0.000000000000000000, -1.000000000000000000, 0.000000000000000000 ) ) ;
#25430=VECTOR ( 'NONE', #86720, 1000.000000000000341 ) ;
#25495=CARTESIAN_POINT ( 'NONE',  ( 6.568242156162281908, 3.336471507263022218, 6.846117829660598453 ) ) ;
#25572=CONICAL_SURFACE ( 'NONE', #80647, 3.309500000000001663, 0.9599310885968770357 ) ;
#25602=DIRECTION ( 'NONE',  ( 0.000000000000000000, 0.000000000000000000, -1.000000000000000000 ) ) ;
#25608=CARTESIAN_POINT ( 'NONE',  ( 23.09999999999999432, 1.533819458162526451E-15, 0.000000000000000000 ) ) ;
#25621=CARTESIAN_POINT ( 'NONE',  ( 0.05533025579362249591, -6.264553569211843254, 2.149474931388136945 ) ) ;
#25634=FACE_OUTER_BOUND ( 'NONE', #27720, .T. ) ;
#25655=DIRECTION ( 'NONE',  ( -1.000000000000000000, -1.224606353822377258E-16, -0.000000000000000000 ) ) ;
#25671=DIRECTION ( 'NONE',  ( 0.000000000000000000, -1.000000000000000000, 0.000000000000000000 ) ) ;
#25678=DIRECTION ( 'NONE',  ( -1.000000000000000000, -1.224606353822377258E-16, -0.000000000000000000 ) ) ;
#25721=ADVANCED_FACE ( 'NONE', ( #51780 ), #80347, .T. ) ;
#25729=CARTESIAN_POINT ( 'NONE',  ( 6.683837171061806082, -3.955946848495971668, -6.851900933636991375 ) ) ;
#25730=EDGE_CURVE ( 'NONE', #66061, #66358, #97021, .T. ) ;
#25734=ORIENTED_EDGE ( 'NONE', *, *, #2446, .T. ) ;
#25738=VERTEX_POINT ( 'NONE', #30736 ) ;
#25793=AXIS2_PLACEMENT_3D ( 'NONE', #74504, #42141, #76101 ) ;
#25809=DIRECTION ( 'NONE',  ( -1.000000000000000000, -1.224606353822377258E-16, -0.000000000000000000 ) ) ;
#25825=CIRCLE ( 'NONE', #1650, 3.309500000000001663 ) ;
#25827=CARTESIAN_POINT ( 'NONE',  ( 24.34999999999999787, 1.533819458162526451E-15, 0.000000000000000000 ) ) ;
#25829=DIRECTION ( 'NONE',  ( -1.000000000000000000, -1.224606353822377258E-16, -0.000000000000000000 ) ) ;
#25841=FACE_OUTER_BOUND ( 'NONE', #6437, .T. ) ;
#25844=VECTOR ( 'NONE', #50091, 1000.000000000000000 ) ;
#25862=ORIENTED_EDGE ( 'NONE', *, *, #41792, .T. ) ;
#25874=CARTESIAN_POINT ( 'NONE',  ( 20.59999999999999787, -3.309499999999999886, 0.000000000000000000 ) ) ;
#25908=ORIENTED_EDGE ( 'NONE', *, *, #60818, .F. ) ;
#25927=EDGE_CURVE ( 'NONE', #9982, #90846, #9822, .T. ) ;
#25966=LINE ( 'NONE', #24869, #94899 ) ;
#25973=DIRECTION ( 'NONE',  ( 0.000000000000000000, 0.000000000000000000, -1.000000000000000000 ) ) ;
#25977=CARTESIAN_POINT ( 'NONE',  ( 17.33349330513380693, 1.593028355512270962E-15, 0.000000000000000000 ) ) ;
#25992=AXIS2_PLACEMENT_3D ( 'NONE', #37289, #56052, #96556 ) ;
#26003=EDGE_LOOP ( 'NONE', ( #32900, #78242, #29815, #4895, #65812 ) ) ;
#26010=FACE_OUTER_BOUND ( 'NONE', #65858, .T. ) ;
#26014=EDGE_CURVE ( 'NONE', #44978, #31177, #104536, .T. ) ;
#26018=AXIS2_PLACEMENT_3D ( 'NONE', #104383, #45120, #70446 ) ;
#26032=DIRECTION ( 'NONE',  ( -1.000000000000000000, -1.224606353822377258E-16, -0.000000000000000000 ) ) ;
#26035=DIRECTION ( 'NONE',  ( 0.000000000000000000, 0.000000000000000000, 1.000000000000000000 ) ) ;
#26061=CIRCLE ( 'NONE', #17399, 3.309500000000001663 ) ;
#26077=CONICAL_SURFACE ( 'NONE', #74197, 3.309500000000001663, 0.9599310885968770357 ) ;
#26125=DIRECTION ( 'NONE',  ( 0.000000000000000000, 1.000000000000000000, 0.000000000000000000 ) ) ;
#26139=ORIENTED_EDGE ( 'NONE', *, *, #63229, .T. ) ;
#26147=LINE ( 'NONE', #1799, #36566 ) ;
#26148=CARTESIAN_POINT ( 'NONE',  ( 0.000000000000000000, 0.000000000000000000, 0.000000000000000000 ) ) ;
#26190=DIRECTION ( 'NONE',  ( 0.000000000000000000, -1.000000000000000000, 0.000000000000000000 ) ) ;
#26192=CARTESIAN_POINT ( 'NONE',  ( 18.58349330513380693, 4.898587196589411843E-16, -4.000000000000001776 ) ) ;
#26223=LINE ( 'NONE', #74176, #11714 ) ;
#26244=ORIENTED_EDGE ( 'NONE', *, *, #7689, .F. ) ;
#26261=DIRECTION ( 'NONE',  ( -1.000000000000000000, -1.224606353822377258E-16, -0.000000000000000000 ) ) ;
#26263=EDGE_CURVE ( 'NONE', #81794, #99203, #85617, .T. ) ;
#26284=VERTEX_POINT ( 'NONE', #94261 ) ;
#26308=DIRECTION ( 'NONE',  ( 0.000000000000000000, -1.000000000000000000, 0.000000000000000000 ) ) ;
#26347=DIRECTION ( 'NONE',  ( -1.000000000000000000, -1.224606353822377258E-16, -0.000000000000000000 ) ) ;
#26361=CARTESIAN_POINT ( 'NONE',  ( 0.000000000000000000, 4.898587196589413815E-16, -4.000000000000000888 ) ) ;
#26391=DIRECTION ( 'NONE',  ( 0.000000000000000000, -1.000000000000000000, 0.000000000000000000 ) ) ;
#26401=VECTOR ( 'NONE', #27222, 1000.000000000000227 ) ;
#26415=FACE_OUTER_BOUND ( 'NONE', #10705, .T. ) ;
#26418=CONICAL_SURFACE ( 'NONE', #84965, 3.309500000000001663, 0.9599310885968770357 ) ;
#26423=ORIENTED_EDGE ( 'NONE', *, *, #62642, .T. ) ;
#26431=ORIENTED_EDGE ( 'NONE', *, *, #49212, .F. ) ;
#26444=DIRECTION ( 'NONE',  ( 1.000000000000000000, 1.224606353822377258E-16, 0.000000000000000000 ) ) ;
#26449=DIRECTION ( 'NONE',  ( -1.000000000000000000, -1.224606353822377258E-16, -0.000000000000000000 ) ) ;
#26460=VECTOR ( 'NONE', #60968, 1000.000000000000000 ) ;
#26482=DIRECTION ( 'NONE',  ( 0.000000000000000000, -1.000000000000000000, 0.000000000000000000 ) ) ;
#26483=CIRCLE ( 'NONE', #31630, 4.000000000000001776 ) ;
#26500=DIRECTION ( 'NONE',  ( -1.000000000000000000, -1.224606353822377258E-16, -0.000000000000000000 ) ) ;
#26565=CARTESIAN_POINT ( 'NONE',  ( 11.36650669486618881, 1.474610560812782335E-15, 0.000000000000000000 ) ) ;
#26566=DIRECTION ( 'NONE',  ( -1.000000000000000000, -0.000000000000000000, -0.000000000000000000 ) ) ;
#26567=B_SPLINE_CURVE_WITH_KNOTS ( 'NONE', 3,
 ( #25729, #19769, #83911, #42385, #77423, #100624 ),
 .UNSPECIFIED., .F., .F.,
 ( 4, 2, 4 ),
 ( 0.000000000000000000, 0.001995463903526791850, 0.003990927807053583701 ),
 .UNSPECIFIED. ) ;
#26587=EDGE_CURVE ( 'NONE', #98662, #42319, #58107, .T. ) ;
#26601=CIRCLE ( 'NONE', #2440, 4.000000000000001776 ) ;
#26602=DIRECTION ( 'NONE',  ( -1.000000000000000000, -0.000000000000000000, -0.000000000000000000 ) ) ;
#26607=DIRECTION ( 'NONE',  ( 0.000000000000000000, -1.000000000000000000, 0.000000000000000000 ) ) ;
#26614=LINE ( 'NONE', #91840, #66764 ) ;
#26616=( BOUNDED_SURFACE ( )  B_SPLINE_SURFACE ( 3, 2, ( 
 ( #39240, #47300, #71055 ),
 ( #80196, #104479, #64567 ),
 ( #6300, #105023, #31164 ),
 ( #47820, #72641, #30092 ),
 ( #31681, #62975, #48359 ),
 ( #23595, #89376, #81251 ) ),
 .UNSPECIFIED., .F., .F., .F. ) 
 B_SPLINE_SURFACE_WITH_KNOTS ( ( 4, 2, 4 ),
 ( 3, 3 ),
 ( 0.03206831234578191858, 0.03607477026923514019, 0.04008122819268836873 ),
 ( 0.000000000000000000, 1.000000000000000000 ),
 .UNSPECIFIED. ) 
 GEOMETRIC_REPRESENTATION_ITEM ( )  RATIONAL_B_SPLINE_SURFACE ( (
 ( 1.000000000000000000, 0.8047780936700358323, 1.000000000000000000),
 ( 1.000000000000000000, 0.8123790890099117368, 1.000000000000000000),
 ( 1.000000000000000000, 0.8190678900508682192, 1.000000000000000000),
 ( 1.000000000000000000, 0.8192345188317075033, 1.000000000000000000),
 ( 1.000000000000000000, 0.8126126219723355248, 1.000000000000000000),
 ( 1.000000000000000000, 0.8047712657247791945, 1.000000000000000000) ) ) 
 REPRESENTATION_ITEM ( '' )  SURFACE ( )  );
#26618=VERTEX_POINT ( 'NONE', #61520 ) ;
#26646=ORIENTED_EDGE ( 'NONE', *, *, #99351, .T. ) ;
#26680=CARTESIAN_POINT ( 'NONE',  ( 11.08349330513380515, 4.898587196589411843E-16, -4.000000000000001776 ) ) ;
#26692=DIRECTION ( 'NONE',  ( 0.000000000000000000, -1.000000000000000000, 0.000000000000000000 ) ) ;
#26704=CARTESIAN_POINT ( 'NONE',  ( 30.11650669486618881, 1.474610560812782335E-15, 0.000000000000000000 ) ) ;
#26720=DIRECTION ( 'NONE',  ( 0.000000000000000000, 0.5000000000000009992, 0.8660254037844381525 ) ) ;
#26729=CARTESIAN_POINT ( 'NONE',  ( 0.000000000000000000, 0.000000000000000000, 0.000000000000000000 ) ) ;
#26831=ORIENTED_EDGE ( 'NONE', *, *, #71252, .F. ) ;
#26884=DIRECTION ( 'NONE',  ( -1.000000000000000000, -0.000000000000000000, -0.000000000000000000 ) ) ;
#26888=ORIENTED_EDGE ( 'NONE', *, *, #39369, .T. ) ;
#26894=DIRECTION ( 'NONE',  ( -1.000000000000000000, -0.000000000000000000, -0.000000000000000000 ) ) ;
#26905=CIRCLE ( 'NONE', #38960, 4.000000000000000888 ) ;
#26910=VERTEX_POINT ( 'NONE', #41990 ) ;
#26912=VECTOR ( 'NONE', #2145, 1000.000000000000000 ) ;
#26941=CYLINDRICAL_SURFACE ( 'NONE', #90978, 4.000000000000000888 ) ;
#26978=ADVANCED_FACE ( 'NONE', ( #57100 ), #4833, .T. ) ;
#26995=CONICAL_SURFACE ( 'NONE', #66606, 4.000000000000001776, 0.9599310885968774798 ) ;
#27005=DIRECTION ( 'NONE',  ( 0.000000000000000000, -1.000000000000000000, 0.000000000000000000 ) ) ;
#27020=FACE_OUTER_BOUND ( 'NONE', #83424, .T. ) ;
#27048=VECTOR ( 'NONE', #70100, 1000.000000000000341 ) ;
#27059=ORIENTED_EDGE ( 'NONE', *, *, #75224, .F. ) ;
#27066=ORIENTED_EDGE ( 'NONE', *, *, #59356, .T. ) ;
#27093=DIRECTION ( 'NONE',  ( -1.000000000000000000, -1.224606353822377258E-16, -0.000000000000000000 ) ) ;
#27094=DIRECTION ( 'NONE',  ( -1.000000000000000000, -1.224606353822377258E-16, -0.000000000000000000 ) ) ;
#27114=ORIENTED_EDGE ( 'NONE', *, *, #31364, .F. ) ;
#27131=DIRECTION ( 'NONE',  ( 0.000000000000000000, 0.000000000000000000, 1.000000000000000000 ) ) ;
#27144=VECTOR ( 'NONE', #85786, 1000.000000000000000 ) ;
#27171=DIRECTION ( 'NONE',  ( -1.000000000000000000, -0.000000000000000000, -0.000000000000000000 ) ) ;
#27183=LINE ( 'NONE', #60599, #102640 ) ;
#27218=CIRCLE ( 'NONE', #16866, 4.000000000000000888 ) ;
#27222=DIRECTION ( 'NONE',  ( 0.5735764363510491570, -0.8191520442889895781, 1.003171929053522035E-16 ) ) ;
#27275=AXIS2_PLACEMENT_3D ( 'NONE', #94502, #37346, #70208 ) ;
#27286=FACE_OUTER_BOUND ( 'NONE', #22459, .T. ) ;
#27330=DIRECTION ( 'NONE',  ( -1.000000000000000000, -1.224606353822377258E-16, -0.000000000000000000 ) ) ;
#27343=VERTEX_POINT ( 'NONE', #100103 ) ;
#27344=CARTESIAN_POINT ( 'NONE',  ( 0.000000000000000000, 4.898587196589413815E-16, -4.000000000000000888 ) ) ;
#27361=CARTESIAN_POINT ( 'NONE',  ( 0.000000000000000000, 0.000000000000000000, 0.000000000000000000 ) ) ;
#27366=ORIENTED_EDGE ( 'NONE', *, *, #104173, .F. ) ;
#27372=DIRECTION ( 'NONE',  ( 1.000000000000000000, 0.000000000000000000, 0.000000000000000000 ) ) ;
#27383=CARTESIAN_POINT ( 'NONE',  ( 14.34999999999999787, 1.533819458162526451E-15, 0.000000000000000000 ) ) ;
#27442=CONICAL_SURFACE ( 'NONE', #15388, 3.309500000000001663, 0.9599310885968770357 ) ;
#27466=AXIS2_PLACEMENT_3D ( 'NONE', #20658, #29264, #101517 ) ;
#27538=DIRECTION ( 'NONE',  ( -1.000000000000000000, -0.000000000000000000, -0.000000000000000000 ) ) ;
#27545=CARTESIAN_POINT ( 'NONE',  ( 0.000000000000000000, 4.898587196589413815E-16, -4.000000000000000888 ) ) ;
#27553=LINE ( 'NONE', #99794, #26912 ) ;
#27565=VECTOR ( 'NONE', #15358, 1000.000000000000000 ) ;
#27581=EDGE_CURVE ( 'NONE', #82621, #26618, #10067, .T. ) ;
#27596=ORIENTED_EDGE ( 'NONE', *, *, #70152, .F. ) ;
#27602=ORIENTED_EDGE ( 'NONE', *, *, #43391, .T. ) ;
#27606=EDGE_CURVE ( 'NONE', #89753, #67545, #73028, .T. ) ;
#27642=DIRECTION ( 'NONE',  ( -1.000000000000000000, -1.224606353822377258E-16, -0.000000000000000000 ) ) ;
#27656=AXIS2_PLACEMENT_3D ( 'NONE', #90812, #24515, #80571 ) ;
#27659=ORIENTED_EDGE ( 'NONE', *, *, #97404, .F. ) ;
#27666=ADVANCED_FACE ( 'NONE', ( #101046 ), #67631, .T. ) ;
#27683=DIRECTION ( 'NONE',  ( -0.5735764363510497121, 0.8191520442889892450, 1.003171929053521665E-16 ) ) ;
#27701=CIRCLE ( 'NONE', #24303, 3.309500000000001663 ) ;
#27716=EDGE_CURVE ( 'NONE', #35657, #93202, #38668, .T. ) ;
#27720=EDGE_LOOP ( 'NONE', ( #58692, #62237, #66477, #38086, #8595 ) ) ;
#27767=DIRECTION ( 'NONE',  ( 0.000000000000000000, -1.000000000000000000, 0.000000000000000000 ) ) ;
#27792=AXIS2_PLACEMENT_3D ( 'NONE', #70183, #21145, #62632 ) ;
#27843=CARTESIAN_POINT ( 'NONE',  ( 15.11650669486618881, 4.000000000000003553, 4.898587196589414801E-16 ) ) ;
#27921=DIRECTION ( 'NONE',  ( 0.000000000000000000, -1.000000000000000000, 0.000000000000000000 ) ) ;
#28005=CARTESIAN_POINT ( 'NONE',  ( 0.000000000000000000, 0.000000000000000000, 4.000000000000000888 ) ) ;
#28041=ORIENTED_EDGE ( 'NONE', *, *, #72474, .T. ) ;
#28056=DIRECTION ( 'NONE',  ( 0.000000000000000000, -1.000000000000000000, 0.000000000000000000 ) ) ;
#28093=DIRECTION ( 'NONE',  ( -1.000000000000000000, -1.224606353822377258E-16, -0.000000000000000000 ) ) ;
#28099=ORIENTED_EDGE ( 'NONE', *, *, #37039, .F. ) ;
#28101=EDGE_LOOP ( 'NONE', ( #87265, #60040, #63094, #29305, #43251 ) ) ;
#28115=EDGE_CURVE ( 'NONE', #18709, #16503, #73020, .T. ) ;
#28132=LINE ( 'NONE', #37819, #106418 ) ;
#28169=CARTESIAN_POINT ( 'NONE',  ( 5.691929483231186637, -5.629165124598852543, 3.250000000000002220 ) ) ;
#28192=ORIENTED_EDGE ( 'NONE', *, *, #78967, .F. ) ;
#28229=EDGE_CURVE ( 'NONE', #35708, #89211, #102737, .T. ) ;
#28303=CIRCLE ( 'NONE', #19767, 3.309500000000001663 ) ;
#28354=B_SPLINE_CURVE_WITH_KNOTS ( 'NONE', 3,
 ( #12434, #101465, #35161, #18992, #52912 ),
 .UNSPECIFIED., .F., .F.,
 ( 4, 1, 4 ),
 ( 0.000000000000000000, 0.003752776749732567464, 0.007505553499465134927 ),
 .UNSPECIFIED. ) ;
#28358=DIRECTION ( 'NONE',  ( -1.000000000000000000, -1.224606353822377258E-16, -0.000000000000000000 ) ) ;
#28361=ORIENTED_EDGE ( 'NONE', *, *, #95771, .T. ) ;
#28381=DIRECTION ( 'NONE',  ( 1.000000000000000000, 1.224606353822377258E-16, 0.000000000000000000 ) ) ;
#28390=EDGE_CURVE ( 'NONE', #78191, #26284, #106166, .T. ) ;
#28397=EDGE_CURVE ( 'NONE', #98690, #32616, #21492, .T. ) ;
#28407=CARTESIAN_POINT ( 'NONE',  ( 14.83349330513380693, 1.593028355512270962E-15, 0.000000000000000000 ) ) ;
#28435=CARTESIAN_POINT ( 'NONE',  ( 34.35000000000000142, 3.309500000000003439, 0.000000000000000000 ) ) ;
#28437=CARTESIAN_POINT ( 'NONE',  ( 26.36650669486618881, 0.000000000000000000, 4.000000000000000888 ) ) ;
#28455=DIRECTION ( 'NONE',  ( 0.000000000000000000, 0.000000000000000000, -1.000000000000000000 ) ) ;
#28460=LINE ( 'NONE', #29015, #72826 ) ;
#28474=CARTESIAN_POINT ( 'NONE',  ( 0.000000000000000000, 0.000000000000000000, 4.000000000000000888 ) ) ;
#28491=CARTESIAN_POINT ( 'NONE',  ( 21.84999999999999787, 1.533819458162526451E-15, 0.000000000000000000 ) ) ;
#28525=EDGE_CURVE ( 'NONE', #42350, #37712, #100958, .T. ) ;
#28565=CARTESIAN_POINT ( 'NONE',  ( 14.83349330513380693, -3.851859888774471706E-31, 4.000000000000001776 ) ) ;
#28575=CARTESIAN_POINT ( 'NONE',  ( 0.000000000000000000, 0.000000000000000000, 0.000000000000000000 ) ) ;
#28613=B_SPLINE_CURVE_WITH_KNOTS ( 'NONE', 3,
 ( #95785, #89287, #21918, #80112, #81168, #7278 ),
 .UNSPECIFIED., .F., .F.,
 ( 4, 2, 4 ),
 ( 0.01913986446880884540, 0.02104055318064343080, 0.02294124189247801621 ),
 .UNSPECIFIED. ) ;
#28618=CARTESIAN_POINT ( 'NONE',  ( 0.000000000000000000, 5.629165124598848102, -3.250000000000007105 ) ) ;
#28637=ORIENTED_EDGE ( 'NONE', *, *, #87065, .T. ) ;
#28642=DIRECTION ( 'NONE',  ( 0.000000000000000000, 1.000000000000000000, 0.000000000000000000 ) ) ;
#28665=EDGE_CURVE ( 'NONE', #56180, #88131, #33860, .T. ) ;
#28667=AXIS2_PLACEMENT_3D ( 'NONE', #88239, #103361, #104402 ) ;
#28731=DIRECTION ( 'NONE',  ( 0.000000000000000000, -1.000000000000000000, 0.000000000000000000 ) ) ;
#28734=AXIS2_PLACEMENT_3D ( 'NONE', #10606, #3057, #27921 ) ;
#28763=DIRECTION ( 'NONE',  ( -1.000000000000000000, -1.224606353822377258E-16, -0.000000000000000000 ) ) ;
#28790=DIRECTION ( 'NONE',  ( 0.000000000000000000, -1.000000000000000000, 0.000000000000000000 ) ) ;
#28856=VERTEX_POINT ( 'NONE', #6710 ) ;
#28862=ORIENTED_EDGE ( 'NONE', *, *, #38175, .T. ) ;
#28863=( LENGTH_UNIT ( ) NAMED_UNIT ( * ) SI_UNIT ( .MILLI., .METRE. ) );
#28868=VECTOR ( 'NONE', #1564, 1000.000000000000000 ) ;
#28871=FACE_OUTER_BOUND ( 'NONE', #56780, .T. ) ;
#28873=VECTOR ( 'NONE', #83524, 1000.000000000000000 ) ;
#28886=ADVANCED_FACE ( 'NONE', ( #6170 ), #82727, .T. ) ;
#28919=CARTESIAN_POINT ( 'NONE',  ( 22.33349330513380693, 1.593028355512270962E-15, 0.000000000000000000 ) ) ;
#28923=CONICAL_SURFACE ( 'NONE', #23734, 4.000000000000001776, 0.9599310885968774798 ) ;
#28930=DIRECTION ( 'NONE',  ( 0.000000000000000000, 1.000000000000000000, 0.000000000000000000 ) ) ;
#28934=AXIS2_PLACEMENT_3D ( 'NONE', #77406, #28358, #86589 ) ;
#28978=VECTOR ( 'NONE', #92156, 1000.000000000000227 ) ;
#28981=ORIENTED_EDGE ( 'NONE', *, *, #41792, .F. ) ;
#29015=CARTESIAN_POINT ( 'NONE',  ( 26.84999999999999787, -3.309499999999999886, 0.000000000000000000 ) ) ;
#29019=EDGE_CURVE ( 'NONE', #81142, #38220, #66617, .T. ) ;
#29052=LINE ( 'NONE', #14375, #25430 ) ;
#29110=CIRCLE ( 'NONE', #96282, 4.000000000000000888 ) ;
#29125=EDGE_CURVE ( 'NONE', #79927, #87702, #35633, .T. ) ;
#29162=CARTESIAN_POINT ( 'NONE',  ( 0.06682554136337871820, 4.993536075455421219, -4.350941807883113022 ) ) ;
#29177=VERTEX_POINT ( 'NONE', #85943 ) ;
#29178=ORIENTED_EDGE ( 'NONE', *, *, #90736, .F. ) ;
#29187=EDGE_CURVE ( 'NONE', #80223, #10937, #49355, .T. ) ;
#29194=ADVANCED_FACE ( 'NONE', ( #3940, #19101 ), #92400, .T. ) ;
#29264=DIRECTION ( 'NONE',  ( -1.000000000000000000, -1.224606353822377258E-16, -0.000000000000000000 ) ) ;
#29287=CARTESIAN_POINT ( 'NONE',  ( 6.683837171061802529, 3.955946848495962787, 6.851900933636986935 ) ) ;
#29305=ORIENTED_EDGE ( 'NONE', *, *, #1825, .F. ) ;
#29325=EDGE_CURVE ( 'NONE', #83521, #8349, #68403, .T. ) ;
#29330=CYLINDRICAL_SURFACE ( 'NONE', #45373, 4.000000000000000888 ) ;
#29342=CARTESIAN_POINT ( 'NONE',  ( 11.08349330513380515, 1.593028355512270962E-15, 0.000000000000000000 ) ) ;
#29357=DIRECTION ( 'NONE',  ( 0.000000000000000000, 0.000000000000000000, 1.000000000000000000 ) ) ;
#29365=ORIENTED_EDGE ( 'NONE', *, *, #258, .F. ) ;
#29379=SHAPE_REPRESENTATION_RELATIONSHIP ( 'NONE' , 'NONE' ,  #22667, #38340 ) ;
#29395=CARTESIAN_POINT ( 'NONE',  ( 16.08349330513380337, -3.851859888774471706E-31, 4.000000000000001776 ) ) ;
#29408=CIRCLE ( 'NONE', #77572, 4.000000000000001776 ) ;
#29411=DIRECTION ( 'NONE',  ( 0.000000000000000000, -1.000000000000000000, 0.000000000000000000 ) ) ;
#29414=ADVANCED_FACE ( 'NONE', ( #26010 ), #1214, .T. ) ;
#29438=AXIS2_PLACEMENT_3D ( 'NONE', #89417, #7940, #73739 ) ;
#29469=ORIENTED_EDGE ( 'NONE', *, *, #93163, .T. ) ;
#29494=CARTESIAN_POINT ( 'NONE',  ( 28.58349330513380337, 1.593028355512270962E-15, 0.000000000000000000 ) ) ;
#29554=CARTESIAN_POINT ( 'NONE',  ( 7.432714112156483503E-16, -0.6346842323187762425, -6.500000000000000888 ) ) ;
#29555=CONICAL_SURFACE ( 'NONE', #101887, 4.000000000000001776, 0.9599310885968774798 ) ;
#29567=ORIENTED_EDGE ( 'NONE', *, *, #60558, .F. ) ;
#29607=LINE ( 'NONE', #5816, #106487 ) ;
#29631=CARTESIAN_POINT ( 'NONE',  ( 36.36650669486618881, 1.474610560812782335E-15, 0.000000000000000000 ) ) ;
#29641=CARTESIAN_POINT ( 'NONE',  ( 6.575918192882435953, -7.701766175471826514, -3.282668101273427886E-15 ) ) ;
#29677=FACE_OUTER_BOUND ( 'NONE', #74110, .T. ) ;
#29682=CARTESIAN_POINT ( 'NONE',  ( 0.000000000000000000, 0.000000000000000000, 4.000000000000000888 ) ) ;
#29695=ORIENTED_EDGE ( 'NONE', *, *, #64219, .T. ) ;
#29732=AXIS2_PLACEMENT_3D ( 'NONE', #31452, #64334, #96692 ) ;
#29744=AXIS2_PLACEMENT_3D ( 'NONE', #5693, #88219, #55806 ) ;
#29745=EDGE_CURVE ( 'NONE', #45187, #87964, #85679, .T. ) ;
#29766=FACE_OUTER_BOUND ( 'NONE', #50450, .T. ) ;
#29772=DIRECTION ( 'NONE',  ( 0.000000000000000000, 0.000000000000000000, -1.000000000000000000 ) ) ;
#29779=AXIS2_PLACEMENT_3D ( 'NONE', #30389, #15237, #13633 ) ;
#29781=CARTESIAN_POINT ( 'NONE',  ( 11.84999999999999787, 1.533819458162526451E-15, 0.000000000000000000 ) ) ;
#29809=CARTESIAN_POINT ( 'NONE',  ( 6.289692432696784685, 1.244853941008388061E-13, 6.828989928337166226 ) ) ;
#29815=ORIENTED_EDGE ( 'NONE', *, *, #10972, .F. ) ;
#29825=EDGE_CURVE ( 'NONE', #88573, #31318, #67883, .T. ) ;
#29832=CARTESIAN_POINT ( 'NONE',  ( 32.61650669486618881, 1.474610560812782335E-15, 0.000000000000000000 ) ) ;
#29858=CARTESIAN_POINT ( 'NONE',  ( 6.445370176742148516, -4.584736124524471101, 5.738941594275039471 ) ) ;
#29878=ORIENTED_EDGE ( 'NONE', *, *, #6996, .T. ) ;
#29891=CARTESIAN_POINT ( 'NONE',  ( 19.83349330513380693, 4.898587196589411843E-16, -4.000000000000001776 ) ) ;
#29929=DIRECTION ( 'NONE',  ( 0.000000000000000000, -1.000000000000000000, 0.000000000000000000 ) ) ;
#29944=VECTOR ( 'NONE', #40599, 1000.000000000000000 ) ;
#29965=ORIENTED_EDGE ( 'NONE', *, *, #4714, .F. ) ;
#29972=FACE_OUTER_BOUND ( 'NONE', #49211, .T. ) ;
#30003=LINE ( 'NONE', #37044, #98254 ) ;
#30008=DIRECTION ( 'NONE',  ( 0.000000000000000000, -1.000000000000000000, 0.000000000000000000 ) ) ;
#30024=CIRCLE ( 'NONE', #4140, 4.000000000000000888 ) ;
#30092=CARTESIAN_POINT ( 'NONE',  ( 6.287679341995269233, -1.331405739683436007, -6.828854810278214948 ) ) ;
#30100=B_SPLINE_CURVE_WITH_KNOTS ( 'NONE', 3,
 ( #73156, #706, #17488, #33679, #31683, #30627 ),
 .UNSPECIFIED., .F., .F.,
 ( 4, 2, 4 ),
 ( -4.698498716302814272E-06, 0.0003457374136927988083, 0.0006961733261019004918 ),
 .UNSPECIFIED. ) ;
#30124=ORIENTED_EDGE ( 'NONE', *, *, #6996, .F. ) ;
#30155=CARTESIAN_POINT ( 'NONE',  ( 6.683837171061806970, -7.911893696991936231, 5.688671339918660213E-17 ) ) ;
#30158=DIRECTION ( 'NONE',  ( 0.000000000000000000, -1.000000000000000000, 0.000000000000000000 ) ) ;
#30199=ORIENTED_EDGE ( 'NONE', *, *, #105092, .T. ) ;
#30225=ORIENTED_EDGE ( 'NONE', *, *, #5206, .F. ) ;
#30236=ADVANCED_FACE ( 'NONE', ( #95626 ), #59029, .F. ) ;
#30246=ADVANCED_FACE ( 'NONE', ( #105824 ), #31965, .T. ) ;
#30260=VECTOR ( 'NONE', #11561, 1000.000000000000227 ) ;
#30267=CONICAL_SURFACE ( 'NONE', #92281, 6.500000000000000000, 1.047197551196600296 ) ;
#30285=DIRECTION ( 'NONE',  ( 1.000000000000000000, 1.224606353822377258E-16, 0.000000000000000000 ) ) ;
#30304=DIRECTION ( 'NONE',  ( -1.000000000000000000, -1.224606353822377258E-16, -0.000000000000000000 ) ) ;
#30305=VERTEX_POINT ( 'NONE', #36771 ) ;
#30331=CARTESIAN_POINT ( 'NONE',  ( 28.58349330513380337, 1.593028355512270962E-15, 0.000000000000000000 ) ) ;
#30373=FACE_OUTER_BOUND ( 'NONE', #53853, .T. ) ;
#30382=FACE_OUTER_BOUND ( 'NONE', #63972, .T. ) ;
#30389=CARTESIAN_POINT ( 'NONE',  ( 0.000000000000000000, 0.000000000000000000, 0.000000000000000000 ) ) ;
#30391=AXIS2_PLACEMENT_3D ( 'NONE', #90961, #26261, #7885 ) ;
#30421=ORIENTED_EDGE ( 'NONE', *, *, #95673, .F. ) ;
#30431=AXIS2_PLACEMENT_3D ( 'NONE', #33849, #66721, #99602 ) ;
#30433=CIRCLE ( 'NONE', #90692, 4.000000000000001776 ) ;
#30434=CYLINDRICAL_SURFACE ( 'NONE', #78412, 4.000000000000000888 ) ;
#30441=VERTEX_POINT ( 'NONE', #64205 ) ;
#30524=CARTESIAN_POINT ( 'NONE',  ( 0.000000000000000000, 0.000000000000000000, 4.000000000000000888 ) ) ;
#30529=CARTESIAN_POINT ( 'NONE',  ( 28.86650669486618881, 1.474610560812782335E-15, 0.000000000000000000 ) ) ;
#30543=CARTESIAN_POINT ( 'NONE',  ( 0.000000000000000000, 0.000000000000000000, 4.000000000000000888 ) ) ;
#30570=DIRECTION ( 'NONE',  ( -1.000000000000000000, -1.224606353822377258E-16, -0.000000000000000000 ) ) ;
#30576=VECTOR ( 'NONE', #68672, 1000.000000000000227 ) ;
#30601=CARTESIAN_POINT ( 'NONE',  ( 0.000000000000000000, 7.511572993685796142E-16, -6.500000000000000888 ) ) ;
#30627=CARTESIAN_POINT ( 'NONE',  ( 6.162888688655344893, 3.752776749732562589, -6.500000000000000888 ) ) ;
#30658=DIRECTION ( 'NONE',  ( -1.000000000000000000, -0.000000000000000000, -0.000000000000000000 ) ) ;
#30663=VERTEX_POINT ( 'NONE', #94320 ) ;
#30722=CARTESIAN_POINT ( 'NONE',  ( 6.169949891408690767, -6.308465495018908520, -2.073417244830776163 ) ) ;
#30735=CARTESIAN_POINT ( 'NONE',  ( 6.692588830498425345, 3.932766476276031486, 6.892929031562513131 ) ) ;
#30736=CARTESIAN_POINT ( 'NONE',  ( 29.83349330513380693, 4.000000000000002665, 0.000000000000000000 ) ) ;
#30747=VERTEX_POINT ( 'NONE', #75988 ) ;
#30763=ORIENTED_EDGE ( 'NONE', *, *, #92466, .F. ) ;
#30775=CARTESIAN_POINT ( 'NONE',  ( 6.683837171061806970, -7.911893696991936231, 5.688671339918660213E-17 ) ) ;
#30805=DIRECTION ( 'NONE',  ( -1.000000000000000000, -1.224606353822377258E-16, -0.000000000000000000 ) ) ;
#30809=EDGE_CURVE ( 'NONE', #26618, #17716, #29607, .T. ) ;
#30819=VECTOR ( 'NONE', #79529, 1000.000000000000000 ) ;
#30821=CONICAL_SURFACE ( 'NONE', #22191, 4.000000000000001776, 0.9599310885968774798 ) ;
#30857=ORIENTED_EDGE ( 'NONE', *, *, #34126, .T. ) ;
#30859=DIRECTION ( 'NONE',  ( -1.000000000000000000, -1.224606353822377258E-16, -0.000000000000000000 ) ) ;
#30860=ORIENTED_EDGE ( 'NONE', *, *, #34019, .T. ) ;
#30888=ORIENTED_EDGE ( 'NONE', *, *, #15027, .T. ) ;
#30900=DIRECTION ( 'NONE',  ( 0.000000000000000000, -1.000000000000000000, 0.000000000000000000 ) ) ;
#30928=CARTESIAN_POINT ( 'NONE',  ( 6.289692432696780244, 0.6618655008720334409, -6.828989928337168891 ) ) ;
#30995=ADVANCED_FACE ( 'NONE', ( #49456 ), #80618, .T. ) ;
#31004=ORIENTED_EDGE ( 'NONE', *, *, #53322, .F. ) ;
#31009=EDGE_LOOP ( 'NONE', ( #44251, #38942, #32990, #60260, #90939 ) ) ;
#31022=CIRCLE ( 'NONE', #39627, 4.000000000000000888 ) ;
#31027=SURFACE_SIDE_STYLE ('',( #87647 ) ) ;
#31063=LINE ( 'NONE', #91393, #51749 ) ;
#31087=DIRECTION ( 'NONE',  ( 0.000000000000000000, 1.000000000000000000, 0.000000000000000000 ) ) ;
#31091=FACE_OUTER_BOUND ( 'NONE', #2692, .T. ) ;
#31097=AXIS2_PLACEMENT_3D ( 'NONE', #26565, #27094, #99873 ) ;
#31137=CIRCLE ( 'NONE', #79298, 4.000000000000000888 ) ;
#31142=DIRECTION ( 'NONE',  ( 0.000000000000000000, -1.000000000000000000, 0.000000000000000000 ) ) ;
#31154=ORIENTED_EDGE ( 'NONE', *, *, #41725, .F. ) ;
#31164=CARTESIAN_POINT ( 'NONE',  ( 6.291746522141163922, 1.386194408032345615, -6.829127798246563685 ) ) ;
#31177=VERTEX_POINT ( 'NONE', #22452 ) ;
#31198=DIRECTION ( 'NONE',  ( -1.000000000000000000, -1.224606353822377258E-16, -0.000000000000000000 ) ) ;
#31203=ORIENTED_EDGE ( 'NONE', *, *, #61722, .F. ) ;
#31213=DIRECTION ( 'NONE',  ( 0.000000000000000000, -1.000000000000000000, 0.000000000000000000 ) ) ;
#31216=FACE_OUTER_BOUND ( 'NONE', #59919, .T. ) ;
#31234=AXIS2_PLACEMENT_3D ( 'NONE', #53976, #94473, #36792 ) ;
#31249=B_SPLINE_CURVE_WITH_KNOTS ( 'NONE', 3,
 ( #8332, #22964, #40701, #14293, #7792, #73588 ),
 .UNSPECIFIED., .F., .F.,
 ( 4, 2, 4 ),
 ( 0.003990927807053575027, 0.005983070073873393568, 0.007975212340693212110 ),
 .UNSPECIFIED. ) ;
#31253=ORIENTED_EDGE ( 'NONE', *, *, #87065, .F. ) ;
#31318=VERTEX_POINT ( 'NONE', #33000 ) ;
#31351=CARTESIAN_POINT ( 'NONE',  ( 34.35000000000000142, 1.533819458162526451E-15, 0.000000000000000000 ) ) ;
#31358=ORIENTED_EDGE ( 'NONE', *, *, #58254, .F. ) ;
#31364=EDGE_CURVE ( 'NONE', #53134, #78006, #68723, .T. ) ;
#31370=ORIENTED_EDGE ( 'NONE', *, *, #96592, .F. ) ;
#31419=ADVANCED_FACE ( 'NONE', ( #92799 ), #18960, .T. ) ;
#31452=CARTESIAN_POINT ( 'NONE',  ( 16.84999999999999787, 1.533819458162526451E-15, 0.000000000000000000 ) ) ;
#31467=ADVANCED_FACE ( 'NONE', ( #11332 ), #49746, .T. ) ;
#31479=EDGE_CURVE ( 'NONE', #36519, #28856, #29110, .T. ) ;
#31495=EDGE_LOOP ( 'NONE', ( #101335, #33855, #99181, #15705, #21613, #16636 ) ) ;
#31498=CARTESIAN_POINT ( 'NONE',  ( 22.61650669486618526, 1.474610560812782335E-15, 0.000000000000000000 ) ) ;
#31511=CARTESIAN_POINT ( 'NONE',  ( 29.83349330513380693, 1.593028355512270962E-15, 0.000000000000000000 ) ) ;
#31517=DIRECTION ( 'NONE',  ( 0.000000000000000000, -1.224646799147353700E-16, 1.000000000000000000 ) ) ;
#31524=VECTOR ( 'NONE', #11752, 1000.000000000000227 ) ;
#31574=EDGE_LOOP ( 'NONE', ( #90495, #73478, #76843, #71080, #48950 ) ) ;
#31582=CARTESIAN_POINT ( 'NONE',  ( 33.58349330513380693, -4.000000000000000888, 4.898587196589416773E-16 ) ) ;
#31630=AXIS2_PLACEMENT_3D ( 'NONE', #105074, #64099, #31213 ) ;
#31652=DIRECTION ( 'NONE',  ( -1.000000000000000000, -0.000000000000000000, -0.000000000000000000 ) ) ;
#31654=ORIENTED_EDGE ( 'NONE', *, *, #26263, .T. ) ;
#31661=EDGE_CURVE ( 'NONE', #88306, #8828, #18844, .T. ) ;
#31681=CARTESIAN_POINT ( 'NONE',  ( 5.974109059516062636, -2.735160444458186735, -6.500000000000002665 ) ) ;
#31683=CARTESIAN_POINT ( 'NONE',  ( 6.281175601187038993, 3.752776749732559480, -6.500000000000007105 ) ) ;
#31693=DIRECTION ( 'NONE',  ( 0.000000000000000000, -1.000000000000000000, 0.000000000000000000 ) ) ;
#31739=DIRECTION ( 'NONE',  ( 0.000000000000000000, -1.000000000000000000, 0.000000000000000000 ) ) ;
#31753=DIRECTION ( 'NONE',  ( -1.000000000000000000, -0.000000000000000000, -0.000000000000000000 ) ) ;
#31804=LINE ( 'NONE', #41469, #25844 ) ;
#31812=AXIS2_PLACEMENT_3D ( 'NONE', #6183, #5665, #71452 ) ;
#31835=ADVANCED_FACE ( 'NONE', ( #38075 ), #12679, .T. ) ;
#31883=FACE_OUTER_BOUND ( 'NONE', #87286, .T. ) ;
#31887=CIRCLE ( 'NONE', #2531, 3.309500000000001663 ) ;
#31902=ORIENTED_EDGE ( 'NONE', *, *, #64902, .T. ) ;
#31915=CARTESIAN_POINT ( 'NONE',  ( 6.683837171061802529, 3.955946848495962787, 6.851900933636986935 ) ) ;
#31965=CYLINDRICAL_SURFACE ( 'NONE', #35787, 4.000000000000000888 ) ;
#31971=CARTESIAN_POINT ( 'NONE',  ( 19.83349330513380693, 4.000000000000002665, 0.000000000000000000 ) ) ;
#31972=CARTESIAN_POINT ( 'NONE',  ( 6.326195795702099112, 1.326139502404654280, 6.831522767506993610 ) ) ;
#31978=FACE_OUTER_BOUND ( 'NONE', #38989, .T. ) ;
#31998=LINE ( 'NONE', #89690, #68432 ) ;
#32028=DIRECTION ( 'NONE',  ( -1.000000000000000000, -1.224606353822377258E-16, -0.000000000000000000 ) ) ;
#32032=CARTESIAN_POINT ( 'NONE',  ( 29.83349330513380693, 4.898587196589411843E-16, -4.000000000000001776 ) ) ;
#32067=LINE ( 'NONE', #6160, #30819 ) ;
#32101=CONICAL_SURFACE ( 'NONE', #21801, 3.309500000000001663, 0.9599310885968770357 ) ;
#32104=DIRECTION ( 'NONE',  ( 0.000000000000000000, -1.000000000000000000, 0.000000000000000000 ) ) ;
#32116=CARTESIAN_POINT ( 'NONE',  ( 23.86650669486618881, 1.474610560812782335E-15, 0.000000000000000000 ) ) ;
#32121=CARTESIAN_POINT ( 'NONE',  ( 22.33349330513380693, 1.593028355512270962E-15, 0.000000000000000000 ) ) ;
#32125=AXIS2_PLACEMENT_3D ( 'NONE', #92581, #10592, #43510 ) ;
#32140=AXIS2_PLACEMENT_3D ( 'NONE', #50269, #42176, #84241 ) ;
#32147=CARTESIAN_POINT ( 'NONE',  ( 18.58349330513380693, -3.851859888774471706E-31, 4.000000000000001776 ) ) ;
#32173=ORIENTED_EDGE ( 'NONE', *, *, #70152, .T. ) ;
#32188=AXIS2_PLACEMENT_3D ( 'NONE', #24089, #48839, #16492 ) ;
#32213=CARTESIAN_POINT ( 'NONE',  ( 28.09999999999999787, 1.533819458162526451E-15, 0.000000000000000000 ) ) ;
#32236=ORIENTED_EDGE ( 'NONE', *, *, #62548, .F. ) ;
#32285=AXIS2_PLACEMENT_3D ( 'NONE', #53522, #12511, #82016 ) ;
#32291=DIRECTION ( 'NONE',  ( -1.000000000000000000, -1.224606353822377258E-16, -0.000000000000000000 ) ) ;
#32293=DIRECTION ( 'NONE',  ( 0.5735764363510491570, -0.8191520442889895781, 1.003171929053522035E-16 ) ) ;
#32299=CARTESIAN_POINT ( 'NONE',  ( 14.83349330513380693, 4.000000000000002665, 0.000000000000000000 ) ) ;
#32304=DIRECTION ( 'NONE',  ( -1.000000000000000000, -1.224606353822377258E-16, -0.000000000000000000 ) ) ;
#32330=EDGE_CURVE ( 'NONE', #63739, #94695, #86042, .T. ) ;
#32347=DIRECTION ( 'NONE',  ( 1.000000000000000000, 1.224606353822377258E-16, 0.000000000000000000 ) ) ;
#32349=DIRECTION ( 'NONE',  ( 0.000000000000000000, -1.000000000000000000, 0.000000000000000000 ) ) ;
#32377=VERTEX_POINT ( 'NONE', #1124 ) ;
#32411=DIRECTION ( 'NONE',  ( 0.000000000000000000, -1.000000000000000000, 0.000000000000000000 ) ) ;
#32432=CARTESIAN_POINT ( 'NONE',  ( 0.000000000000000000, 4.898587196589413815E-16, -4.000000000000000888 ) ) ;
#32441=DIRECTION ( 'NONE',  ( -1.000000000000000000, -0.000000000000000000, -0.000000000000000000 ) ) ;
#32495=DIRECTION ( 'NONE',  ( 0.000000000000000000, -1.000000000000000000, 0.000000000000000000 ) ) ;
#32509=ORIENTED_EDGE ( 'NONE', *, *, #52348, .T. ) ;
#32514=CARTESIAN_POINT ( 'NONE',  ( 6.098403338275567798, 3.412123303362088578, 6.499999999999997335 ) ) ;
#32543=VERTEX_POINT ( 'NONE', #89516 ) ;
#32575=LINE ( 'NONE', #81598, #47897 ) ;
#32600=ORIENTED_EDGE ( 'NONE', *, *, #87728, .T. ) ;
#32616=VERTEX_POINT ( 'NONE', #30775 ) ;
#32618=CYLINDRICAL_SURFACE ( 'NONE', #35907, 4.000000000000000888 ) ;
#32652=ORIENTED_EDGE ( 'NONE', *, *, #14637, .F. ) ;
#32662=AXIS2_PLACEMENT_3D ( 'NONE', #37617, #70480, #103375 ) ;
#32672=CONICAL_SURFACE ( 'NONE', #42959, 3.309500000000001663, 0.9599310885968770357 ) ;
#32680=AXIS2_PLACEMENT_3D ( 'NONE', #70396, #11601, #52596 ) ;
#32702=LINE ( 'NONE', #65571, #70777 ) ;
#32785=ORIENTED_EDGE ( 'NONE', *, *, #63900, .T. ) ;
#32818=FACE_OUTER_BOUND ( 'NONE', #98939, .T. ) ;
#32824=DIRECTION ( 'NONE',  ( -0.5735764363510497121, 0.8191520442889892450, 1.003171929053521665E-16 ) ) ;
#32836=CARTESIAN_POINT ( 'NONE',  ( 6.585468679846623985, -3.617797563910821079, -6.733790807807558565 ) ) ;
#32845=AXIS2_PLACEMENT_3D ( 'NONE', #21428, #22499, #37093 ) ;
#32900=ORIENTED_EDGE ( 'NONE', *, *, #48232, .T. ) ;
#32971=CYLINDRICAL_SURFACE ( 'NONE', #99650, 4.000000000000000888 ) ;
#32987=AXIS2_PLACEMENT_3D ( 'NONE', #29631, #85176, #36667 ) ;
#32990=ORIENTED_EDGE ( 'NONE', *, *, #79121, .T. ) ;
#32998=DIRECTION ( 'NONE',  ( 0.000000000000000000, -1.000000000000000000, 0.000000000000000000 ) ) ;
#33000=CARTESIAN_POINT ( 'NONE',  ( 20.11650669486618881, 4.000000000000003553, 4.898587196589414801E-16 ) ) ;
#33036=FACE_OUTER_BOUND ( 'NONE', #17566, .T. ) ;
#33075=CIRCLE ( 'NONE', #2074, 4.000000000000000888 ) ;
#33085=EDGE_LOOP ( 'NONE', ( #41102, #92789, #95085, #91083, #54866 ) ) ;
#33150=DIRECTION ( 'NONE',  ( 0.000000000000000000, 0.000000000000000000, 1.000000000000000000 ) ) ;
#33173=AXIS2_PLACEMENT_3D ( 'NONE', #18349, #68483, #84123 ) ;
#33176=DIRECTION ( 'NONE',  ( 0.000000000000000000, 0.000000000000000000, -1.000000000000000000 ) ) ;
#33192=CARTESIAN_POINT ( 'NONE',  ( 9.349999999999997868, 1.533819458162526451E-15, 0.000000000000000000 ) ) ;
#33256=CARTESIAN_POINT ( 'NONE',  ( 10.11650669486618881, 1.474610560812782335E-15, 0.000000000000000000 ) ) ;
#33286=CIRCLE ( 'NONE', #93565, 4.000000000000001776 ) ;
#33288=CARTESIAN_POINT ( 'NONE',  ( 6.289572920342625828, 5.584521518880460889, 3.985288806461539046 ) ) ;
#33302=DIRECTION ( 'NONE',  ( 0.000000000000000000, -1.000000000000000000, 0.000000000000000000 ) ) ;
#33323=DIRECTION ( 'NONE',  ( 0.000000000000000000, 0.000000000000000000, -1.000000000000000000 ) ) ;
#33364=AXIS2_PLACEMENT_3D ( 'NONE', #28491, #11722, #45195 ) ;
#33386=ORIENTED_EDGE ( 'NONE', *, *, #41183, .F. ) ;
#33396=CARTESIAN_POINT ( 'NONE',  ( 8.099999999999999645, -7.505553499465142053, -3.129864801432410934E-16 ) ) ;
#33416=CARTESIAN_POINT ( 'NONE',  ( 28.86650669486618881, 0.000000000000000000, 4.000000000000000888 ) ) ;
#33471=EDGE_CURVE ( 'NONE', #77629, #55271, #87640, .T. ) ;
#33508=ORIENTED_EDGE ( 'NONE', *, *, #62548, .T. ) ;
#33521=CARTESIAN_POINT ( 'NONE',  ( 13.58349330513380515, 1.593028355512270962E-15, 0.000000000000000000 ) ) ;
#33551=CARTESIAN_POINT ( 'NONE',  ( 25.11650669486618881, 1.474610560812782335E-15, 0.000000000000000000 ) ) ;
#33557=ORIENTED_EDGE ( 'NONE', *, *, #24415, .T. ) ;
#33566=CARTESIAN_POINT ( 'NONE',  ( 32.61650669486618881, 1.474610560812782335E-15, 0.000000000000000000 ) ) ;
#33587=CONICAL_SURFACE ( 'NONE', #88697, 4.000000000000001776, 0.9599310885968774798 ) ;
#33602=CARTESIAN_POINT ( 'NONE',  ( 13.58349330513380515, 4.898587196589411843E-16, -4.000000000000001776 ) ) ;
#33623=ORIENTED_EDGE ( 'NONE', *, *, #16598, .T. ) ;
#33659=DIRECTION ( 'NONE',  ( 0.000000000000000000, -1.000000000000000000, 0.000000000000000000 ) ) ;
#33661=CONICAL_SURFACE ( 'NONE', #47404, 4.000000000000001776, 0.9599310885968774798 ) ;
#33679=CARTESIAN_POINT ( 'NONE',  ( 6.394337469123802187, 3.776351736504755863, -6.540833074877207665 ) ) ;
#33770=ORIENTED_EDGE ( 'NONE', *, *, #15801, .T. ) ;
#33776=DIRECTION ( 'NONE',  ( -1.000000000000000000, -0.000000000000000000, -0.000000000000000000 ) ) ;
#33800=CARTESIAN_POINT ( 'NONE',  ( 0.000000000000000000, 0.000000000000000000, 4.000000000000000888 ) ) ;
#33801=ADVANCED_FACE ( 'NONE', ( #10922 ), #86037, .T. ) ;
#33820=ORIENTED_EDGE ( 'NONE', *, *, #65918, .F. ) ;
#33836=CIRCLE ( 'NONE', #69987, 4.000000000000000888 ) ;
#33849=CARTESIAN_POINT ( 'NONE',  ( 19.83349330513380693, 1.593028355512270962E-15, 0.000000000000000000 ) ) ;
#33855=ORIENTED_EDGE ( 'NONE', *, *, #7689, .T. ) ;
#33860=CIRCLE ( 'NONE', #94109, 4.000000000000000888 ) ;
#33861=CARTESIAN_POINT ( 'NONE',  ( -2.896852679609707160E-16, -5.309483803148803638, -3.803704290982251379 ) ) ;
#33865=ADVANCED_FACE ( 'NONE', ( #8815 ), #73985, .T. ) ;
#33911=AXIS2_PLACEMENT_3D ( 'NONE', #104312, #55223, #70897 ) ;
#33918=ORIENTED_EDGE ( 'NONE', *, *, #46194, .T. ) ;
#33936=EDGE_CURVE ( 'NONE', #35336, #8054, #73905, .T. ) ;
#33939=EDGE_LOOP ( 'NONE', ( #52474, #35243, #41141, #60683, #80113 ) ) ;
#33946=CARTESIAN_POINT ( 'NONE',  ( 11.84999999999999787, 3.309500000000003439, 4.052968581778167743E-16 ) ) ;
#33972=CIRCLE ( 'NONE', #94235, 4.000000000000000888 ) ;
#33977=ORIENTED_EDGE ( 'NONE', *, *, #67044, .T. ) ;
#33984=AXIS2_PLACEMENT_3D ( 'NONE', #5112, #11586, #44513 ) ;
#33992=AXIS2_PLACEMENT_3D ( 'NONE', #22771, #23839, #15172 ) ;
#34010=DIRECTION ( 'NONE',  ( -1.000000000000000000, -0.000000000000000000, -0.000000000000000000 ) ) ;
#34019=EDGE_CURVE ( 'NONE', #45187, #42880, #7440, .T. ) ;
#34025=CIRCLE ( 'NONE', #35799, 3.309500000000001663 ) ;
#34062=CIRCLE ( 'NONE', #94334, 3.309500000000001663 ) ;
#34079=AXIS2_PLACEMENT_3D ( 'NONE', #92980, #1823, #34783 ) ;
#34080=ORIENTED_EDGE ( 'NONE', *, *, #67181, .T. ) ;
#34083=ORIENTED_EDGE ( 'NONE', *, *, #90865, .F. ) ;
#34095=FACE_OUTER_BOUND ( 'NONE', #31495, .T. ) ;
#34105=B_SPLINE_CURVE_WITH_KNOTS ( 'NONE', 3,
 ( #77750, #2779, #28169, #54497, #3323 ),
 .UNSPECIFIED., .F., .F.,
 ( 4, 1, 4 ),
 ( 0.000000000000000000, 0.003752776749732570066, 0.007505553499465140131 ),
 .UNSPECIFIED. ) ;
#34114=CARTESIAN_POINT ( 'NONE',  ( 0.000000000000000000, 0.000000000000000000, 0.000000000000000000 ) ) ;
#34118=CARTESIAN_POINT ( 'NONE',  ( 6.222582369487715148, -4.088457415080688051, 6.499999999999999112 ) ) ;
#34124=CARTESIAN_POINT ( 'NONE',  ( 22.61650669486618526, 0.000000000000000000, 4.000000000000000888 ) ) ;
#34126=EDGE_CURVE ( 'NONE', #826, #86797, #5183, .T. ) ;
#34132=DIRECTION ( 'NONE',  ( 0.5735764363510491570, -0.8191520442889895781, 1.003171929053522035E-16 ) ) ;
#34180=CARTESIAN_POINT ( 'NONE',  ( 0.000000000000000000, 0.000000000000000000, 0.000000000000000000 ) ) ;
#34193=CIRCLE ( 'NONE', #47920, 4.000000000000001776 ) ;
#34194=VECTOR ( 'NONE', #58581, 1000.000000000000000 ) ;
#34197=EDGE_CURVE ( 'NONE', #16689, #90625, #94741, .T. ) ;
#34219=CARTESIAN_POINT ( 'NONE',  ( 36.08349330513379982, 1.593028355512270962E-15, 0.000000000000000000 ) ) ;
#34233=CARTESIAN_POINT ( 'NONE',  ( 0.5805565836007664515, -7.505553499465142053, -1.357586595304856736E-16 ) ) ;
#34253=CYLINDRICAL_SURFACE ( 'NONE', #64895, 4.000000000000000888 ) ;
#34324=DIRECTION ( 'NONE',  ( 0.000000000000000000, -1.000000000000000000, 0.000000000000000000 ) ) ;
#34376=ORIENTED_EDGE ( 'NONE', *, *, #29187, .F. ) ;
#34409=VERTEX_POINT ( 'NONE', #88791 ) ;
#34420=VECTOR ( 'NONE', #35275, 1000.000000000000000 ) ;
#34441=CARTESIAN_POINT ( 'NONE',  ( 9.833493305133805151, -3.851859888774471706E-31, 4.000000000000001776 ) ) ;
#34485=CIRCLE ( 'NONE', #5116, 4.000000000000000888 ) ;
#34494=DIRECTION ( 'NONE',  ( -0.5735764363510494901, -0.8191520442889894671, 0.000000000000000000 ) ) ;
#34547=CIRCLE ( 'NONE', #1764, 3.309500000000001663 ) ;
#34563=CARTESIAN_POINT ( 'NONE',  ( 11.84999999999999787, 3.309500000000003439, 0.000000000000000000 ) ) ;
#34573=CARTESIAN_POINT ( 'NONE',  ( 16.08349330513380337, 1.593028355512270962E-15, 0.000000000000000000 ) ) ;
#34581=CARTESIAN_POINT ( 'NONE',  ( 11.08349330513380515, 1.593028355512270962E-15, 0.000000000000000000 ) ) ;
#34600=CARTESIAN_POINT ( 'NONE',  ( 0.1061556211655340504, 6.421950209808279020, 1.876855952934452620 ) ) ;
#34622=EDGE_LOOP ( 'NONE', ( #7676, #67767, #37578 ) ) ;
#34667=AXIS2_PLACEMENT_3D ( 'NONE', #37218, #51763, #35629 ) ;
#34688=DIRECTION ( 'NONE',  ( -0.5735764363510494901, -0.8191520442889894671, 0.000000000000000000 ) ) ;
#34712=LINE ( 'NONE', #7729, #4533 ) ;
#34730=CIRCLE ( 'NONE', #96684, 4.000000000000001776 ) ;
#34731=DIRECTION ( 'NONE',  ( 0.000000000000000000, 1.000000000000000000, 0.000000000000000000 ) ) ;
#34761=ORIENTED_EDGE ( 'NONE', *, *, #15713, .T. ) ;
#34769=CARTESIAN_POINT ( 'NONE',  ( 0.000000000000000000, -5.629165124598847214, 3.250000000000005329 ) ) ;
#34783=DIRECTION ( 'NONE',  ( 0.000000000000000000, -1.000000000000000000, 0.000000000000000000 ) ) ;
#34791=DIRECTION ( 'NONE',  ( -1.000000000000000000, -1.224606353822377258E-16, -0.000000000000000000 ) ) ;
#34799=ORIENTED_EDGE ( 'NONE', *, *, #59305, .T. ) ;
#34803=DIRECTION ( 'NONE',  ( 0.000000000000000000, -1.000000000000000000, 0.000000000000000000 ) ) ;
#34806=ORIENTED_EDGE ( 'NONE', *, *, #49904, .T. ) ;
#34811=EDGE_CURVE ( 'NONE', #90141, #89211, #13697, .T. ) ;
#34815=LINE ( 'NONE', #59062, #7558 ) ;
#34818=CYLINDRICAL_SURFACE ( 'NONE', #4823, 4.000000000000000888 ) ;
#34828=DIRECTION ( 'NONE',  ( -1.000000000000000000, -1.224606353822377258E-16, -0.000000000000000000 ) ) ;
#34878=ADVANCED_FACE ( 'NONE', ( #74849 ), #2031, .T. ) ;
#34882=CARTESIAN_POINT ( 'NONE',  ( 31.84999999999999787, 1.533819458162526451E-15, 0.000000000000000000 ) ) ;
#34896=CARTESIAN_POINT ( 'NONE',  ( 36.08349330513379982, 4.000000000000002665, 0.000000000000000000 ) ) ;
#34929=AXIS2_PLACEMENT_3D ( 'NONE', #40348, #80800, #30158 ) ;
#34952=DIRECTION ( 'NONE',  ( -1.000000000000000000, -1.224606353822377258E-16, -0.000000000000000000 ) ) ;
#34989=AXIS2_PLACEMENT_3D ( 'NONE', #6435, #8032, #32349 ) ;
#35026=DIRECTION ( 'NONE',  ( -1.000000000000000000, -0.000000000000000000, -0.000000000000000000 ) ) ;
#35065=VECTOR ( 'NONE', #45296, 1000.000000000000341 ) ;
#35142=EDGE_LOOP ( 'NONE', ( #26431, #28192, #39181, #55380, #72343 ) ) ;
#35161=CARTESIAN_POINT ( 'NONE',  ( 5.691929483231186637, 5.629165124598853431, 3.249999999999998668 ) ) ;
#35173=DIRECTION ( 'NONE',  ( 0.000000000000000000, -1.000000000000000000, 0.000000000000000000 ) ) ;
#35198=ORIENTED_EDGE ( 'NONE', *, *, #59486, .F. ) ;
#35200=CARTESIAN_POINT ( 'NONE',  ( 0.000000000000000000, 4.898587196589413815E-16, -4.000000000000000888 ) ) ;
#35207=VERTEX_POINT ( 'NONE', #94117 ) ;
#35243=ORIENTED_EDGE ( 'NONE', *, *, #13178, .T. ) ;
#35269=ORIENTED_EDGE ( 'NONE', *, *, #20313, .F. ) ;
#35275=DIRECTION ( 'NONE',  ( -0.5735764363510494901, -0.8191520442889894671, 0.000000000000000000 ) ) ;
#35283=AXIS2_PLACEMENT_3D ( 'NONE', #105057, #31198, #4765 ) ;
#35292=EDGE_LOOP ( 'NONE', ( #22979, #99239, #92151, #52488, #21581 ) ) ;
#35298=DIRECTION ( 'NONE',  ( -1.000000000000000000, -0.000000000000000000, -0.000000000000000000 ) ) ;
#35306=CIRCLE ( 'NONE', #14530, 4.000000000000001776 ) ;
#35336=VERTEX_POINT ( 'NONE', #39612 ) ;
#35358=DIRECTION ( 'NONE',  ( -1.000000000000000000, -1.224606353822377258E-16, -0.000000000000000000 ) ) ;
#35409=ORIENTED_EDGE ( 'NONE', *, *, #12626, .F. ) ;
#35416=EDGE_LOOP ( 'NONE', ( #64437, #44898, #106047, #100532, #21382 ) ) ;
#35453=ORIENTED_EDGE ( 'NONE', *, *, #79459, .T. ) ;
#35463=VECTOR ( 'NONE', #76121, 1000.000000000000227 ) ;
#35480=LINE ( 'NONE', #900, #86371 ) ;
#35486=CARTESIAN_POINT ( 'NONE',  ( 31.08349330513380693, 1.593028355512270962E-15, 0.000000000000000000 ) ) ;
#35491=DIRECTION ( 'NONE',  ( -1.000000000000000000, -1.224606353822377258E-16, -0.000000000000000000 ) ) ;
#35523=FACE_OUTER_BOUND ( 'NONE', #81285, .T. ) ;
#35565=DIRECTION ( 'NONE',  ( 0.000000000000000000, -1.000000000000000000, 0.000000000000000000 ) ) ;
#35604=ORIENTED_EDGE ( 'NONE', *, *, #41266, .T. ) ;
#35606=DIRECTION ( 'NONE',  ( -1.000000000000000000, -1.224606353822377258E-16, -0.000000000000000000 ) ) ;
#35607=FACE_OUTER_BOUND ( 'NONE', #21574, .T. ) ;
#35619=DIRECTION ( 'NONE',  ( -0.5735764363510497121, 0.8191520442889892450, 1.003171929053521665E-16 ) ) ;
#35629=DIRECTION ( 'NONE',  ( 0.000000000000000000, -1.000000000000000000, 0.000000000000000000 ) ) ;
#35633=CIRCLE ( 'NONE', #78689, 4.000000000000001776 ) ;
#35642=ORIENTED_EDGE ( 'NONE', *, *, #53030, .F. ) ;
#35657=VERTEX_POINT ( 'NONE', #78325 ) ;
#35672=DIRECTION ( 'NONE',  ( 1.000000000000000000, 1.224606353822377258E-16, 0.000000000000000000 ) ) ;
#35681=CONICAL_SURFACE ( 'NONE', #64897, 3.309500000000001663, 0.9599310885968770357 ) ;
#35708=VERTEX_POINT ( 'NONE', #71822 ) ;
#35732=VECTOR ( 'NONE', #42525, 1000.000000000000000 ) ;
#35740=CIRCLE ( 'NONE', #1243, 4.000000000000000888 ) ;
#35771=EDGE_CURVE ( 'NONE', #48969, #62332, #69838, .T. ) ;
#35787=AXIS2_PLACEMENT_3D ( 'NONE', #99862, #90719, #26035 ) ;
#35799=AXIS2_PLACEMENT_3D ( 'NONE', #34882, #60741, #67750 ) ;
#35801=ADVANCED_FACE ( 'NONE', ( #89084 ), #25123, .T. ) ;
#35811=DIRECTION ( 'NONE',  ( 1.000000000000000000, 0.000000000000000000, -0.000000000000000000 ) ) ;
#35815=ORIENTED_EDGE ( 'NONE', *, *, #43391, .F. ) ;
#35829=AXIS2_PLACEMENT_3D ( 'NONE', #92249, #76074, #18403 ) ;
#35860=CARTESIAN_POINT ( 'NONE',  ( 11.08349330513380515, -4.000000000000000000, 4.898587196589415787E-16 ) ) ;
#35880=ORIENTED_EDGE ( 'NONE', *, *, #39193, .T. ) ;
#35894=CARTESIAN_POINT ( 'NONE',  ( 34.35000000000000142, 1.533819458162526451E-15, 0.000000000000000000 ) ) ;
#35904=EDGE_CURVE ( 'NONE', #11120, #30663, #19989, .T. ) ;
#35907=AXIS2_PLACEMENT_3D ( 'NONE', #82185, #63915, #8303 ) ;
#35921=EDGE_LOOP ( 'NONE', ( #33557, #65333, #82625, #29178 ) ) ;
#35930=LINE ( 'NONE', #53136, #64985 ) ;
#35932=DIRECTION ( 'NONE',  ( -1.000000000000000000, -1.224606353822377258E-16, -0.000000000000000000 ) ) ;
#35955=DIRECTION ( 'NONE',  ( 0.000000000000000000, 0.000000000000000000, 1.000000000000000000 ) ) ;
#35957=ADVANCED_FACE ( 'NONE', ( #65334 ), #78448, .T. ) ;
#35986=ORIENTED_EDGE ( 'NONE', *, *, #83081, .F. ) ;
#35987=ORIENTED_EDGE ( 'NONE', *, *, #59664, .T. ) ;
#36056=CARTESIAN_POINT ( 'NONE',  ( 15.59999999999999787, 3.309500000000003439, 0.000000000000000000 ) ) ;
#36085=CARTESIAN_POINT ( 'NONE',  ( 23.58349330513380337, -4.000000000000000888, 4.898587196589416773E-16 ) ) ;
#36136=DIRECTION ( 'NONE',  ( 0.000000000000000000, 1.000000000000000000, 0.000000000000000000 ) ) ;
#36159=CIRCLE ( 'NONE', #15466, 4.000000000000000888 ) ;
#36187=LINE ( 'NONE', #44782, #69014 ) ;
#36198=VERTEX_POINT ( 'NONE', #71041 ) ;
#36200=VERTEX_POINT ( 'NONE', #43709 ) ;
#36207=CARTESIAN_POINT ( 'NONE',  ( 20.59999999999999787, 1.533819458162526451E-15, 0.000000000000000000 ) ) ;
#36248=CARTESIAN_POINT ( 'NONE',  ( 33.86650669486618881, 1.474610560812782335E-15, 0.000000000000000000 ) ) ;
#36254=CARTESIAN_POINT ( 'NONE',  ( 36.84999999999999432, 1.533819458162526451E-15, 0.000000000000000000 ) ) ;
#36277=ORIENTED_EDGE ( 'NONE', *, *, #95299, .F. ) ;
#36301=CONICAL_SURFACE ( 'NONE', #13825, 3.309500000000001663, 0.9599310885968770357 ) ;
#36307=ORIENTED_EDGE ( 'NONE', *, *, #95299, .T. ) ;
#36368=ORIENTED_EDGE ( 'NONE', *, *, #98815, .T. ) ;
#36374=VERTEX_POINT ( 'NONE', #15992 ) ;
#36383=CARTESIAN_POINT ( 'NONE',  ( 36.36650669486618881, 1.474610560812782335E-15, 0.000000000000000000 ) ) ;
#36385=VERTEX_POINT ( 'NONE', #55372 ) ;
#36394=ORIENTED_EDGE ( 'NONE', *, *, #14307, .F. ) ;
#36400=CARTESIAN_POINT ( 'NONE',  ( 6.575925811255157072, 7.701774614579012912, 6.632038761762336177E-16 ) ) ;
#36441=VERTEX_POINT ( 'NONE', #8951 ) ;
#36456=DIRECTION ( 'NONE',  ( 0.5735764363510490460, 0.8191520442889896891, 0.000000000000000000 ) ) ;
#36464=DIRECTION ( 'NONE',  ( 0.000000000000000000, -0.4999999999999999445, 0.8660254037844385966 ) ) ;
#36470=DIRECTION ( 'NONE',  ( -1.000000000000000000, -1.224606353822377258E-16, -0.000000000000000000 ) ) ;
#36477=DIRECTION ( 'NONE',  ( 0.000000000000000000, -1.000000000000000000, 0.000000000000000000 ) ) ;
#36518=CONICAL_SURFACE ( 'NONE', #88139, 4.000000000000001776, 0.9599310885968774798 ) ;
#36519=VERTEX_POINT ( 'NONE', #78998 ) ;
#36521=CYLINDRICAL_SURFACE ( 'NONE', #29744, 4.000000000000000888 ) ;
#36540=CARTESIAN_POINT ( 'NONE',  ( 23.86650669486618881, -3.999999999999998224, 0.000000000000000000 ) ) ;
#36543=B_SPLINE_CURVE_WITH_KNOTS ( 'NONE', 3,
 ( #3569, #78502, #45104, #94722, #37028, #4636, #37565, #101723 ),
 .UNSPECIFIED., .F., .F.,
 ( 4, 2, 2, 4 ),
 ( 0.003797433802554438936, 0.004743183970586236156, 0.005688934138618033376, 0.007580434474681626948 ),
 .UNSPECIFIED. ) ;
#36560=CARTESIAN_POINT ( 'NONE',  ( 5.691929483231184861, -4.336808689942017736E-16, 6.500000000000001776 ) ) ;
#36566=VECTOR ( 'NONE', #16405, 1000.000000000000000 ) ;
#36587=CARTESIAN_POINT ( 'NONE',  ( 27.61650669486618881, 1.474610560812782335E-15, 0.000000000000000000 ) ) ;
#36617=CARTESIAN_POINT ( 'NONE',  ( 23.09999999999999432, -3.309499999999999886, 4.475777889183790779E-16 ) ) ;
#36619=ORIENTED_EDGE ( 'NONE', *, *, #92466, .T. ) ;
#36637=ORIENTED_EDGE ( 'NONE', *, *, #52739, .T. ) ;
#36645=EDGE_CURVE ( 'NONE', #48387, #25099, #14792, .T. ) ;
#36663=ORIENTED_EDGE ( 'NONE', *, *, #91155, .F. ) ;
#36667=DIRECTION ( 'NONE',  ( 0.000000000000000000, -1.000000000000000000, 0.000000000000000000 ) ) ;
#36682=CARTESIAN_POINT ( 'NONE',  ( 5.691929483231186637, -3.469446951953614189E-15, -6.500000000000000000 ) ) ;
#36698=CARTESIAN_POINT ( 'NONE',  ( 6.289692432696767810, 6.589071317540670769, -2.245373559998994573 ) ) ;
#36699=CIRCLE ( 'NONE', #34989, 4.000000000000000888 ) ;
#36716=EDGE_CURVE ( 'NONE', #36385, #104544, #37219, .T. ) ;
#36728=CARTESIAN_POINT ( 'NONE',  ( 15.59999999999999787, 1.533819458162526451E-15, 0.000000000000000000 ) ) ;
#36731=ORIENTED_EDGE ( 'NONE', *, *, #27716, .T. ) ;
#36738=COLOUR_RGB ( '', 0.08235294, 0.09019608, 0.10196078) ;
#36765=ADVANCED_FACE ( 'NONE', ( #93994 ), #53005, .T. ) ;
#36771=CARTESIAN_POINT ( 'NONE',  ( 26.36650669486618881, 4.000000000000003553, 4.898587196589414801E-16 ) ) ;
#36790=CARTESIAN_POINT ( 'NONE',  ( 21.36650669486618881, 4.000000000000003553, 4.898587196589414801E-16 ) ) ;
#36792=DIRECTION ( 'NONE',  ( 0.000000000000000000, -1.000000000000000000, 0.000000000000000000 ) ) ;
#36819=CARTESIAN_POINT ( 'NONE',  ( 24.83349330513380693, 4.898587196589411843E-16, -4.000000000000001776 ) ) ;
#36836=ORIENTED_EDGE ( 'NONE', *, *, #33936, .T. ) ;
#36873=ORIENTED_EDGE ( 'NONE', *, *, #88622, .F. ) ;
#36875=EDGE_LOOP ( 'NONE', ( #48453, #92794, #87438, #64696, #33820 ) ) ;
#36882=AXIS2_PLACEMENT_3D ( 'NONE', #12209, #94755, #88240 ) ;
#36914=ORIENTED_EDGE ( 'NONE', *, *, #87532, .F. ) ;
#36916=LINE ( 'NONE', #87044, #522 ) ;
#36923=DIRECTION ( 'NONE',  ( 0.000000000000000000, 0.000000000000000000, 1.000000000000000000 ) ) ;
#36959=CIRCLE ( 'NONE', #102359, 4.000000000000000888 ) ;
#36979=CARTESIAN_POINT ( 'NONE',  ( 6.281178480976146616, 3.752776749732564809, 6.499999999999995559 ) ) ;
#36997=CIRCLE ( 'NONE', #12849, 4.000000000000000888 ) ;
#37028=CARTESIAN_POINT ( 'NONE',  ( 0.1061556211655369231, -6.421950209808287902, -1.876855952934449290 ) ) ;
#37031=DIRECTION ( 'NONE',  ( 0.000000000000000000, 1.000000000000000000, 0.000000000000000000 ) ) ;
#37039=EDGE_CURVE ( 'NONE', #68858, #78191, #21118, .T. ) ;
#37044=CARTESIAN_POINT ( 'NONE',  ( 29.83349330513380693, -4.000000000000000000, 4.898587196589415787E-16 ) ) ;
#37063=FACE_OUTER_BOUND ( 'NONE', #78837, .T. ) ;
#37082=ORIENTED_EDGE ( 'NONE', *, *, #24353, .F. ) ;
#37093=DIRECTION ( 'NONE',  ( 0.000000000000000000, -1.000000000000000000, 0.000000000000000000 ) ) ;
#37095=ADVANCED_FACE ( 'NONE', ( #73408 ), #11446, .T. ) ;
#37114=VERTEX_POINT ( 'NONE', #68549 ) ;
#37146=AXIS2_PLACEMENT_3D ( 'NONE', #102118, #52498, #54082 ) ;
#37198=ORIENTED_EDGE ( 'NONE', *, *, #103232, .T. ) ;
#37210=DIRECTION ( 'NONE',  ( 0.000000000000000000, -1.000000000000000000, 0.000000000000000000 ) ) ;
#37218=CARTESIAN_POINT ( 'NONE',  ( 22.61650669486618526, 1.474610560812782335E-15, 0.000000000000000000 ) ) ;
#37219=CIRCLE ( 'NONE', #97452, 4.000000000000000888 ) ;
#37239=CARTESIAN_POINT ( 'NONE',  ( 5.819846122303830249, 4.937269551422740044, 4.448398286273013369 ) ) ;
#37247=CYLINDRICAL_SURFACE ( 'NONE', #59911, 4.000000000000000888 ) ;
#37289=CARTESIAN_POINT ( 'NONE',  ( 33.58349330513380693, 1.593028355512270962E-15, 0.000000000000000000 ) ) ;
#37322=CIRCLE ( 'NONE', #68232, 4.000000000000000888 ) ;
#37323=CARTESIAN_POINT ( 'NONE',  ( 16.36650669486618881, 1.474610560812782335E-15, 0.000000000000000000 ) ) ;
#37325=CIRCLE ( 'NONE', #9693, 4.000000000000001776 ) ;
#37330=ORIENTED_EDGE ( 'NONE', *, *, #103409, .F. ) ;
#37346=DIRECTION ( 'NONE',  ( -1.000000000000000000, -1.224606353822377258E-16, -0.000000000000000000 ) ) ;
#37374=VECTOR ( 'NONE', #3861, 1000.000000000000341 ) ;
#37385=EDGE_CURVE ( 'NONE', #59167, #45575, #57106, .T. ) ;
#37419=CARTESIAN_POINT ( 'NONE',  ( 20.11650669486618881, -3.999999999999998224, 0.000000000000000000 ) ) ;
#37438=DIRECTION ( 'NONE',  ( -1.000000000000000000, -1.224606353822377258E-16, -0.000000000000000000 ) ) ;
#37467=ORIENTED_EDGE ( 'NONE', *, *, #4151, .F. ) ;
#37468=EDGE_CURVE ( 'NONE', #78006, #56185, #76485, .T. ) ;
#37475=( NAMED_UNIT ( * ) SI_UNIT ( $, .STERADIAN. ) SOLID_ANGLE_UNIT ( ) );
#37482=DIRECTION ( 'NONE',  ( 0.000000000000000000, 0.000000000000000000, 1.000000000000000000 ) ) ;
#37519=DIRECTION ( 'NONE',  ( -0.000000000000000000, 0.8660254037844387076, 0.5000000000000000000 ) ) ;
#37543=DIRECTION ( 'NONE',  ( -1.000000000000000000, -1.224606353822377258E-16, -0.000000000000000000 ) ) ;
#37565=CARTESIAN_POINT ( 'NONE',  ( 0.4037800551813762184, -7.199367570657610571, -0.5303295852573148839 ) ) ;
#37578=ORIENTED_EDGE ( 'NONE', *, *, #55874, .F. ) ;
#37611=VECTOR ( 'NONE', #102754, 1000.000000000000000 ) ;
#37617=CARTESIAN_POINT ( 'NONE',  ( 23.86650669486618881, 1.474610560812782335E-15, 0.000000000000000000 ) ) ;
#37626=DIRECTION ( 'NONE',  ( 0.000000000000000000, 1.000000000000000000, 0.000000000000000000 ) ) ;
#37647=ORIENTED_EDGE ( 'NONE', *, *, #60166, .F. ) ;
#37685=EDGE_LOOP ( 'NONE', ( #35880, #26888, #20901, #77031, #37647, #98021 ) ) ;
#37692=ORIENTED_EDGE ( 'NONE', *, *, #36716, .F. ) ;
#37703=EDGE_LOOP ( 'NONE', ( #92981, #2728, #22262, #105576, #40663 ) ) ;
#37712=VERTEX_POINT ( 'NONE', #39768 ) ;
#37763=ADVANCED_FACE ( 'NONE', ( #6844 ), #2915, .T. ) ;
#37773=DIRECTION ( 'NONE',  ( 1.000000000000000000, 0.000000000000000000, -0.000000000000000000 ) ) ;
#37819=CARTESIAN_POINT ( 'NONE',  ( 14.83349330513380693, -4.000000000000000000, 4.898587196589415787E-16 ) ) ;
#37844=EDGE_LOOP ( 'NONE', ( #95355, #29469, #17175, #52738, #37467 ) ) ;
#37845=EDGE_CURVE ( 'NONE', #48387, #90863, #30100, .T. ) ;
#37850=ORIENTED_EDGE ( 'NONE', *, *, #41725, .T. ) ;
#37883=CARTESIAN_POINT ( 'NONE',  ( 35.11650669486618170, 4.898587196589413815E-16, -4.000000000000000888 ) ) ;
#37905=DIRECTION ( 'NONE',  ( 0.000000000000000000, -1.000000000000000000, 0.000000000000000000 ) ) ;
#37959=CARTESIAN_POINT ( 'NONE',  ( 6.333820801330181993, -6.982605850970108108, 0.9057718968895951406 ) ) ;
#37960=CONICAL_SURFACE ( 'NONE', #74081, 3.309500000000001663, 0.9599310885968770357 ) ;
#37979=VERTEX_POINT ( 'NONE', #20182 ) ;
#38026=CARTESIAN_POINT ( 'NONE',  ( 14.34999999999999787, -3.309499999999999886, 0.000000000000000000 ) ) ;
#38048=DIRECTION ( 'NONE',  ( -1.000000000000000000, -1.224606353822377258E-16, -0.000000000000000000 ) ) ;
#38061=CARTESIAN_POINT ( 'NONE',  ( 10.59999999999999609, 3.309500000000003439, 0.000000000000000000 ) ) ;
#38071=DIRECTION ( 'NONE',  ( 0.000000000000000000, -1.000000000000000000, 0.000000000000000000 ) ) ;
#38075=FACE_OUTER_BOUND ( 'NONE', #81715, .T. ) ;
#38078=CARTESIAN_POINT ( 'NONE',  ( 8.099999999999999645, 0.000000000000000000, 0.000000000000000000 ) ) ;
#38086=ORIENTED_EDGE ( 'NONE', *, *, #12758, .F. ) ;
#38175=EDGE_CURVE ( 'NONE', #64739, #45575, #46050, .T. ) ;
#38203=CONICAL_SURFACE ( 'NONE', #5454, 3.309500000000001663, 0.9599310885968770357 ) ;
#38206=VERTEX_POINT ( 'NONE', #42142 ) ;
#38220=VERTEX_POINT ( 'NONE', #50748 ) ;
#38226=VERTEX_POINT ( 'NONE', #2742 ) ;
#38227=DIRECTION ( 'NONE',  ( -1.000000000000000000, -1.224606353822377258E-16, -0.000000000000000000 ) ) ;
#38246=ORIENTED_EDGE ( 'NONE', *, *, #56545, .F. ) ;
#38255=DIRECTION ( 'NONE',  ( -1.000000000000000000, -1.224606353822377258E-16, -0.000000000000000000 ) ) ;
#38261=ORIENTED_EDGE ( 'NONE', *, *, #92199, .F. ) ;
#38291=EDGE_CURVE ( 'NONE', #98079, #98690, #31249, .T. ) ;
#38292=CARTESIAN_POINT ( 'NONE',  ( 6.333820801329741457, 6.982605850968585770, 0.9057718968909901358 ) ) ;
#38318=AXIS2_PLACEMENT_3D ( 'NONE', #39256, #55913, #72132 ) ;
#38323=EDGE_LOOP ( 'NONE', ( #38444, #9808, #25734, #57591, #43930 ) ) ;
#38340=ADVANCED_BREP_SHAPE_REPRESENTATION ( '', ( #52984, #10728 ), #57385 ) ;
#38366=ORIENTED_EDGE ( 'NONE', *, *, #88197, .T. ) ;
#38379=ADVANCED_FACE ( 'NONE', ( #72018 ), #73653, .T. ) ;
#38401=ORIENTED_EDGE ( 'NONE', *, *, #43117, .F. ) ;
#38444=ORIENTED_EDGE ( 'NONE', *, *, #41000, .F. ) ;
#38457=VECTOR ( 'NONE', #91979, 1000.000000000000227 ) ;
#38470=CARTESIAN_POINT ( 'NONE',  ( 5.975663821521392194, -7.000939006314269797, 0.8740179403729263496 ) ) ;
#38471=EDGE_CURVE ( 'NONE', #42319, #98662, #85784, .T. ) ;
#38485=CIRCLE ( 'NONE', #74560, 4.000000000000000888 ) ;
#38489=ORIENTED_EDGE ( 'NONE', *, *, #19941, .T. ) ;
#38492=ORIENTED_EDGE ( 'NONE', *, *, #87129, .F. ) ;
#38513=ORIENTED_EDGE ( 'NONE', *, *, #10028, .T. ) ;
#38545=DIRECTION ( 'NONE',  ( -1.000000000000000000, -1.224606353822377258E-16, -0.000000000000000000 ) ) ;
#38553=VECTOR ( 'NONE', #42304, 1000.000000000000000 ) ;
#38561=CIRCLE ( 'NONE', #4055, 4.000000000000000888 ) ;
#38569=ORIENTED_EDGE ( 'NONE', *, *, #6251, .F. ) ;
#38592=DIRECTION ( 'NONE',  ( -1.000000000000000000, -1.224606353822377258E-16, -0.000000000000000000 ) ) ;
#38599=DIRECTION ( 'NONE',  ( -1.000000000000000000, -1.224606353822377258E-16, -0.000000000000000000 ) ) ;
#38629=FACE_OUTER_BOUND ( 'NONE', #8588, .T. ) ;
#38661=DIRECTION ( 'NONE',  ( 0.000000000000000000, -1.000000000000000000, 0.000000000000000000 ) ) ;
#38668=CIRCLE ( 'NONE', #90385, 3.309500000000001663 ) ;
#38790=AXIS2_PLACEMENT_3D ( 'NONE', #56384, #30570, #81718 ) ;
#38814=DIRECTION ( 'NONE',  ( 0.000000000000000000, 0.000000000000000000, 1.000000000000000000 ) ) ;
#38829=CARTESIAN_POINT ( 'NONE',  ( 0.000000000000000000, 0.000000000000000000, 4.000000000000000888 ) ) ;
#38862=ORIENTED_EDGE ( 'NONE', *, *, #87728, .F. ) ;
#38876=ORIENTED_EDGE ( 'NONE', *, *, #22492, .F. ) ;
#38885=CARTESIAN_POINT ( 'NONE',  ( 8.099999999999999645, 0.000000000000000000, 0.000000000000000000 ) ) ;
#38891=EDGE_CURVE ( 'NONE', #90401, #52034, #14319, .T. ) ;
#38942=ORIENTED_EDGE ( 'NONE', *, *, #14486, .T. ) ;
#38960=AXIS2_PLACEMENT_3D ( 'NONE', #4468, #79932, #104747 ) ;
#38981=CARTESIAN_POINT ( 'NONE',  ( 28.09999999999999787, 3.309500000000003439, 4.052968581778167743E-16 ) ) ;
#38989=EDGE_LOOP ( 'NONE', ( #48088, #46494, #33508, #92215, #56560, #103620 ) ) ;
#39006=VERTEX_POINT ( 'NONE', #29891 ) ;
#39022=DIRECTION ( 'NONE',  ( -1.000000000000000000, -1.224606353822377258E-16, -0.000000000000000000 ) ) ;
#39063=ORIENTED_EDGE ( 'NONE', *, *, #69650, .T. ) ;
#39087=DIRECTION ( 'NONE',  ( 0.000000000000000000, -1.000000000000000000, 0.000000000000000000 ) ) ;
#39088=CARTESIAN_POINT ( 'NONE',  ( 23.58349330513380337, 4.000000000000003553, 0.000000000000000000 ) ) ;
#39127=CARTESIAN_POINT ( 'NONE',  ( 8.099999999999999645, 3.752776749732565253, 6.499999999999997335 ) ) ;
#39144=ORIENTED_EDGE ( 'NONE', *, *, #85532, .F. ) ;
#39172=CARTESIAN_POINT ( 'NONE',  ( 17.61650669486618881, -3.999999999999998224, 0.000000000000000000 ) ) ;
#39181=ORIENTED_EDGE ( 'NONE', *, *, #17009, .T. ) ;
#39183=FACE_OUTER_BOUND ( 'NONE', #43169, .T. ) ;
#39193=EDGE_CURVE ( 'NONE', #8349, #59362, #68615, .T. ) ;
#39211=VERTEX_POINT ( 'NONE', #67550 ) ;
#39240=CARTESIAN_POINT ( 'NONE',  ( 6.222583235320747974, 4.088462131826499757, -6.500000000000000888 ) ) ;
#39256=CARTESIAN_POINT ( 'NONE',  ( 36.08349330513379982, 1.593028355512270962E-15, 0.000000000000000000 ) ) ;
#39369=EDGE_CURVE ( 'NONE', #59362, #62868, #96173, .T. ) ;
#39423=CARTESIAN_POINT ( 'NONE',  ( 0.000000000000000000, 1.502314598737160412E-15, 6.500000000000000888 ) ) ;
#39540=DIRECTION ( 'NONE',  ( 1.000000000000000000, 0.000000000000000000, 0.000000000000000000 ) ) ;
#39558=ORIENTED_EDGE ( 'NONE', *, *, #8740, .F. ) ;
#39612=CARTESIAN_POINT ( 'NONE',  ( 9.833493305133805151, 4.000000000000002665, 0.000000000000000000 ) ) ;
#39614=CARTESIAN_POINT ( 'NONE',  ( 0.000000000000000000, 0.000000000000000000, 0.000000000000000000 ) ) ;
#39627=AXIS2_PLACEMENT_3D ( 'NONE', #51822, #11350, #100903 ) ;
#39672=ORIENTED_EDGE ( 'NONE', *, *, #8120, .T. ) ;
#39685=DIRECTION ( 'NONE',  ( -1.000000000000000000, -0.000000000000000000, -0.000000000000000000 ) ) ;
#39695=CARTESIAN_POINT ( 'NONE',  ( 6.643884894376898664, -3.901062859469766497, -6.756839076127126198 ) ) ;
#39696=ORIENTED_EDGE ( 'NONE', *, *, #41690, .F. ) ;
#39716=VECTOR ( 'NONE', #65301, 1000.000000000000000 ) ;
#39737=CARTESIAN_POINT ( 'NONE',  ( 0.4042117618284704061, -3.141900367810047889, -6.500000000000002665 ) ) ;
#39750=VECTOR ( 'NONE', #17523, 1000.000000000000227 ) ;
#39768=CARTESIAN_POINT ( 'NONE',  ( 25.59999999999999787, 3.309500000000003439, 0.000000000000000000 ) ) ;
#39786=DIRECTION ( 'NONE',  ( 0.000000000000000000, -1.000000000000000000, 0.000000000000000000 ) ) ;
#39823=DIRECTION ( 'NONE',  ( 0.5735764363510490460, 0.8191520442889896891, 0.000000000000000000 ) ) ;
#39833=CIRCLE ( 'NONE', #17430, 4.000000000000000888 ) ;
#39843=EDGE_CURVE ( 'NONE', #59167, #16558, #18816, .T. ) ;
#39906=DIRECTION ( 'NONE',  ( 0.5735764363510490460, 0.8191520442889896891, 0.000000000000000000 ) ) ;
#39920=ORIENTED_EDGE ( 'NONE', *, *, #3338, .T. ) ;
#39943=DIRECTION ( 'NONE',  ( -1.000000000000000000, -0.000000000000000000, -0.000000000000000000 ) ) ;
#39964=DIRECTION ( 'NONE',  ( 0.000000000000000000, 1.000000000000000000, 0.000000000000000000 ) ) ;
#40007=DIRECTION ( 'NONE',  ( 1.000000000000000000, 1.224606353822377258E-16, 0.000000000000000000 ) ) ;
#40019=DIRECTION ( 'NONE',  ( 1.000000000000000000, 1.224606353822377258E-16, 0.000000000000000000 ) ) ;
#40058=ORIENTED_EDGE ( 'NONE', *, *, #51719, .F. ) ;
#40062=CARTESIAN_POINT ( 'NONE',  ( 25.11650669486618881, 0.000000000000000000, 4.000000000000000888 ) ) ;
#40069=CARTESIAN_POINT ( 'NONE',  ( 28.86650669486618881, 1.474610560812782335E-15, 0.000000000000000000 ) ) ;
#40104=DIRECTION ( 'NONE',  ( -1.000000000000000000, -1.224606353822377258E-16, -0.000000000000000000 ) ) ;
#40120=ORIENTED_EDGE ( 'NONE', *, *, #10972, .T. ) ;
#40142=EDGE_LOOP ( 'NONE', ( #77496, #9343, #77012, #56240, #42963 ) ) ;
#40189=ORIENTED_EDGE ( 'NONE', *, *, #44856, .T. ) ;
#40190=CYLINDRICAL_SURFACE ( 'NONE', #74272, 4.000000000000000888 ) ;
#40197=AXIS2_PLACEMENT_3D ( 'NONE', #53908, #28093, #68527 ) ;
#40203=VERTEX_POINT ( 'NONE', #90790 ) ;
#40246=ORIENTED_EDGE ( 'NONE', *, *, #51061, .T. ) ;
#40294=ADVANCED_FACE ( 'NONE', ( #15161 ), #1578, .T. ) ;
#40298=DIRECTION ( 'NONE',  ( -1.000000000000000000, -1.224606353822377258E-16, -0.000000000000000000 ) ) ;
#40314=DIRECTION ( 'NONE',  ( 0.000000000000000000, 1.000000000000000000, 0.000000000000000000 ) ) ;
#40327=DIRECTION ( 'NONE',  ( 0.000000000000000000, 0.000000000000000000, 1.000000000000000000 ) ) ;
#40342=ORIENTED_EDGE ( 'NONE', *, *, #82546, .F. ) ;
#40346=ORIENTED_EDGE ( 'NONE', *, *, #8152, .T. ) ;
#40348=CARTESIAN_POINT ( 'NONE',  ( 9.833493305133805151, 1.593028355512270962E-15, 0.000000000000000000 ) ) ;
#40375=ORIENTED_EDGE ( 'NONE', *, *, #64591, .T. ) ;
#40377=ADVANCED_FACE ( 'NONE', ( #22761 ), #27442, .T. ) ;
#40388=ORIENTED_EDGE ( 'NONE', *, *, #75417, .T. ) ;
#40397=DIRECTION ( 'NONE',  ( 0.000000000000000000, 1.000000000000000000, 0.000000000000000000 ) ) ;
#40422=AXIS2_PLACEMENT_3D ( 'NONE', #59197, #25809, #106656 ) ;
#40430=VERTEX_POINT ( 'NONE', #80416 ) ;
#40435=EDGE_LOOP ( 'NONE', ( #5, #90053, #77535, #18591, #25908, #79245 ) ) ;
#40449=AXIS2_PLACEMENT_3D ( 'NONE', #44746, #61466, #93815 ) ;
#40501=DIRECTION ( 'NONE',  ( -1.000000000000000000, -1.224606353822377258E-16, -0.000000000000000000 ) ) ;
#40575=CARTESIAN_POINT ( 'NONE',  ( 6.683837171061803417, 3.955946848495959234, -6.851900933636991375 ) ) ;
#40585=ORIENTED_EDGE ( 'NONE', *, *, #36716, .T. ) ;
#40599=DIRECTION ( 'NONE',  ( -1.000000000000000000, -0.000000000000000000, -0.000000000000000000 ) ) ;
#40663=ORIENTED_EDGE ( 'NONE', *, *, #95493, .F. ) ;
#40666=ORIENTED_EDGE ( 'NONE', *, *, #54618, .F. ) ;
#40671=DIRECTION ( 'NONE',  ( 0.000000000000000000, -1.000000000000000000, 0.000000000000000000 ) ) ;
#40679=CARTESIAN_POINT ( 'NONE',  ( 13.58349330513380515, 1.593028355512270962E-15, 0.000000000000000000 ) ) ;
#40691=DIRECTION ( 'NONE',  ( -1.000000000000000000, -0.000000000000000000, -0.000000000000000000 ) ) ;
#40701=CARTESIAN_POINT ( 'NONE',  ( 6.326622418652845248, -1.327077765693001954, 6.831545684615176306 ) ) ;
#40704=CONICAL_SURFACE ( 'NONE', #14897, 4.000000000000001776, 0.9599310885968774798 ) ;
#40749=DIRECTION ( 'NONE',  ( 0.000000000000000000, 1.000000000000000000, 0.000000000000000000 ) ) ;
#40771=CYLINDRICAL_SURFACE ( 'NONE', #66943, 4.000000000000000888 ) ;
#40787=DIRECTION ( 'NONE',  ( 0.000000000000000000, -1.000000000000000000, 0.000000000000000000 ) ) ;
#40795=VECTOR ( 'NONE', #43466, 1000.000000000000227 ) ;
#40801=ORIENTED_EDGE ( 'NONE', *, *, #53219, .T. ) ;
#40810=DIRECTION ( 'NONE',  ( -1.000000000000000000, -1.224606353822377258E-16, -0.000000000000000000 ) ) ;
#40811=EDGE_CURVE ( 'NONE', #17716, #82575, #96162, .T. ) ;
#40820=CARTESIAN_POINT ( 'NONE',  ( 6.326445470157509909, 5.253846677262519194, 4.563138989068573181 ) ) ;
#40823=ORIENTED_EDGE ( 'NONE', *, *, #81408, .F. ) ;
#40870=EDGE_CURVE ( 'NONE', #16558, #83521, #57483, .T. ) ;
#40884=LINE ( 'NONE', #15538, #73402 ) ;
#40885=CONICAL_SURFACE ( 'NONE', #13305, 4.000000000000001776, 0.9599310885968774798 ) ;
#40892=DIRECTION ( 'NONE',  ( -1.000000000000000000, -1.224606353822377258E-16, -0.000000000000000000 ) ) ;
#40912=AXIS2_PLACEMENT_3D ( 'NONE', #3824, #78750, #4883 ) ;
#40929=EDGE_CURVE ( 'NONE', #91201, #35207, #84060, .T. ) ;
#40952=EDGE_LOOP ( 'NONE', ( #74495, #23566 ) ) ;
#40959=EDGE_CURVE ( 'NONE', #100664, #47749, #106443, .T. ) ;
#40989=CARTESIAN_POINT ( 'NONE',  ( 27.61650669486618881, -3.999999999999998224, 0.000000000000000000 ) ) ;
#41000=EDGE_CURVE ( 'NONE', #90863, #49600, #20296, .T. ) ;
#41001=DIRECTION ( 'NONE',  ( 0.000000000000000000, -1.000000000000000000, 0.000000000000000000 ) ) ;
#41102=ORIENTED_EDGE ( 'NONE', *, *, #15064, .F. ) ;
#41112=CARTESIAN_POINT ( 'NONE',  ( 6.463647488011505793, 2.646730816809990561, -6.840026438643560525 ) ) ;
#41141=ORIENTED_EDGE ( 'NONE', *, *, #71742, .F. ) ;
#41150=EDGE_CURVE ( 'NONE', #54423, #80223, #99603, .T. ) ;
#41160=EDGE_CURVE ( 'NONE', #59167, #59362, #47679, .T. ) ;
#41169=EDGE_CURVE ( 'NONE', #98221, #9982, #97863, .T. ) ;
#41183=EDGE_CURVE ( 'NONE', #58745, #42272, #32067, .T. ) ;
#41198=ORIENTED_EDGE ( 'NONE', *, *, #78401, .F. ) ;
#41246=FACE_OUTER_BOUND ( 'NONE', #95041, .T. ) ;
#41266=EDGE_CURVE ( 'NONE', #104544, #62332, #42246, .T. ) ;
#41270=DIRECTION ( 'NONE',  ( -1.000000000000000000, -0.000000000000000000, -0.000000000000000000 ) ) ;
#41272=CYLINDRICAL_SURFACE ( 'NONE', #103210, 4.000000000000000888 ) ;
#41308=CYLINDRICAL_SURFACE ( 'NONE', #72384, 4.000000000000000888 ) ;
#41329=ORIENTED_EDGE ( 'NONE', *, *, #41989, .T. ) ;
#41330=DIRECTION ( 'NONE',  ( 1.000000000000000000, 1.224606353822377258E-16, 0.000000000000000000 ) ) ;
#41354=CARTESIAN_POINT ( 'NONE',  ( 6.289812543865804351, 6.246946743711088601, 2.837966828325882318 ) ) ;
#41371=AXIS2_PLACEMENT_3D ( 'NONE', #95035, #105229, #79878 ) ;
#41394=ORIENTED_EDGE ( 'NONE', *, *, #38891, .T. ) ;
#41421=DIRECTION ( 'NONE',  ( -1.000000000000000000, -1.224606353822377258E-16, -0.000000000000000000 ) ) ;
#41426=DIRECTION ( 'NONE',  ( 0.000000000000000000, -1.000000000000000000, 0.000000000000000000 ) ) ;
#41427=VECTOR ( 'NONE', #45641, 1000.000000000000000 ) ;
#41469=CARTESIAN_POINT ( 'NONE',  ( 0.000000000000000000, 0.000000000000000000, 4.000000000000000888 ) ) ;
#41488=EDGE_CURVE ( 'NONE', #20548, #32543, #18281, .T. ) ;
#41523=FACE_OUTER_BOUND ( 'NONE', #79462, .T. ) ;
#41530=B_SPLINE_CURVE_WITH_KNOTS ( 'NONE', 3,
 ( #34233, #83802, #91905, #25621, #58483, #34769 ),
 .UNSPECIFIED., .F., .F.,
 ( 4, 2, 4 ),
 ( 2.380733003146920563E-07, 0.001898835937927383956, 0.003797433802554453248 ),
 .UNSPECIFIED. ) ;
#41544=CARTESIAN_POINT ( 'NONE',  ( 21.84999999999999787, 1.533819458162526451E-15, 0.000000000000000000 ) ) ;
#41555=EDGE_LOOP ( 'NONE', ( #66686, #91002, #8907, #80460, #100806 ) ) ;
#41589=CIRCLE ( 'NONE', #96493, 4.000000000000001776 ) ;
#41640=CARTESIAN_POINT ( 'NONE',  ( 5.980097492742490140, -2.767486787162143802, 6.499999999999999112 ) ) ;
#41645=EDGE_CURVE ( 'NONE', #26618, #74653, #98984, .T. ) ;
#41651=ORIENTED_EDGE ( 'NONE', *, *, #1046, .F. ) ;
#41690=EDGE_CURVE ( 'NONE', #90250, #12821, #75831, .T. ) ;
#41698=EDGE_CURVE ( 'NONE', #77950, #72376, #19844, .T. ) ;
#41725=EDGE_CURVE ( 'NONE', #27343, #75403, #11081, .T. ) ;
#41771=CARTESIAN_POINT ( 'NONE',  ( 8.099999999999999645, 0.000000000000000000, 0.000000000000000000 ) ) ;
#41792=EDGE_CURVE ( 'NONE', #35657, #94819, #86084, .T. ) ;
#41850=ORIENTED_EDGE ( 'NONE', *, *, #34019, .F. ) ;
#41851=LINE ( 'NONE', #90955, #17183 ) ;
#41940=DIRECTION ( 'NONE',  ( 1.000000000000000000, 1.224606353822377258E-16, 0.000000000000000000 ) ) ;
#41943=EDGE_CURVE ( 'NONE', #63078, #51593, #14604, .T. ) ;
#41946=DIRECTION ( 'NONE',  ( -0.5735764363510494901, -0.8191520442889894671, 0.000000000000000000 ) ) ;
#41947=ADVANCED_FACE ( 'NONE', ( #29972 ), #62861, .T. ) ;
#41989=EDGE_CURVE ( 'NONE', #9118, #94433, #102480, .T. ) ;
#41990=CARTESIAN_POINT ( 'NONE',  ( 32.33349330513380693, 4.000000000000002665, 0.000000000000000000 ) ) ;
#41997=CIRCLE ( 'NONE', #55751, 3.309500000000001663 ) ;
#42001=DIRECTION ( 'NONE',  ( 0.000000000000000000, 1.000000000000000000, 0.000000000000000000 ) ) ;
#42115=DIRECTION ( 'NONE',  ( -1.000000000000000000, -0.000000000000000000, -0.000000000000000000 ) ) ;
#42117=CARTESIAN_POINT ( 'NONE',  ( 16.36650669486618881, 1.474610560812782335E-15, 0.000000000000000000 ) ) ;
#42127=ORIENTED_EDGE ( 'NONE', *, *, #73180, .T. ) ;
#42141=DIRECTION ( 'NONE',  ( -1.000000000000000000, -1.224606353822377258E-16, -0.000000000000000000 ) ) ;
#42142=CARTESIAN_POINT ( 'NONE',  ( 33.58349330513380693, 4.898587196589411843E-16, -4.000000000000001776 ) ) ;
#42164=CARTESIAN_POINT ( 'NONE',  ( 6.338278980374676408, -2.729992536301781403, 6.499999999999998224 ) ) ;
#42176=DIRECTION ( 'NONE',  ( -1.000000000000000000, -1.224606353822377258E-16, -0.000000000000000000 ) ) ;
#42177=CARTESIAN_POINT ( 'NONE',  ( 18.58349330513380693, -4.000000000000000888, 4.898587196589416773E-16 ) ) ;
#42181=CIRCLE ( 'NONE', #61143, 4.000000000000001776 ) ;
#42192=VERTEX_POINT ( 'NONE', #37419 ) ;
#42195=DIRECTION ( 'NONE',  ( -1.000000000000000000, -0.000000000000000000, -0.000000000000000000 ) ) ;
#42216=LINE ( 'NONE', #9842, #58405 ) ;
#42235=AXIS2_PLACEMENT_3D ( 'NONE', #44308, #30805, #63151 ) ;
#42246=LINE ( 'NONE', #57359, #65187 ) ;
#42268=DIRECTION ( 'NONE',  ( 0.000000000000000000, 0.000000000000000000, 1.000000000000000000 ) ) ;
#42271=EDGE_CURVE ( 'NONE', #93202, #82322, #71329, .T. ) ;
#42272=VERTEX_POINT ( 'NONE', #87531 ) ;
#42284=DIRECTION ( 'NONE',  ( -1.000000000000000000, -1.224606353822377258E-16, -0.000000000000000000 ) ) ;
#42298=ORIENTED_EDGE ( 'NONE', *, *, #52278, .F. ) ;
#42304=DIRECTION ( 'NONE',  ( -1.000000000000000000, -0.000000000000000000, -0.000000000000000000 ) ) ;
#42319=VERTEX_POINT ( 'NONE', #7640 ) ;
#42329=CARTESIAN_POINT ( 'NONE',  ( 27.33349330513380693, 4.000000000000002665, 0.000000000000000000 ) ) ;
#42331=DIRECTION ( 'NONE',  ( -0.5735764363510494901, -0.8191520442889894671, 0.000000000000000000 ) ) ;
#42350=VERTEX_POINT ( 'NONE', #75580 ) ;
#42351=ORIENTED_EDGE ( 'NONE', *, *, #22249, .F. ) ;
#42385=CARTESIAN_POINT ( 'NONE',  ( 6.326416241096634252, -1.324101276589546794, -6.831531844319976621 ) ) ;
#42399=ORIENTED_EDGE ( 'NONE', *, *, #258, .T. ) ;
#42435=FACE_OUTER_BOUND ( 'NONE', #51701, .T. ) ;
#42438=CARTESIAN_POINT ( 'NONE',  ( 6.169949891409288512, 4.949864754178546100, -4.426582755169667927 ) ) ;
#42466=VERTEX_POINT ( 'NONE', #93901 ) ;
#42508=CARTESIAN_POINT ( 'NONE',  ( 11.08349330513380515, 4.000000000000002665, 0.000000000000000000 ) ) ;
#42518=CARTESIAN_POINT ( 'NONE',  ( 36.84999999999999432, 1.533819458162526451E-15, 0.000000000000000000 ) ) ;
#42525=DIRECTION ( 'NONE',  ( -0.5735764363510494901, -0.8191520442889894671, 0.000000000000000000 ) ) ;
#42535=CARTESIAN_POINT ( 'NONE',  ( 20.59999999999999787, 3.309500000000003439, 4.052968581778167743E-16 ) ) ;
#42537=ORIENTED_EDGE ( 'NONE', *, *, #86640, .T. ) ;
#42568=CARTESIAN_POINT ( 'NONE',  ( 0.000000000000000000, 0.000000000000000000, 4.000000000000000888 ) ) ;
#42570=CIRCLE ( 'NONE', #33992, 4.000000000000001776 ) ;
#42581=DIRECTION ( 'NONE',  ( 0.000000000000000000, -1.000000000000000000, 0.000000000000000000 ) ) ;
#42591=DIRECTION ( 'NONE',  ( -0.7071067811865555663, 8.659560562354833018E-17, -0.7071067811865393571 ) ) ;
#42629=DIRECTION ( 'NONE',  ( -0.5735764363510497121, 0.8191520442889892450, 1.003171929053521665E-16 ) ) ;
#42641=EDGE_LOOP ( 'NONE', ( #105689, #2165, #25862, #2082, #96329 ) ) ;
#42648=CARTESIAN_POINT ( 'NONE',  ( 0.01372220897661698483, 5.948365447239581272, 2.697128823393880381 ) ) ;
#42652=LINE ( 'NONE', #16245, #21579 ) ;
#42664=ORIENTED_EDGE ( 'NONE', *, *, #12758, .T. ) ;
#42696=ORIENTED_EDGE ( 'NONE', *, *, #31661, .T. ) ;
#42709=DIRECTION ( 'NONE',  ( 1.000000000000000000, 1.224606353822377258E-16, 0.000000000000000000 ) ) ;
#42738=ORIENTED_EDGE ( 'NONE', *, *, #38175, .F. ) ;
#42769=CIRCLE ( 'NONE', #54779, 3.309500000000001663 ) ;
#42785=DIRECTION ( 'NONE',  ( 0.000000000000000000, -1.000000000000000000, 0.000000000000000000 ) ) ;
#42798=CARTESIAN_POINT ( 'NONE',  ( 25.11650669486618881, 1.474610560812782335E-15, 0.000000000000000000 ) ) ;
#42811=AXIS2_PLACEMENT_3D ( 'NONE', #100336, #26500, #100866 ) ;
#42816=ORIENTED_EDGE ( 'NONE', *, *, #70438, .F. ) ;
#42817=ADVANCED_FACE ( 'NONE', ( #20342 ), #18678, .T. ) ;
#42843=DIRECTION ( 'NONE',  ( -1.000000000000000000, -1.224606353822377258E-16, -0.000000000000000000 ) ) ;
#42851=ORIENTED_EDGE ( 'NONE', *, *, #104754, .T. ) ;
#42880=VERTEX_POINT ( 'NONE', #31582 ) ;
#42882=CARTESIAN_POINT ( 'NONE',  ( 22.61650669486618526, 1.474610560812782335E-15, 0.000000000000000000 ) ) ;
#42939=CARTESIAN_POINT ( 'NONE',  ( 38.09999999999998721, 0.000000000000000000, 0.000000000000000000 ) ) ;
#42942=DIRECTION ( 'NONE',  ( -1.000000000000000000, -1.224606353822377258E-16, -0.000000000000000000 ) ) ;
#42959=AXIS2_PLACEMENT_3D ( 'NONE', #92431, #44980, #3975 ) ;
#42963=ORIENTED_EDGE ( 'NONE', *, *, #66206, .F. ) ;
#43017=CYLINDRICAL_SURFACE ( 'NONE', #21226, 4.000000000000000888 ) ;
#43045=ORIENTED_EDGE ( 'NONE', *, *, #41150, .T. ) ;
#43050=VECTOR ( 'NONE', #32293, 1000.000000000000227 ) ;
#43102=EDGE_LOOP ( 'NONE', ( #50202, #49289, #49337, #63307, #55787 ) ) ;
#43117=EDGE_CURVE ( 'NONE', #39006, #12821, #56581, .T. ) ;
#43133=DIRECTION ( 'NONE',  ( 0.000000000000000000, -1.000000000000000000, 0.000000000000000000 ) ) ;
#43149=LINE ( 'NONE', #76032, #22088 ) ;
#43169=EDGE_LOOP ( 'NONE', ( #19485, #84576, #42851, #20987, #73115 ) ) ;
#43176=LINE ( 'NONE', #58837, #87630 ) ;
#43215=CIRCLE ( 'NONE', #69098, 3.309500000000001663 ) ;
#43251=ORIENTED_EDGE ( 'NONE', *, *, #59625, .F. ) ;
#43273=ORIENTED_EDGE ( 'NONE', *, *, #93544, .F. ) ;
#43326=CONICAL_SURFACE ( 'NONE', #103612, 3.309500000000001663, 0.9599310885968770357 ) ;
#43372=VECTOR ( 'NONE', #85865, 1000.000000000000000 ) ;
#43391=EDGE_CURVE ( 'NONE', #25738, #14483, #103114, .T. ) ;
#43398=ORIENTED_EDGE ( 'NONE', *, *, #26587, .T. ) ;
#43407=CARTESIAN_POINT ( 'NONE',  ( 33.58349330513380693, -3.851859888774471706E-31, 4.000000000000001776 ) ) ;
#43408=VECTOR ( 'NONE', #15355, 1000.000000000000000 ) ;
#43466=DIRECTION ( 'NONE',  ( 0.5735764363510491570, -0.8191520442889895781, 1.003171929053522035E-16 ) ) ;
#43468=DIRECTION ( 'NONE',  ( 0.000000000000000000, -1.000000000000000000, 0.000000000000000000 ) ) ;
#43470=FACE_OUTER_BOUND ( 'NONE', #59660, .T. ) ;
#43510=DIRECTION ( 'NONE',  ( 0.000000000000000000, -1.000000000000000000, 0.000000000000000000 ) ) ;
#43513=CARTESIAN_POINT ( 'NONE',  ( 6.585468679846620432, 3.617797563910809533, -6.733790807807556789 ) ) ;
#43516=EDGE_LOOP ( 'NONE', ( #70628, #70032, #81149, #49585, #5645 ) ) ;
#43534=VERTEX_POINT ( 'NONE', #60032 ) ;
#43601=ORIENTED_EDGE ( 'NONE', *, *, #40811, .T. ) ;
#43607=VERTEX_POINT ( 'NONE', #68091 ) ;
#43625=EDGE_CURVE ( 'NONE', #61515, #101499, #26614, .T. ) ;
#43639=CARTESIAN_POINT ( 'NONE',  ( 36.36650669486618881, -3.999999999999998224, 0.000000000000000000 ) ) ;
#43665=STYLED_ITEM ( 'NONE', ( #47685 ), #52984 ) ;
#43680=LINE ( 'NONE', #84679, #72576 ) ;
#43688=ORIENTED_EDGE ( 'NONE', *, *, #100555, .F. ) ;
#43709=CARTESIAN_POINT ( 'NONE',  ( 21.08349330513380693, 4.000000000000002665, 0.000000000000000000 ) ) ;
#43714=CIRCLE ( 'NONE', #90299, 4.000000000000001776 ) ;
#43789=EDGE_LOOP ( 'NONE', ( #71367, #53276, #39063 ) ) ;
#43797=B_SPLINE_CURVE_WITH_KNOTS ( 'NONE', 3,
 ( #88602, #30928, #64338, #41112, #57268, #40575 ),
 .UNSPECIFIED., .F., .F.,
 ( 4, 2, 4 ),
 ( 0.003990927807053583701, 0.005983070073873398773, 0.007975212340693213844 ),
 .UNSPECIFIED. ) ;
#43886=DIRECTION ( 'NONE',  ( 0.5735764363510490460, 0.8191520442889896891, 0.000000000000000000 ) ) ;
#43929=PRODUCT_DEFINITION_FORMATION_WITH_SPECIFIED_SOURCE ( 'ANY', '', #104487, .NOT_KNOWN. ) ;
#43930=ORIENTED_EDGE ( 'NONE', *, *, #50420, .F. ) ;
#43934=DIRECTION ( 'NONE',  ( 0.000000000000000000, -1.000000000000000000, 0.000000000000000000 ) ) ;
#43948=CARTESIAN_POINT ( 'NONE',  ( 19.83349330513380693, 1.593028355512270962E-15, 0.000000000000000000 ) ) ;
#43969=LINE ( 'NONE', #85501, #503 ) ;
#43991=CARTESIAN_POINT ( 'NONE',  ( 26.08349330513380693, -4.000000000000000000, 4.898587196589415787E-16 ) ) ;
#44016=ORIENTED_EDGE ( 'NONE', *, *, #88667, .F. ) ;
#44030=DIRECTION ( 'NONE',  ( -1.000000000000000000, -0.000000000000000000, -0.000000000000000000 ) ) ;
#44033=ORIENTED_EDGE ( 'NONE', *, *, #27606, .T. ) ;
#44146=FACE_OUTER_BOUND ( 'NONE', #98193, .T. ) ;
#44160=DIRECTION ( 'NONE',  ( 0.000000000000000000, -1.000000000000000000, 0.000000000000000000 ) ) ;
#44180=CIRCLE ( 'NONE', #28734, 4.000000000000000888 ) ;
#44199=AXIS2_PLACEMENT_3D ( 'NONE', #60587, #27171, #92386 ) ;
#44205=ORIENTED_EDGE ( 'NONE', *, *, #64471, .T. ) ;
#44221=CARTESIAN_POINT ( 'NONE',  ( 6.445370176742730273, 7.262437273741188193, -1.101027156350174341 ) ) ;
#44223=DIRECTION ( 'NONE',  ( -1.000000000000000000, -0.000000000000000000, -0.000000000000000000 ) ) ;
#44240=EDGE_CURVE ( 'NONE', #66028, #63078, #14477, .T. ) ;
#44250=EDGE_CURVE ( 'NONE', #67548, #32377, #65138, .T. ) ;
#44251=ORIENTED_EDGE ( 'NONE', *, *, #106551, .F. ) ;
#44252=ADVANCED_FACE ( 'NONE', ( #23688 ), #57724, .F. ) ;
#44259=FACE_OUTER_BOUND ( 'NONE', #102917, .T. ) ;
#44270=ORIENTED_EDGE ( 'NONE', *, *, #15027, .F. ) ;
#44282=DIRECTION ( 'NONE',  ( -1.000000000000000000, -0.000000000000000000, -0.000000000000000000 ) ) ;
#44283=CIRCLE ( 'NONE', #66677, 8.605212085995399107 ) ;
#44307=CONICAL_SURFACE ( 'NONE', #106257, 3.309500000000001663, 0.9599310885968770357 ) ;
#44308=CARTESIAN_POINT ( 'NONE',  ( 29.83349330513380693, 1.593028355512270962E-15, 0.000000000000000000 ) ) ;
#44310=ORIENTED_EDGE ( 'NONE', *, *, #80846, .F. ) ;
#44414=DIRECTION ( 'NONE',  ( -1.000000000000000000, -1.224606353822377258E-16, -0.000000000000000000 ) ) ;
#44459=CARTESIAN_POINT ( 'NONE',  ( 29.34999999999999787, 1.533819458162526451E-15, 0.000000000000000000 ) ) ;
#44475=FACE_OUTER_BOUND ( 'NONE', #37685, .T. ) ;
#44497=AXIS2_PLACEMENT_3D ( 'NONE', #7480, #74871, #40397 ) ;
#44498=CARTESIAN_POINT ( 'NONE',  ( 17.33349330513380693, -4.000000000000000888, 4.898587196589416773E-16 ) ) ;
#44513=DIRECTION ( 'NONE',  ( 0.000000000000000000, -1.000000000000000000, 0.000000000000000000 ) ) ;
#44527=CARTESIAN_POINT ( 'NONE',  ( 8.099999999999999645, 3.752776749732562589, -6.500000000000000888 ) ) ;
#44549=DIRECTION ( 'NONE',  ( 0.5735764363510491570, -0.8191520442889895781, 1.003171929053522035E-16 ) ) ;
#44551=CONICAL_SURFACE ( 'NONE', #70337, 3.309500000000001663, 0.9599310885968770357 ) ;
#44571=ORIENTED_EDGE ( 'NONE', *, *, #17216, .T. ) ;
#44583=CARTESIAN_POINT ( 'NONE',  ( 22.33349330513380693, 1.593028355512270962E-15, 0.000000000000000000 ) ) ;
#44622=EDGE_CURVE ( 'NONE', #96540, #15029, #105253, .T. ) ;
#44704=VERTEX_POINT ( 'NONE', #106287 ) ;
#44742=CARTESIAN_POINT ( 'NONE',  ( 6.162888688655347558, 7.505553499465140277, 0.000000000000000000 ) ) ;
#44746=CARTESIAN_POINT ( 'NONE',  ( 17.61650669486618881, 1.474610560812782335E-15, 0.000000000000000000 ) ) ;
#44762=CARTESIAN_POINT ( 'NONE',  ( 5.975663821521874475, 7.000939006314125024, -0.8740179403731729302 ) ) ;
#44770=CARTESIAN_POINT ( 'NONE',  ( 14.34999999999999787, -3.309499999999999886, 4.475777889183790779E-16 ) ) ;
#44779=ORIENTED_EDGE ( 'NONE', *, *, #95771, .F. ) ;
#44782=CARTESIAN_POINT ( 'NONE',  ( 23.09999999999999432, 3.309500000000003439, 4.052968581778167743E-16 ) ) ;
#44799=ORIENTED_EDGE ( 'NONE', *, *, #60166, .T. ) ;
#44836=AXIS2_PLACEMENT_3D ( 'NONE', #24261, #57110, #90023 ) ;
#44856=EDGE_CURVE ( 'NONE', #37712, #38220, #43176, .T. ) ;
#44865=AXIS2_PLACEMENT_3D ( 'NONE', #29342, #62232, #96695 ) ;
#44868=ORIENTED_EDGE ( 'NONE', *, *, #80711, .F. ) ;
#44870=EDGE_CURVE ( 'NONE', #19669, #1420, #47943, .T. ) ;
#44898=ORIENTED_EDGE ( 'NONE', *, *, #95834, .T. ) ;
#44936=AXIS2_PLACEMENT_3D ( 'NONE', #65277, #97624, #41001 ) ;
#44944=DIRECTION ( 'NONE',  ( -1.000000000000000000, -1.224606353822377258E-16, -0.000000000000000000 ) ) ;
#44978=VERTEX_POINT ( 'NONE', #21069 ) ;
#44980=DIRECTION ( 'NONE',  ( -1.000000000000000000, -1.224606353822377258E-16, -0.000000000000000000 ) ) ;
#45061=VERTEX_POINT ( 'NONE', #71157 ) ;
#45104=CARTESIAN_POINT ( 'NONE',  ( 0.01372220897661975345, -5.948365447239588377, -2.697128823393877273 ) ) ;
#45120=DIRECTION ( 'NONE',  ( -1.000000000000000000, -0.000000000000000000, -0.000000000000000000 ) ) ;
#45158=VECTOR ( 'NONE', #55470, 1000.000000000000000 ) ;
#45162=AXIS2_PLACEMENT_3D ( 'NONE', #78887, #21234, #54063 ) ;
#45171=DIRECTION ( 'NONE',  ( 0.000000000000000000, -1.000000000000000000, 0.000000000000000000 ) ) ;
#45187=VERTEX_POINT ( 'NONE', #99683 ) ;
#45195=DIRECTION ( 'NONE',  ( 0.000000000000000000, -1.000000000000000000, 0.000000000000000000 ) ) ;
#45200=ORIENTED_EDGE ( 'NONE', *, *, #72802, .T. ) ;
#45205=DIRECTION ( 'NONE',  ( -1.000000000000000000, -1.224606353822377258E-16, -0.000000000000000000 ) ) ;
#45283=DIRECTION ( 'NONE',  ( -1.000000000000000000, -1.224606353822377258E-16, -0.000000000000000000 ) ) ;
#45296=DIRECTION ( 'NONE',  ( 0.5735764363510490460, 0.8191520442889896891, 0.000000000000000000 ) ) ;
#45307=CARTESIAN_POINT ( 'NONE',  ( 15.11650669486618881, 0.000000000000000000, 4.000000000000000888 ) ) ;
#45315=CARTESIAN_POINT ( 'NONE',  ( 32.61650669486618881, -3.999999999999998224, 0.000000000000000000 ) ) ;
#45346=( BOUNDED_SURFACE ( )  B_SPLINE_SURFACE ( 3, 2, ( 
 ( #52832, #62018, #11833 ),
 ( #44762, #11290, #44221 ),
 ( #77652, #3767, #36698 ),
 ( #67266, #42438, #58639 ),
 ( #59173, #100145, #91540 ),
 ( #51588, #43513, #92053 ) ),
 .UNSPECIFIED., .F., .F., .F. ) 
 B_SPLINE_SURFACE_WITH_KNOTS ( ( 4, 2, 4 ),
 ( 3, 3 ),
 ( 0.003199762745115996340, 0.007302762474435749336, 0.01140576220375550190 ),
 ( 0.000000000000000000, 1.000000000000000000 ),
 .UNSPECIFIED. ) 
 GEOMETRIC_REPRESENTATION_ITEM ( )  RATIONAL_B_SPLINE_SURFACE ( (
 ( 1.000000000000000000, 0.8047731410850428313, 1.000000000000000000),
 ( 1.000000000000000000, 0.8125552299151648228, 1.000000000000000000),
 ( 1.000000000000000000, 0.8191520442896039755, 1.000000000000000000),
 ( 1.000000000000000000, 0.8191520442883749586, 1.000000000000000000),
 ( 1.000000000000000000, 0.8125552299160877512, 1.000000000000000000),
 ( 1.000000000000000000, 0.8047731410850426093, 1.000000000000000000) ) ) 
 REPRESENTATION_ITEM ( '' )  SURFACE ( )  );
#45373=AXIS2_PLACEMENT_3D ( 'NONE', #63263, #103186, #21761 ) ;
#45378=CONICAL_SURFACE ( 'NONE', #102264, 3.309500000000001663, 0.9599310885968770357 ) ;
#45396=DIRECTION ( 'NONE',  ( 0.000000000000000000, -1.000000000000000000, 0.000000000000000000 ) ) ;
#45402=ORIENTED_EDGE ( 'NONE', *, *, #88714, .F. ) ;
#45407=DIRECTION ( 'NONE',  ( -1.000000000000000000, -1.224606353822377258E-16, -0.000000000000000000 ) ) ;
#45415=VECTOR ( 'NONE', #42591, 1000.000000000000114 ) ;
#45449=DIRECTION ( 'NONE',  ( 0.000000000000000000, 1.000000000000000000, 0.000000000000000000 ) ) ;
#45453=CARTESIAN_POINT ( 'NONE',  ( 23.09999999999999432, 3.309500000000003439, 0.000000000000000000 ) ) ;
#45505=DIRECTION ( 'NONE',  ( 0.5735764363510491570, -0.8191520442889895781, 1.003171929053522035E-16 ) ) ;
#45539=EDGE_CURVE ( 'NONE', #81756, #83791, #41851, .T. ) ;
#45554=AXIS2_PLACEMENT_3D ( 'NONE', #47894, #106669, #80801 ) ;
#45556=ORIENTED_EDGE ( 'NONE', *, *, #77436, .F. ) ;
#45575=VERTEX_POINT ( 'NONE', #10545 ) ;
#45597=SURFACE_STYLE_USAGE ( .BOTH. , #31027 ) ;
#45612=DIRECTION ( 'NONE',  ( 0.000000000000000000, 0.000000000000000000, 1.000000000000000000 ) ) ;
#45641=DIRECTION ( 'NONE',  ( -1.000000000000000000, -0.000000000000000000, -0.000000000000000000 ) ) ;
#45652=FACE_OUTER_BOUND ( 'NONE', #101747, .T. ) ;
#45695=CIRCLE ( 'NONE', #105961, 4.000000000000000888 ) ;
#45736=CIRCLE ( 'NONE', #4387, 4.000000000000000888 ) ;
#45785=VERTEX_POINT ( 'NONE', #38061 ) ;
#45788=ADVANCED_FACE ( 'NONE', ( #70917 ), #60247, .T. ) ;
#45792=EDGE_CURVE ( 'NONE', #79214, #47612, #13693, .T. ) ;
#45798=ADVANCED_FACE ( 'NONE', ( #5128 ), #70533, .T. ) ;
#45806=DIRECTION ( 'NONE',  ( -1.000000000000000000, -0.000000000000000000, -0.000000000000000000 ) ) ;
#45839=CARTESIAN_POINT ( 'NONE',  ( 0.000000000000000000, 0.000000000000000000, 0.000000000000000000 ) ) ;
#45843=ORIENTED_EDGE ( 'NONE', *, *, #80846, .T. ) ;
#45847=EDGE_CURVE ( 'NONE', #83001, #98221, #87118, .T. ) ;
#45887=EDGE_CURVE ( 'NONE', #81895, #56180, #65218, .T. ) ;
#45919=ORIENTED_EDGE ( 'NONE', *, *, #68885, .F. ) ;
#45932=EDGE_CURVE ( 'NONE', #74451, #64739, #31804, .T. ) ;
#45937=ADVANCED_FACE ( 'NONE', ( #82997 ), #53286, .T. ) ;
#45945=EDGE_CURVE ( 'NONE', #104544, #101499, #6840, .T. ) ;
#45953=DIRECTION ( 'NONE',  ( 1.000000000000000000, 1.224606353822377258E-16, 0.000000000000000000 ) ) ;
#45965=CARTESIAN_POINT ( 'NONE',  ( 33.09999999999999432, 3.309500000000003439, 4.052968581778167743E-16 ) ) ;
#45967=VECTOR ( 'NONE', #67354, 1000.000000000000000 ) ;
#45991=VERTEX_POINT ( 'NONE', #93219 ) ;
#46019=CARTESIAN_POINT ( 'NONE',  ( 6.445370176742772017, -7.262437273741305432, 1.101027156350034231 ) ) ;
#46023=LINE ( 'NONE', #79438, #6943 ) ;
#46036=EDGE_LOOP ( 'NONE', ( #63669, #1899, #51152, #54767, #94873, #4355 ) ) ;
#46039=DIRECTION ( 'NONE',  ( 0.5735764363510490460, 0.8191520442889896891, 0.000000000000000000 ) ) ;
#46050=CIRCLE ( 'NONE', #49491, 4.000000000000001776 ) ;
#46086=ORIENTED_EDGE ( 'NONE', *, *, #1355, .T. ) ;
#46111=CARTESIAN_POINT ( 'NONE',  ( 9.833493305133805151, 1.593028355512270962E-15, 0.000000000000000000 ) ) ;
#46119=CARTESIAN_POINT ( 'NONE',  ( 0.05533025579362134405, 6.264553569211843254, -2.149474931388135612 ) ) ;
#46123=( NAMED_UNIT ( * ) SI_UNIT ( $, .STERADIAN. ) SOLID_ANGLE_UNIT ( ) );
#46125=AXIS2_PLACEMENT_3D ( 'NONE', #24560, #47725, #32104 ) ;
#46128=ORIENTED_EDGE ( 'NONE', *, *, #95834, .F. ) ;
#46130=DIRECTION ( 'NONE',  ( -1.000000000000000000, -1.224606353822377258E-16, -0.000000000000000000 ) ) ;
#46164=ORIENTED_EDGE ( 'NONE', *, *, #94277, .F. ) ;
#46183=VERTEX_POINT ( 'NONE', #36617 ) ;
#46194=EDGE_CURVE ( 'NONE', #35657, #37979, #12814, .T. ) ;
#46262=VECTOR ( 'NONE', #87641, 1000.000000000000000 ) ;
#46275=ORIENTED_EDGE ( 'NONE', *, *, #56545, .T. ) ;
#46288=LINE ( 'NONE', #71085, #5979 ) ;
#46366=DIRECTION ( 'NONE',  ( -1.000000000000000000, -1.224606353822377258E-16, -0.000000000000000000 ) ) ;
#46367=AXIS2_PLACEMENT_3D ( 'NONE', #42939, #101706, #35955 ) ;
#46373=LINE ( 'NONE', #72748, #84518 ) ;
#46374=ADVANCED_FACE ( 'NONE', ( #48367 ), #19060, .T. ) ;
#46381=AXIS2_PLACEMENT_3D ( 'NONE', #92194, #67937, #58796 ) ;
#46389=AXIS2_PLACEMENT_3D ( 'NONE', #55775, #104345, #55258 ) ;
#46455=DIRECTION ( 'NONE',  ( 0.000000000000000000, -1.000000000000000000, 0.000000000000000000 ) ) ;
#46462=ADVANCED_FACE ( 'NONE', ( #68293 ), #100113, .T. ) ;
#46467=AXIS2_PLACEMENT_3D ( 'NONE', #2739, #44282, #91770 ) ;
#46494=ORIENTED_EDGE ( 'NONE', *, *, #19163, .T. ) ;
#46512=EDGE_CURVE ( 'NONE', #99443, #98362, #83931, .T. ) ;
#46514=EDGE_LOOP ( 'NONE', ( #30888, #61735, #7909, #30124, #64167, #44016 ) ) ;
#46517=CARTESIAN_POINT ( 'NONE',  ( 18.86650669486618881, 1.474610560812782335E-15, 0.000000000000000000 ) ) ;
#46553=CARTESIAN_POINT ( 'NONE',  ( 6.162888688655344005, 3.752776749732565253, 6.499999999999997335 ) ) ;
#46570=VERTEX_POINT ( 'NONE', #51560 ) ;
#46590=CARTESIAN_POINT ( 'NONE',  ( 28.09999999999999787, 1.533819458162526451E-15, 0.000000000000000000 ) ) ;
#46613=LINE ( 'NONE', #53122, #54635 ) ;
#46707=EDGE_CURVE ( 'NONE', #38220, #104988, #31137, .T. ) ;
#46709=AXIS2_PLACEMENT_3D ( 'NONE', #65062, #56418, #17056 ) ;
#46778=VECTOR ( 'NONE', #10681, 1000.000000000000000 ) ;
#46797=ORIENTED_EDGE ( 'NONE', *, *, #12626, .T. ) ;
#46803=EDGE_CURVE ( 'NONE', #82575, #38206, #65524, .T. ) ;
#46826=ORIENTED_EDGE ( 'NONE', *, *, #4809, .F. ) ;
#46828=LINE ( 'NONE', #55955, #66780 ) ;
#46920=CARTESIAN_POINT ( 'NONE',  ( 0.5805565836007617886, -3.752776749732566142, 6.499999999999999112 ) ) ;
#46953=DIRECTION ( 'NONE',  ( 0.000000000000000000, -1.000000000000000000, 0.000000000000000000 ) ) ;
#46974=VERTEX_POINT ( 'NONE', #455 ) ;
#47036=CARTESIAN_POINT ( 'NONE',  ( 0.000000000000000000, 4.898587196589413815E-16, -4.000000000000000888 ) ) ;
#47096=CARTESIAN_POINT ( 'NONE',  ( 6.289812543865805239, -6.246946743711091266, -2.837966828325885871 ) ) ;
#47114=SHAPE_DEFINITION_REPRESENTATION ( #20094, #22667 ) ;
#47117=CARTESIAN_POINT ( 'NONE',  ( 14.83349330513380693, 1.593028355512270962E-15, 0.000000000000000000 ) ) ;
#47126=CARTESIAN_POINT ( 'NONE',  ( 29.83349330513380693, 4.000000000000003553, 0.000000000000000000 ) ) ;
#47181=ORIENTED_EDGE ( 'NONE', *, *, #100937, .T. ) ;
#47192=VERTEX_POINT ( 'NONE', #68440 ) ;
#47200=ORIENTED_EDGE ( 'NONE', *, *, #45932, .T. ) ;
#47206=DIRECTION ( 'NONE',  ( -1.000000000000000000, -0.000000000000000000, -0.000000000000000000 ) ) ;
#47212=CARTESIAN_POINT ( 'NONE',  ( 34.83349330513380693, 4.000000000000002665, 0.000000000000000000 ) ) ;
#47248=ADVANCED_FACE ( 'NONE', ( #69500 ), #26077, .T. ) ;
#47265=EDGE_CURVE ( 'NONE', #37712, #59582, #68979, .T. ) ;
#47288=VERTEX_POINT ( 'NONE', #61418 ) ;
#47300=CARTESIAN_POINT ( 'NONE',  ( 6.585304930659545697, 4.021878819315965359, -6.500000000000000888 ) ) ;
#47317=ORIENTED_EDGE ( 'NONE', *, *, #29187, .T. ) ;
#47333=DIRECTION ( 'NONE',  ( -1.000000000000000000, -0.000000000000000000, -0.000000000000000000 ) ) ;
#47363=CARTESIAN_POINT ( 'NONE',  ( 31.84999999999999787, -3.309499999999999886, 4.475777889183790779E-16 ) ) ;
#47390=ORIENTED_EDGE ( 'NONE', *, *, #20313, .T. ) ;
#47391=CARTESIAN_POINT ( 'NONE',  ( 6.289692432696722513, -6.589071317540692085, -2.245373559998704582 ) ) ;
#47399=VECTOR ( 'NONE', #30658, 1000.000000000000000 ) ;
#47404=AXIS2_PLACEMENT_3D ( 'NONE', #77853, #13095, #12041 ) ;
#47425=CARTESIAN_POINT ( 'NONE',  ( 16.08349330513380337, 4.000000000000003553, 0.000000000000000000 ) ) ;
#47443=CONICAL_SURFACE ( 'NONE', #55977, 3.309500000000001663, 0.9599310885968770357 ) ;
#47477=ORIENTED_EDGE ( 'NONE', *, *, #67276, .T. ) ;
#47480=DIRECTION ( 'NONE',  ( -1.000000000000000000, -1.224606353822377258E-16, -0.000000000000000000 ) ) ;
#47485=CIRCLE ( 'NONE', #18260, 4.000000000000000888 ) ;
#47489=AXIS2_PLACEMENT_3D ( 'NONE', #15712, #16781, #83105 ) ;
#47498=CARTESIAN_POINT ( 'NONE',  ( 34.83349330513380693, 4.898587196589411843E-16, -4.000000000000001776 ) ) ;
#47503=EDGE_LOOP ( 'NONE', ( #84037, #94917 ) ) ;
#47549=FACE_OUTER_BOUND ( 'NONE', #35142, .T. ) ;
#47551=EDGE_CURVE ( 'NONE', #37712, #42350, #70838, .T. ) ;
#47579=ORIENTED_EDGE ( 'NONE', *, *, #22249, .T. ) ;
#47612=VERTEX_POINT ( 'NONE', #82358 ) ;
#47650=PLANE ( 'NONE',  #12289 ) ;
#47679=LINE ( 'NONE', #72497, #46262 ) ;
#47685=PRESENTATION_STYLE_ASSIGNMENT (( #45597 ) ) ;
#47688=AXIS2_PLACEMENT_3D ( 'NONE', #67571, #93440, #1191 ) ;
#47708=CARTESIAN_POINT ( 'NONE',  ( 18.09999999999999787, 1.533819458162526451E-15, 0.000000000000000000 ) ) ;
#47715=CARTESIAN_POINT ( 'NONE',  ( 24.34999999999999787, 3.309500000000003439, 4.052968581778167743E-16 ) ) ;
#47723=LINE ( 'NONE', #30524, #54833 ) ;
#47725=DIRECTION ( 'NONE',  ( -1.000000000000000000, -1.224606353822377258E-16, -0.000000000000000000 ) ) ;
#47746=CARTESIAN_POINT ( 'NONE',  ( 20.11650669486618881, 1.474610560812782335E-15, 0.000000000000000000 ) ) ;
#47749=VERTEX_POINT ( 'NONE', #78510 ) ;
#47760=CIRCLE ( 'NONE', #59888, 4.000000000000000888 ) ;
#47799=EDGE_CURVE ( 'NONE', #78892, #93357, #3710, .T. ) ;
#47820=CARTESIAN_POINT ( 'NONE',  ( 5.817833032102705637, -1.364745674334431280, -6.500000000000000888 ) ) ;
#47828=DIRECTION ( 'NONE',  ( 0.000000000000000000, -1.000000000000000000, 0.000000000000000000 ) ) ;
#47837=DIRECTION ( 'NONE',  ( -1.000000000000000000, -1.224606353822377258E-16, -0.000000000000000000 ) ) ;
#47878=DIRECTION ( 'NONE',  ( 1.000000000000000000, 0.000000000000000000, 0.000000000000000000 ) ) ;
#47894=CARTESIAN_POINT ( 'NONE',  ( 37.33349330513379982, 1.593028355512270962E-15, 0.000000000000000000 ) ) ;
#47897=VECTOR ( 'NONE', #104848, 1000.000000000000000 ) ;
#47912=CARTESIAN_POINT ( 'NONE',  ( 5.819846122303832914, -4.937269551422636127, -4.448398286273207880 ) ) ;
#47920=AXIS2_PLACEMENT_3D ( 'NONE', #65491, #72510, #40671 ) ;
#47931=CARTESIAN_POINT ( 'NONE',  ( 12.61650669486618881, 0.000000000000000000, 4.000000000000000888 ) ) ;
#47943=CIRCLE ( 'NONE', #42811, 4.000000000000001776 ) ;
#47988=DIRECTION ( 'NONE',  ( -1.000000000000000000, -1.224606353822377258E-16, -0.000000000000000000 ) ) ;
#48022=DIRECTION ( 'NONE',  ( 0.000000000000000000, -1.000000000000000000, 0.000000000000000000 ) ) ;
#48088=ORIENTED_EDGE ( 'NONE', *, *, #75151, .F. ) ;
#48112=ADVANCED_FACE ( 'NONE', ( #25634 ), #49508, .T. ) ;
#48133=ORIENTED_EDGE ( 'NONE', *, *, #24204, .T. ) ;
#48186=EDGE_CURVE ( 'NONE', #75208, #17393, #85733, .T. ) ;
#48188=CARTESIAN_POINT ( 'NONE',  ( 19.83349330513380693, 4.000000000000003553, 0.000000000000000000 ) ) ;
#48232=EDGE_CURVE ( 'NONE', #52343, #45785, #104639, .T. ) ;
#48274=DIRECTION ( 'NONE',  ( -1.000000000000000000, -0.000000000000000000, -0.000000000000000000 ) ) ;
#48283=CARTESIAN_POINT ( 'NONE',  ( 19.34999999999999787, -3.309499999999999886, 4.475777889183790779E-16 ) ) ;
#48337=ORIENTED_EDGE ( 'NONE', *, *, #81881, .T. ) ;
#48344=ORIENTED_EDGE ( 'NONE', *, *, #14629, .F. ) ;
#48359=CARTESIAN_POINT ( 'NONE',  ( 6.443810749341881916, -2.669419465175184136, -6.839891222013585015 ) ) ;
#48363=AXIS2_PLACEMENT_3D ( 'NONE', #57098, #106715, #88955 ) ;
#48367=FACE_OUTER_BOUND ( 'NONE', #88411, .T. ) ;
#48387=VERTEX_POINT ( 'NONE', #23907 ) ;
#48390=ORIENTED_EDGE ( 'NONE', *, *, #45539, .F. ) ;
#48395=ORIENTED_EDGE ( 'NONE', *, *, #60818, .T. ) ;
#48406=FACE_OUTER_BOUND ( 'NONE', #43789, .T. ) ;
#48411=ORIENTED_EDGE ( 'NONE', *, *, #61861, .T. ) ;
#48438=CARTESIAN_POINT ( 'NONE',  ( -3.482999479109682994E-15, 5.309483803148794756, 3.803704290982253600 ) ) ;
#48453=ORIENTED_EDGE ( 'NONE', *, *, #2446, .F. ) ;
#48456=ORIENTED_EDGE ( 'NONE', *, *, #87664, .T. ) ;
#48458=CIRCLE ( 'NONE', #19293, 3.309500000000001663 ) ;
#48512=EDGE_CURVE ( 'NONE', #64041, #51129, #9656, .T. ) ;
#48529=VERTEX_POINT ( 'NONE', #11789 ) ;
#48541=CARTESIAN_POINT ( 'NONE',  ( 15.59999999999999787, -3.309499999999999886, 4.475777889183790779E-16 ) ) ;
#48646=DIRECTION ( 'NONE',  ( -0.5735764363510497121, 0.8191520442889892450, 1.003171929053521665E-16 ) ) ;
#48655=DIRECTION ( 'NONE',  ( 0.000000000000000000, -1.000000000000000000, 0.000000000000000000 ) ) ;
#48737=ORIENTED_EDGE ( 'NONE', *, *, #29325, .F. ) ;
#48769=FACE_OUTER_BOUND ( 'NONE', #6879, .T. ) ;
#48784=VERTEX_POINT ( 'NONE', #87799 ) ;
#48796=ORIENTED_EDGE ( 'NONE', *, *, #47551, .T. ) ;
#48817=CARTESIAN_POINT ( 'NONE',  ( 6.162888688655344893, 3.752776749732562589, -6.500000000000000888 ) ) ;
#48819=CARTESIAN_POINT ( 'NONE',  ( 8.866506694866188809, 0.000000000000000000, 4.000000000000000888 ) ) ;
#48839=DIRECTION ( 'NONE',  ( -1.000000000000000000, -1.224606353822377258E-16, -0.000000000000000000 ) ) ;
#48853=AXIS2_PLACEMENT_3D ( 'NONE', #73429, #22804, #65359 ) ;
#48877=CARTESIAN_POINT ( 'NONE',  ( 16.08349330513380337, 1.593028355512270962E-15, 0.000000000000000000 ) ) ;
#48892=ORIENTED_EDGE ( 'NONE', *, *, #93163, .F. ) ;
#48919=ORIENTED_EDGE ( 'NONE', *, *, #90778, .T. ) ;
#48925=EDGE_CURVE ( 'NONE', #25099, #88621, #86689, .T. ) ;
#48930=FACE_OUTER_BOUND ( 'NONE', #91238, .T. ) ;
#48950=ORIENTED_EDGE ( 'NONE', *, *, #41698, .F. ) ;
#48969=VERTEX_POINT ( 'NONE', #51028 ) ;
#48985=DIRECTION ( 'NONE',  ( -1.000000000000000000, -1.224606353822377258E-16, -0.000000000000000000 ) ) ;
#49017=AXIS2_PLACEMENT_3D ( 'NONE', #26148, #52485, #42268 ) ;
#49028=CARTESIAN_POINT ( 'NONE',  ( 0.000000000000000000, 4.898587196589413815E-16, -4.000000000000000888 ) ) ;
#49084=CARTESIAN_POINT ( 'NONE',  ( 11.36650669486618881, 1.474610560812782335E-15, 0.000000000000000000 ) ) ;
#49172=ORIENTED_EDGE ( 'NONE', *, *, #13306, .T. ) ;
#49173=DIRECTION ( 'NONE',  ( 0.000000000000000000, 0.000000000000000000, 1.000000000000000000 ) ) ;
#49178=AXIS2_PLACEMENT_3D ( 'NONE', #75172, #42284, #50368 ) ;
#49211=EDGE_LOOP ( 'NONE', ( #106125, #76447, #50427, #14593, #4768, #38401 ) ) ;
#49212=EDGE_CURVE ( 'NONE', #102768, #30747, #31063, .T. ) ;
#49234=DIRECTION ( 'NONE',  ( 0.000000000000000000, -1.000000000000000000, 0.000000000000000000 ) ) ;
#49244=DIRECTION ( 'NONE',  ( 0.5735764363510490460, 0.8191520442889896891, 0.000000000000000000 ) ) ;
#49259=ORIENTED_EDGE ( 'NONE', *, *, #6030, .T. ) ;
#49281=DIRECTION ( 'NONE',  ( -0.5735764363510494901, -0.8191520442889894671, 0.000000000000000000 ) ) ;
#49289=ORIENTED_EDGE ( 'NONE', *, *, #106551, .T. ) ;
#49301=APPLICATION_CONTEXT ( 'automotive_design' ) ;
#49337=ORIENTED_EDGE ( 'NONE', *, *, #59356, .F. ) ;
#49345=CARTESIAN_POINT ( 'NONE',  ( 6.394337469123806628, -3.776351736504768741, -6.540833074877208553 ) ) ;
#49346=ORIENTED_EDGE ( 'NONE', *, *, #14637, .T. ) ;
#49352=DIRECTION ( 'NONE',  ( 0.5735764363510490460, 0.8191520442889896891, 0.000000000000000000 ) ) ;
#49355=CIRCLE ( 'NONE', #2859, 4.000000000000000888 ) ;
#49364=EDGE_CURVE ( 'NONE', #17049, #73038, #97870, .T. ) ;
#49384=CARTESIAN_POINT ( 'NONE',  ( 0.000000000000000000, 0.000000000000000000, 0.000000000000000000 ) ) ;
#49385=FACE_OUTER_BOUND ( 'NONE', #46514, .T. ) ;
#49416=ORIENTED_EDGE ( 'NONE', *, *, #26263, .F. ) ;
#49456=FACE_OUTER_BOUND ( 'NONE', #19617, .T. ) ;
#49462=EDGE_CURVE ( 'NONE', #63533, #96201, #105116, .T. ) ;
#49486=DIRECTION ( 'NONE',  ( 0.000000000000000000, -1.000000000000000000, 0.000000000000000000 ) ) ;
#49491=AXIS2_PLACEMENT_3D ( 'NONE', #7636, #98776, #32495 ) ;
#49500=CONICAL_SURFACE ( 'NONE', #28934, 3.309500000000001663, 0.9599310885968770357 ) ;
#49506=DIRECTION ( 'NONE',  ( 0.000000000000000000, -1.000000000000000000, 0.000000000000000000 ) ) ;
#49508=CONICAL_SURFACE ( 'NONE', #6465, 3.309500000000001663, 0.9599310885968770357 ) ;
#49509=DIRECTION ( 'NONE',  ( -1.000000000000000000, -1.224606353822377258E-16, -0.000000000000000000 ) ) ;
#49516=CARTESIAN_POINT ( 'NONE',  ( 5.819846122303832914, -6.321060697775078729, -2.051601713726796561 ) ) ;
#49525=CARTESIAN_POINT ( 'NONE',  ( -2.683400376901624263E-15, -5.469921996229798467, 3.525817189091414949 ) ) ;
#49538=AXIS2_PLACEMENT_3D ( 'NONE', #61192, #2401, #43934 ) ;
#49549=CARTESIAN_POINT ( 'NONE',  ( 11.36650669486618881, 4.898587196589413815E-16, -4.000000000000000888 ) ) ;
#49570=CARTESIAN_POINT ( 'NONE',  ( 21.84999999999999787, 1.533819458162526451E-15, 0.000000000000000000 ) ) ;
#49585=ORIENTED_EDGE ( 'NONE', *, *, #85240, .F. ) ;
#49587=VECTOR ( 'NONE', #56725, 1000.000000000000000 ) ;
#49600=VERTEX_POINT ( 'NONE', #95638 ) ;
#49638=AXIS2_PLACEMENT_3D ( 'NONE', #61595, #63714, #86408 ) ;
#49640=VERTEX_POINT ( 'NONE', #79964 ) ;
#49651=EDGE_LOOP ( 'NONE', ( #72080, #79703, #101931, #104677, #93800 ) ) ;
#49722=FACE_OUTER_BOUND ( 'NONE', #13979, .T. ) ;
#49727=CARTESIAN_POINT ( 'NONE',  ( 28.86650669486618881, 4.898587196589413815E-16, -4.000000000000000888 ) ) ;
#49746=CONICAL_SURFACE ( 'NONE', #3255, 4.000000000000001776, 0.9599310885968774798 ) ;
#49776=ORIENTED_EDGE ( 'NONE', *, *, #61176, .F. ) ;
#49800=EDGE_CURVE ( 'NONE', #54339, #60761, #77554, .T. ) ;
#49842=DIRECTION ( 'NONE',  ( -1.000000000000000000, -1.224606353822377258E-16, -0.000000000000000000 ) ) ;
#49859=ORIENTED_EDGE ( 'NONE', *, *, #57291, .T. ) ;
#49890=FACE_OUTER_BOUND ( 'NONE', #89924, .T. ) ;
#49904=EDGE_CURVE ( 'NONE', #90401, #54423, #62110, .T. ) ;
#49913=CARTESIAN_POINT ( 'NONE',  ( 0.000000000000000000, 0.000000000000000000, 0.000000000000000000 ) ) ;
#49932=AXIS2_PLACEMENT_3D ( 'NONE', #50299, #83202, #99915 ) ;
#49965=CARTESIAN_POINT ( 'NONE',  ( 0.000000000000000000, 4.898587196589413815E-16, -4.000000000000000888 ) ) ;
#49970=CARTESIAN_POINT ( 'NONE',  ( 26.08349330513380693, 1.593028355512270962E-15, 0.000000000000000000 ) ) ;
#49990=ORIENTED_EDGE ( 'NONE', *, *, #8935, .F. ) ;
#50036=CARTESIAN_POINT ( 'NONE',  ( 0.2573354458087814822, 4.368923434677189022, 5.432802636760777126 ) ) ;
#50091=DIRECTION ( 'NONE',  ( -1.000000000000000000, -0.000000000000000000, -0.000000000000000000 ) ) ;
#50152=EDGE_CURVE ( 'NONE', #80922, #90030, #87958, .T. ) ;
#50154=CARTESIAN_POINT ( 'NONE',  ( 38.09999999999998721, 4.052968581778165278E-16, -3.309499999999999886 ) ) ;
#50164=AXIS2_PLACEMENT_3D ( 'NONE', #93324, #4308, #3252 ) ;
#50183=EDGE_LOOP ( 'NONE', ( #42696, #28361, #78651, #75013 ) ) ;
#50188=DIRECTION ( 'NONE',  ( -1.000000000000000000, -1.224606353822377258E-16, -0.000000000000000000 ) ) ;
#50202=ORIENTED_EDGE ( 'NONE', *, *, #9204, .T. ) ;
#50205=DIRECTION ( 'NONE',  ( 0.000000000000000000, 1.000000000000000000, 0.000000000000000000 ) ) ;
#50247=CARTESIAN_POINT ( 'NONE',  ( 18.58349330513380693, 1.593028355512270962E-15, 0.000000000000000000 ) ) ;
#50269=CARTESIAN_POINT ( 'NONE',  ( 35.59999999999999432, 1.533819458162526451E-15, 0.000000000000000000 ) ) ;
#50285=CARTESIAN_POINT ( 'NONE',  ( 6.162888688655347558, -3.752776749732574135, -6.500000000000001776 ) ) ;
#50288=EDGE_CURVE ( 'NONE', #94695, #75208, #60492, .T. ) ;
#50299=CARTESIAN_POINT ( 'NONE',  ( 6.936184427528457874, 0.000000000000000000, 0.000000000000000000 ) ) ;
#50311=CONICAL_SURFACE ( 'NONE', #29732, 3.309500000000001663, 0.9599310885968770357 ) ;
#50345=DIRECTION ( 'NONE',  ( 1.000000000000000000, 0.000000000000000000, 0.000000000000000000 ) ) ;
#50352=DIRECTION ( 'NONE',  ( 0.000000000000000000, -1.000000000000000000, 0.000000000000000000 ) ) ;
#50368=DIRECTION ( 'NONE',  ( 0.000000000000000000, -1.000000000000000000, 0.000000000000000000 ) ) ;
#50384=LINE ( 'NONE', #9386, #38553 ) ;
#50420=EDGE_CURVE ( 'NONE', #49600, #16458, #28613, .T. ) ;
#50427=ORIENTED_EDGE ( 'NONE', *, *, #66363, .T. ) ;
#50439=CARTESIAN_POINT ( 'NONE',  ( 11.08349330513380515, -4.000000000000000888, 4.898587196589416773E-16 ) ) ;
#50450=EDGE_LOOP ( 'NONE', ( #92055, #11538, #80828, #21119, #33770 ) ) ;
#50475=CARTESIAN_POINT ( 'NONE',  ( 12.33349330513380693, -3.851859888774471706E-31, 4.000000000000001776 ) ) ;
#50484=DIRECTION ( 'NONE',  ( -1.000000000000000000, -0.000000000000000000, -0.000000000000000000 ) ) ;
#50534=LINE ( 'NONE', #19316, #86755 ) ;
#50595=AXIS2_PLACEMENT_3D ( 'NONE', #8620, #39943, #72298 ) ;
#50621=CONICAL_SURFACE ( 'NONE', #4159, 6.500000000000000000, 1.047197551196600296 ) ;
#50623=EDGE_LOOP ( 'NONE', ( #16052, #73006, #96094, #61878, #7722 ) ) ;
#50648=CARTESIAN_POINT ( 'NONE',  ( 24.34999999999999787, -3.309499999999999886, 4.475777889183790779E-16 ) ) ;
#50651=ADVANCED_FACE ( 'NONE', ( #62251 ), #63827, .T. ) ;
#50653=ORIENTED_EDGE ( 'NONE', *, *, #77329, .T. ) ;
#50680=ORIENTED_EDGE ( 'NONE', *, *, #8120, .F. ) ;
#50688=AXIS2_PLACEMENT_3D ( 'NONE', #47708, #38592, #56860 ) ;
#50698=AXIS2_PLACEMENT_3D ( 'NONE', #58515, #81690, #24579 ) ;
#50711=ORIENTED_EDGE ( 'NONE', *, *, #94630, .F. ) ;
#50715=CARTESIAN_POINT ( 'NONE',  ( 0.000000000000000000, 5.629165124598848102, 3.250000000000005329 ) ) ;
#50748=CARTESIAN_POINT ( 'NONE',  ( 25.11650669486618881, 4.000000000000003553, 4.898587196589414801E-16 ) ) ;
#50752=DIRECTION ( 'NONE',  ( -1.000000000000000000, -1.224606353822377258E-16, -0.000000000000000000 ) ) ;
#50772=CARTESIAN_POINT ( 'NONE',  ( 14.34999999999999787, 1.533819458162526451E-15, 0.000000000000000000 ) ) ;
#50880=CIRCLE ( 'NONE', #16563, 3.309500000000001663 ) ;
#50883=CARTESIAN_POINT ( 'NONE',  ( 16.84999999999999787, 3.309500000000003439, 4.052968581778167743E-16 ) ) ;
#50911=ORIENTED_EDGE ( 'NONE', *, *, #53219, .F. ) ;
#50930=EDGE_LOOP ( 'NONE', ( #57171, #42816, #50680, #96839, #101945, #101701 ) ) ;
#50944=CARTESIAN_POINT ( 'NONE',  ( 12.33349330513380693, 1.593028355512270962E-15, 0.000000000000000000 ) ) ;
#50997=CARTESIAN_POINT ( 'NONE',  ( 6.326445470157510798, -6.578717624163891387, 2.268395195563515099 ) ) ;
#50998=ORIENTED_EDGE ( 'NONE', *, *, #63676, .F. ) ;
#51009=VERTEX_POINT ( 'NONE', #65934 ) ;
#51028=CARTESIAN_POINT ( 'NONE',  ( 29.83349330513380693, -4.000000000000000888, 4.898587196589416773E-16 ) ) ;
#51059=DIRECTION ( 'NONE',  ( -0.5735764363510494901, -0.8191520442889894671, 0.000000000000000000 ) ) ;
#51061=EDGE_CURVE ( 'NONE', #71083, #1485, #92856, .T. ) ;
#51071=LINE ( 'NONE', #85607, #22017 ) ;
#51072=DIRECTION ( 'NONE',  ( -0.5735764363510497121, 0.8191520442889892450, 1.003171929053521665E-16 ) ) ;
#51104=CARTESIAN_POINT ( 'NONE',  ( 6.445370176742730273, -7.262437273741192634, -1.101027156350390390 ) ) ;
#51129=VERTEX_POINT ( 'NONE', #24319 ) ;
#51152=ORIENTED_EDGE ( 'NONE', *, *, #8740, .T. ) ;
#51190=CARTESIAN_POINT ( 'NONE',  ( 26.84999999999999787, -3.309499999999999886, 4.475777889183790779E-16 ) ) ;
#51199=ORIENTED_EDGE ( 'NONE', *, *, #77867, .T. ) ;
#51221=DIRECTION ( 'NONE',  ( -1.000000000000000000, -1.224606353822377258E-16, -0.000000000000000000 ) ) ;
#51232=CIRCLE ( 'NONE', #35829, 6.500000000000000888 ) ;
#51253=ADVANCED_FACE ( 'NONE', ( #7960 ), #86433, .T. ) ;
#51254=CARTESIAN_POINT ( 'NONE',  ( 0.5805565836007658964, 7.505553499465141165, -3.996997974842411264E-16 ) ) ;
#51255=VERTEX_POINT ( 'NONE', #64627 ) ;
#51261=DIRECTION ( 'NONE',  ( -1.000000000000000000, -1.224606353822377258E-16, -0.000000000000000000 ) ) ;
#51279=ORIENTED_EDGE ( 'NONE', *, *, #24838, .T. ) ;
#51284=EDGE_CURVE ( 'NONE', #74653, #25041, #7167, .T. ) ;
#51309=FACE_OUTER_BOUND ( 'NONE', #26003, .T. ) ;
#51333=VECTOR ( 'NONE', #105470, 1000.000000000000000 ) ;
#51351=UNCERTAINTY_MEASURE_WITH_UNIT (LENGTH_MEASURE( 1.000000000000000082E-05 ), #53090, 'distance_accuracy_value', 'NONE');
#51353=CYLINDRICAL_SURFACE ( 'NONE', #953, 4.000000000000000888 ) ;
#51381=CIRCLE ( 'NONE', #27275, 4.000000000000000888 ) ;
#51418=CARTESIAN_POINT ( 'NONE',  ( 26.36650669486618881, -3.999999999999998224, 0.000000000000000000 ) ) ;
#51425=DIRECTION ( 'NONE',  ( 0.000000000000000000, -1.000000000000000000, 0.000000000000000000 ) ) ;
#51442=DIRECTION ( 'NONE',  ( 0.000000000000000000, 0.000000000000000000, 1.000000000000000000 ) ) ;
#51485=CARTESIAN_POINT ( 'NONE',  ( 0.000000000000000000, 0.000000000000000000, 0.000000000000000000 ) ) ;
#51491=EDGE_CURVE ( 'NONE', #32616, #99250, #10400, .T. ) ;
#51524=TOROIDAL_SURFACE ( 'NONE', #46381, 8.400000000000000355, 0.5999999999999978684 ) ;
#51560=CARTESIAN_POINT ( 'NONE',  ( 6.162888688655347558, -3.752776749732574135, -6.500000000000001776 ) ) ;
#51572=ORIENTED_EDGE ( 'NONE', *, *, #64219, .F. ) ;
#51588=CARTESIAN_POINT ( 'NONE',  ( 6.222742520105470021, 3.584500230190541092, -6.791463481567638460 ) ) ;
#51593=VERTEX_POINT ( 'NONE', #33602 ) ;
#51701=EDGE_LOOP ( 'NONE', ( #15371, #11974, #106630 ) ) ;
#51719=EDGE_CURVE ( 'NONE', #80223, #3039, #17752, .T. ) ;
#51727=AXIS2_PLACEMENT_3D ( 'NONE', #32213, #40810, #47828 ) ;
#51749=VECTOR ( 'NONE', #81147, 1000.000000000000227 ) ;
#51750=EDGE_CURVE ( 'NONE', #93357, #47288, #104570, .T. ) ;
#51763=DIRECTION ( 'NONE',  ( -1.000000000000000000, -1.224606353822377258E-16, -0.000000000000000000 ) ) ;
#51780=FACE_OUTER_BOUND ( 'NONE', #34622, .T. ) ;
#51803=CARTESIAN_POINT ( 'NONE',  ( 0.000000000000000000, 0.000000000000000000, 0.000000000000000000 ) ) ;
#51822=CARTESIAN_POINT ( 'NONE',  ( 12.61650669486618881, 1.474610560812782335E-15, 0.000000000000000000 ) ) ;
#51840=ORIENTED_EDGE ( 'NONE', *, *, #56373, .F. ) ;
#51932=CIRCLE ( 'NONE', #3689, 4.000000000000001776 ) ;
#51934=ORIENTED_EDGE ( 'NONE', *, *, #100170, .T. ) ;
#51966=CARTESIAN_POINT ( 'NONE',  ( 18.86650669486618881, -3.999999999999998224, 0.000000000000000000 ) ) ;
#51996=VECTOR ( 'NONE', #35619, 1000.000000000000000 ) ;
#52034=VERTEX_POINT ( 'NONE', #103913 ) ;
#52035=CARTESIAN_POINT ( 'NONE',  ( 38.09999999999998721, 0.000000000000000000, 0.000000000000000000 ) ) ;
#52052=ORIENTED_EDGE ( 'NONE', *, *, #53684, .T. ) ;
#52108=DIRECTION ( 'NONE',  ( 0.000000000000000000, 0.000000000000000000, -1.000000000000000000 ) ) ;
#52156=CARTESIAN_POINT ( 'NONE',  ( 13.09999999999999787, 1.533819458162526451E-15, 0.000000000000000000 ) ) ;
#52192=DIRECTION ( 'NONE',  ( -1.000000000000000000, -1.224606353822377258E-16, -0.000000000000000000 ) ) ;
#52227=VECTOR ( 'NONE', #54246, 1000.000000000000227 ) ;
#52278=EDGE_CURVE ( 'NONE', #63779, #101426, #43969, .T. ) ;
#52294=FACE_OUTER_BOUND ( 'NONE', #85684, .T. ) ;
#52323=ORIENTED_EDGE ( 'NONE', *, *, #49364, .F. ) ;
#52343=VERTEX_POINT ( 'NONE', #53129 ) ;
#52348=EDGE_CURVE ( 'NONE', #36374, #79214, #68247, .T. ) ;
#52354=CARTESIAN_POINT ( 'NONE',  ( 17.33349330513380693, -3.851859888774471706E-31, 4.000000000000001776 ) ) ;
#52370=ORIENTED_EDGE ( 'NONE', *, *, #88622, .T. ) ;
#52372=FACE_OUTER_BOUND ( 'NONE', #18734, .T. ) ;
#52389=VERTEX_POINT ( 'NONE', #1893 ) ;
#52401=ORIENTED_EDGE ( 'NONE', *, *, #22741, .F. ) ;
#52415=CARTESIAN_POINT ( 'NONE',  ( 19.34999999999999787, 3.309500000000003439, 0.000000000000000000 ) ) ;
#52474=ORIENTED_EDGE ( 'NONE', *, *, #18357, .T. ) ;
#52485=DIRECTION ( 'NONE',  ( -1.000000000000000000, -0.000000000000000000, -0.000000000000000000 ) ) ;
#52487=VECTOR ( 'NONE', #13893, 1000.000000000000000 ) ;
#52488=ORIENTED_EDGE ( 'NONE', *, *, #18904, .T. ) ;
#52498=DIRECTION ( 'NONE',  ( -1.000000000000000000, -1.224606353822377258E-16, -0.000000000000000000 ) ) ;
#52526=ORIENTED_EDGE ( 'NONE', *, *, #46194, .F. ) ;
#52566=AXIS2_PLACEMENT_3D ( 'NONE', #85283, #6875, #65655 ) ;
#52596=DIRECTION ( 'NONE',  ( 0.000000000000000000, -1.000000000000000000, 0.000000000000000000 ) ) ;
#52648=AXIS2_PLACEMENT_3D ( 'NONE', #73576, #81143, #89787 ) ;
#52669=CARTESIAN_POINT ( 'NONE',  ( 22.61650669486618526, 4.898587196589413815E-16, -4.000000000000000888 ) ) ;
#52670=ADVANCED_FACE ( 'NONE', ( #54424 ), #45378, .T. ) ;
#52685=CARTESIAN_POINT ( 'NONE',  ( 0.000000000000000000, 0.000000000000000000, 0.000000000000000000 ) ) ;
#52713=EDGE_LOOP ( 'NONE', ( #27066, #78260, #61847, #87138, #105391, #75776 ) ) ;
#52738=ORIENTED_EDGE ( 'NONE', *, *, #49904, .F. ) ;
#52739=EDGE_CURVE ( 'NONE', #4006, #66536, #55724, .T. ) ;
#52806=EDGE_CURVE ( 'NONE', #49640, #77164, #78077, .T. ) ;
#52832=CARTESIAN_POINT ( 'NONE',  ( 6.222742520105473574, 7.673830019007162662, 0.2914634815676395707 ) ) ;
#52841=CONICAL_SURFACE ( 'NONE', #66625, 4.000000000000001776, 0.9599310885968774798 ) ;
#52854=EDGE_LOOP ( 'NONE', ( #92891, #40375, #67760, #47181, #93222, #104250 ) ) ;
#52858=CARTESIAN_POINT ( 'NONE',  ( 0.000000000000000000, 0.000000000000000000, 4.000000000000000888 ) ) ;
#52899=CIRCLE ( 'NONE', #32285, 4.000000000000001776 ) ;
#52912=CARTESIAN_POINT ( 'NONE',  ( 6.162888688655347558, 7.505553499465140277, 0.000000000000000000 ) ) ;
#52927=EDGE_LOOP ( 'NONE', ( #43273, #88087, #53349, #51840, #102029 ) ) ;
#52945=DIRECTION ( 'NONE',  ( 0.000000000000000000, -1.000000000000000000, 0.000000000000000000 ) ) ;
#52972=EDGE_LOOP ( 'NONE', ( #21463, #33623, #72358, #78436, #49990, #86068 ) ) ;
#52976=VECTOR ( 'NONE', #34494, 1000.000000000000000 ) ;
#52984=MANIFOLD_SOLID_BREP ( 'ThdSchPat', #104913 ) ;
#53005=CYLINDRICAL_SURFACE ( 'NONE', #44199, 4.000000000000000888 ) ;
#53030=EDGE_CURVE ( 'NONE', #45061, #876, #17894, .T. ) ;
#53055=DIRECTION ( 'NONE',  ( 0.000000000000000000, -1.000000000000000000, 0.000000000000000000 ) ) ;
#53090=( LENGTH_UNIT ( ) NAMED_UNIT ( * ) SI_UNIT ( .MILLI., .METRE. ) );
#53097=DIRECTION ( 'NONE',  ( 0.000000000000000000, -1.000000000000000000, 0.000000000000000000 ) ) ;
#53122=CARTESIAN_POINT ( 'NONE',  ( 10.59999999999999609, -3.309499999999999886, 0.000000000000000000 ) ) ;
#53129=CARTESIAN_POINT ( 'NONE',  ( 10.59999999999999609, -3.309499999999999886, 4.475777889183790779E-16 ) ) ;
#53134=VERTEX_POINT ( 'NONE', #74086 ) ;
#53136=CARTESIAN_POINT ( 'NONE',  ( 10.59999999999999609, 3.309500000000003439, 4.052968581778167743E-16 ) ) ;
#53140=ORIENTED_EDGE ( 'NONE', *, *, #97311, .T. ) ;
#53150=ORIENTED_EDGE ( 'NONE', *, *, #8152, .F. ) ;
#53194=ORIENTED_EDGE ( 'NONE', *, *, #20351, .T. ) ;
#53197=ORIENTED_EDGE ( 'NONE', *, *, #29125, .T. ) ;
#53219=EDGE_CURVE ( 'NONE', #24036, #6482, #95183, .T. ) ;
#53276=ORIENTED_EDGE ( 'NONE', *, *, #70438, .T. ) ;
#53286=CONICAL_SURFACE ( 'NONE', #80908, 4.000000000000001776, 0.9599310885968774798 ) ;
#53295=DIRECTION ( 'NONE',  ( 0.5735764363510491570, -0.8191520442889895781, 1.003171929053522035E-16 ) ) ;
#53298=EDGE_LOOP ( 'NONE', ( #12329, #40246, #72977, #60482, #33386 ) ) ;
#53322=EDGE_CURVE ( 'NONE', #37979, #47288, #5623, .T. ) ;
#53349=ORIENTED_EDGE ( 'NONE', *, *, #45847, .T. ) ;
#53358=( BOUNDED_SURFACE ( )  B_SPLINE_SURFACE ( 3, 2, ( 
 ( #104579, #87357, #30735 ),
 ( #71672, #102471, #4302 ),
 ( #37239, #5372, #54414 ),
 ( #63621, #70099, #62037 ),
 ( #96509, #38292, #55478 ),
 ( #104048, #95975, #88415 ) ),
 .UNSPECIFIED., .F., .F., .F. ) 
 B_SPLINE_SURFACE_WITH_KNOTS ( ( 4, 2, 4 ),
 ( 3, 3 ),
 ( 0.003199762745115999809, 0.007302762474435751071, 0.01140576220375550190 ),
 ( 0.000000000000000000, 1.000000000000000000 ),
 .UNSPECIFIED. ) 
 GEOMETRIC_REPRESENTATION_ITEM ( )  RATIONAL_B_SPLINE_SURFACE ( (
 ( 1.000000000000000000, 0.8047731410850422762, 1.000000000000000000),
 ( 1.000000000000000000, 0.8125552299159720659, 1.000000000000000000),
 ( 1.000000000000000000, 0.8191520442885290576, 1.000000000000000000),
 ( 1.000000000000000000, 0.8191520442894507648, 1.000000000000000000),
 ( 1.000000000000000000, 0.8125552299152799529, 1.000000000000000000),
 ( 1.000000000000000000, 0.8047731410850428313, 1.000000000000000000) ) ) 
 REPRESENTATION_ITEM ( '' )  SURFACE ( )  );
#53381=LINE ( 'NONE', #86300, #568 ) ;
#53390=DIRECTION ( 'NONE',  ( 0.000000000000000000, -1.000000000000000000, 0.000000000000000000 ) ) ;
#53398=CARTESIAN_POINT ( 'NONE',  ( 25.59999999999999787, 1.533819458162526451E-15, 0.000000000000000000 ) ) ;
#53467=LINE ( 'NONE', #86387, #22946 ) ;
#53478=CARTESIAN_POINT ( 'NONE',  ( 6.162888688655344893, -3.752776749732565253, 6.499999999999999112 ) ) ;
#53522=CARTESIAN_POINT ( 'NONE',  ( 26.08349330513380693, 1.593028355512270962E-15, 0.000000000000000000 ) ) ;
#53611=CONICAL_SURFACE ( 'NONE', #101880, 4.000000000000001776, 0.9599310885968774798 ) ;
#53615=AXIS2_PLACEMENT_3D ( 'NONE', #5332, #38255, #54919 ) ;
#53641=CARTESIAN_POINT ( 'NONE',  ( 37.33349330513379982, 1.593028355512270962E-15, 0.000000000000000000 ) ) ;
#53645=DIRECTION ( 'NONE',  ( 0.000000000000000000, -1.000000000000000000, 0.000000000000000000 ) ) ;
#53684=EDGE_CURVE ( 'NONE', #92773, #90141, #36699, .T. ) ;
#53744=LINE ( 'NONE', #95281, #52227 ) ;
#53762=AXIS2_PLACEMENT_3D ( 'NONE', #14943, #47837, #6859 ) ;
#53765=CARTESIAN_POINT ( 'NONE',  ( 20.59999999999999787, 1.533819458162526451E-15, 0.000000000000000000 ) ) ;
#53853=EDGE_LOOP ( 'NONE', ( #90868, #11194, #15228, #82251, #49416, #38246 ) ) ;
#53908=CARTESIAN_POINT ( 'NONE',  ( 20.11650669486618881, 1.474610560812782335E-15, 0.000000000000000000 ) ) ;
#53922=CARTESIAN_POINT ( 'NONE',  ( 15.11650669486618881, 1.474610560812782335E-15, 0.000000000000000000 ) ) ;
#53964=AXIS2_PLACEMENT_3D ( 'NONE', #53398, #77676, #86319 ) ;
#53972=ORIENTED_EDGE ( 'NONE', *, *, #35771, .T. ) ;
#53974=DIRECTION ( 'NONE',  ( -1.000000000000000000, -0.000000000000000000, -0.000000000000000000 ) ) ;
#53976=CARTESIAN_POINT ( 'NONE',  ( 29.83349330513380693, 1.593028355512270962E-15, 0.000000000000000000 ) ) ;
#53977=FACE_OUTER_BOUND ( 'NONE', #5489, .T. ) ;
#54014=EDGE_CURVE ( 'NONE', #89753, #24036, #12816, .T. ) ;
#54029=CONICAL_SURFACE ( 'NONE', #33364, 3.309500000000001663, 0.9599310885968770357 ) ;
#54051=ORIENTED_EDGE ( 'NONE', *, *, #18641, .T. ) ;
#54063=DIRECTION ( 'NONE',  ( 0.000000000000000000, -1.000000000000000000, 0.000000000000000000 ) ) ;
#54073=CARTESIAN_POINT ( 'NONE',  ( 22.33349330513380693, 1.593028355512270962E-15, 0.000000000000000000 ) ) ;
#54082=DIRECTION ( 'NONE',  ( 0.000000000000000000, -1.000000000000000000, 0.000000000000000000 ) ) ;
#54122=EDGE_CURVE ( 'NONE', #47288, #80922, #33286, .T. ) ;
#54129=B_SPLINE_CURVE_WITH_KNOTS ( 'NONE', 3,
 ( #24755, #49525, #17187, #65724, #89474, #25294, #100210, #8002 ),
 .UNSPECIFIED., .F., .F.,
 ( 4, 2, 2, 4 ),
 ( 0.003797433802554453248, 0.004743183970586247432, 0.005688934138618042050, 0.007580434474681629550 ),
 .UNSPECIFIED. ) ;
#54156=EDGE_LOOP ( 'NONE', ( #12165, #30763, #62380, #41329, #47390 ) ) ;
#54166=DIRECTION ( 'NONE',  ( -1.000000000000000000, -1.224606353822377258E-16, -0.000000000000000000 ) ) ;
#54189=DIRECTION ( 'NONE',  ( -1.000000000000000000, -1.224606353822377258E-16, -0.000000000000000000 ) ) ;
#54197=DIRECTION ( 'NONE',  ( -0.5735764363510494901, -0.8191520442889894671, 0.000000000000000000 ) ) ;
#54218=CIRCLE ( 'NONE', #71475, 4.000000000000000888 ) ;
#54243=AXIS2_PLACEMENT_3D ( 'NONE', #80493, #62751, #48655 ) ;
#54246=DIRECTION ( 'NONE',  ( 0.5735764363510491570, -0.8191520442889895781, 1.003171929053522035E-16 ) ) ;
#54261=CARTESIAN_POINT ( 'NONE',  ( 5.947762761376474749, -2.501851166488376688, 6.500000000000000000 ) ) ;
#54288=DIRECTION ( 'NONE',  ( -1.000000000000000000, -1.224606353822377258E-16, -0.000000000000000000 ) ) ;
#54303=CARTESIAN_POINT ( 'NONE',  ( 21.08349330513380693, 1.593028355512270962E-15, 0.000000000000000000 ) ) ;
#54304=CARTESIAN_POINT ( 'NONE',  ( 27.33349330513380693, 1.593028355512270962E-15, 0.000000000000000000 ) ) ;
#54339=VERTEX_POINT ( 'NONE', #100646 ) ;
#54413=ADVANCED_FACE ( 'NONE', ( #30373 ), #29330, .T. ) ;
#54414=CARTESIAN_POINT ( 'NONE',  ( 6.289692432696588398, 5.239086202714920759, 4.583616368337912306 ) ) ;
#54423=VERTEX_POINT ( 'NONE', #78893 ) ;
#54424=FACE_OUTER_BOUND ( 'NONE', #80495, .T. ) ;
#54425=EDGE_CURVE ( 'NONE', #55271, #63533, #62220, .T. ) ;
#54443=ORIENTED_EDGE ( 'NONE', *, *, #52806, .F. ) ;
#54448=ORIENTED_EDGE ( 'NONE', *, *, #19349, .T. ) ;
#54488=ORIENTED_EDGE ( 'NONE', *, *, #58723, .T. ) ;
#54497=CARTESIAN_POINT ( 'NONE',  ( 5.947762761376473861, -4.378239541354662201, 5.416666666666666963 ) ) ;
#54503=CARTESIAN_POINT ( 'NONE',  ( 6.575925811255158848, -3.850887307289502459, 6.669932470447524686 ) ) ;
#54559=EDGE_CURVE ( 'NONE', #90625, #68858, #60432, .T. ) ;
#54562=ORIENTED_EDGE ( 'NONE', *, *, #79405, .T. ) ;
#54573=VERTEX_POINT ( 'NONE', #85209 ) ;
#54579=CARTESIAN_POINT ( 'NONE',  ( 15.11650669486618881, 1.474610560812782335E-15, 0.000000000000000000 ) ) ;
#54589=AXIS2_PLACEMENT_3D ( 'NONE', #19159, #10997, #36923 ) ;
#54618=EDGE_CURVE ( 'NONE', #62868, #8297, #53381, .T. ) ;
#54635=VECTOR ( 'NONE', #62291, 1000.000000000000000 ) ;
#54687=CARTESIAN_POINT ( 'NONE',  ( 32.33349330513380693, 1.593028355512270962E-15, 0.000000000000000000 ) ) ;
#54708=ORIENTED_EDGE ( 'NONE', *, *, #12450, .T. ) ;
#54732=DIRECTION ( 'NONE',  ( 1.000000000000000000, 1.224606353822377258E-16, 0.000000000000000000 ) ) ;
#54741=ORIENTED_EDGE ( 'NONE', *, *, #63229, .F. ) ;
#54767=ORIENTED_EDGE ( 'NONE', *, *, #50152, .F. ) ;
#54779=AXIS2_PLACEMENT_3D ( 'NONE', #41544, #74957, #100834 ) ;
#54780=EDGE_LOOP ( 'NONE', ( #85695, #74139, #80881, #68255, #29365, #89290 ) ) ;
#54831=CONICAL_SURFACE ( 'NONE', #22153, 3.309500000000001663, 0.9599310885968770357 ) ;
#54833=VECTOR ( 'NONE', #55283, 1000.000000000000000 ) ;
#54866=ORIENTED_EDGE ( 'NONE', *, *, #7740, .F. ) ;
#54889=ORIENTED_EDGE ( 'NONE', *, *, #88197, .F. ) ;
#54919=DIRECTION ( 'NONE',  ( 0.000000000000000000, -1.000000000000000000, 0.000000000000000000 ) ) ;
#54921=ORIENTED_EDGE ( 'NONE', *, *, #66094, .F. ) ;
#54987=ORIENTED_EDGE ( 'NONE', *, *, #60017, .F. ) ;
#55008=CIRCLE ( 'NONE', #32662, 4.000000000000000888 ) ;
#55049=CARTESIAN_POINT ( 'NONE',  ( 12.33349330513380693, 1.593028355512270962E-15, 0.000000000000000000 ) ) ;
#55077=ORIENTED_EDGE ( 'NONE', *, *, #99242, .F. ) ;
#55085=DIRECTION ( 'NONE',  ( 0.000000000000000000, -1.000000000000000000, 0.000000000000000000 ) ) ;
#55089=CARTESIAN_POINT ( 'NONE',  ( 6.463178677061750754, 2.643201791673480905, 6.839998497243177766 ) ) ;
#55141=CARTESIAN_POINT ( 'NONE',  ( 6.333820801329765438, -4.275724398228747170, 5.594228103109105454 ) ) ;
#55178=DIRECTION ( 'NONE',  ( 0.5735764363510490460, 0.8191520442889896891, 0.000000000000000000 ) ) ;
#55186=ORIENTED_EDGE ( 'NONE', *, *, #718, .T. ) ;
#55205=AXIS2_PLACEMENT_3D ( 'NONE', #26704, #34791, #2900 ) ;
#55218=EDGE_CURVE ( 'NONE', #59988, #46183, #28303, .T. ) ;
#55223=DIRECTION ( 'NONE',  ( -1.000000000000000000, -1.224606353822377258E-16, -0.000000000000000000 ) ) ;
#55255=CARTESIAN_POINT ( 'NONE',  ( 35.59999999999999432, 1.533819458162526451E-15, 0.000000000000000000 ) ) ;
#55258=DIRECTION ( 'NONE',  ( 0.000000000000000000, 1.000000000000000000, -2.311253228826401127E-16 ) ) ;
#55271=VERTEX_POINT ( 'NONE', #90655 ) ;
#55283=DIRECTION ( 'NONE',  ( -1.000000000000000000, -0.000000000000000000, -0.000000000000000000 ) ) ;
#55304=DIRECTION ( 'NONE',  ( 0.000000000000000000, 0.000000000000000000, 1.000000000000000000 ) ) ;
#55347=CIRCLE ( 'NONE', #64016, 6.500000000000000888 ) ;
#55358=CARTESIAN_POINT ( 'NONE',  ( 0.2565376335216150161, -2.516992571280034952, -6.500000000000001776 ) ) ;
#55372=CARTESIAN_POINT ( 'NONE',  ( 30.11650669486618881, -3.999999999999998224, 0.000000000000000000 ) ) ;
#55380=ORIENTED_EDGE ( 'NONE', *, *, #103836, .T. ) ;
#55410=EDGE_CURVE ( 'NONE', #22594, #88800, #105772, .T. ) ;
#55429=AXIS2_PLACEMENT_3D ( 'NONE', #21680, #45407, #46455 ) ;
#55436=VERTEX_POINT ( 'NONE', #77128 ) ;
#55470=DIRECTION ( 'NONE',  ( -1.000000000000000000, -0.000000000000000000, -0.000000000000000000 ) ) ;
#55477=EDGE_LOOP ( 'NONE', ( #73694, #66604, #47477, #76132, #70510 ) ) ;
#55478=CARTESIAN_POINT ( 'NONE',  ( 6.445370176741849200, 7.262437273738760801, 1.101027156348632685 ) ) ;
#55537=ORIENTED_EDGE ( 'NONE', *, *, #84423, .T. ) ;
#55608=DIRECTION ( 'NONE',  ( -1.000000000000000000, -0.000000000000000000, -0.000000000000000000 ) ) ;
#55640=LINE ( 'NONE', #47036, #55779 ) ;
#55679=VERTEX_POINT ( 'NONE', #13841 ) ;
#55703=CARTESIAN_POINT ( 'NONE',  ( 6.289572920342628493, -5.584521518880464441, -3.985288806461544375 ) ) ;
#55708=CARTESIAN_POINT ( 'NONE',  ( 16.84999999999999787, 1.533819458162526451E-15, 0.000000000000000000 ) ) ;
#55724=CIRCLE ( 'NONE', #85023, 4.000000000000001776 ) ;
#55727=CARTESIAN_POINT ( 'NONE',  ( 11.84999999999999787, 1.533819458162526451E-15, 0.000000000000000000 ) ) ;
#55751=AXIS2_PLACEMENT_3D ( 'NONE', #99769, #66884, #32411 ) ;
#55753=EDGE_CURVE ( 'NONE', #61515, #21783, #9371, .T. ) ;
#55775=CARTESIAN_POINT ( 'NONE',  ( 8.099999999999999645, 3.752776749732565253, 6.499999999999997335 ) ) ;
#55778=CARTESIAN_POINT ( 'NONE',  ( 33.86650669486618881, 1.474610560812782335E-15, 0.000000000000000000 ) ) ;
#55779=VECTOR ( 'NONE', #56166, 1000.000000000000000 ) ;
#55787=ORIENTED_EDGE ( 'NONE', *, *, #79121, .F. ) ;
#55806=DIRECTION ( 'NONE',  ( 0.000000000000000000, 0.000000000000000000, 1.000000000000000000 ) ) ;
#55808=DIRECTION ( 'NONE',  ( 0.000000000000000000, 0.000000000000000000, 1.000000000000000000 ) ) ;
#55817=CARTESIAN_POINT ( 'NONE',  ( 0.000000000000000000, 0.000000000000000000, 0.000000000000000000 ) ) ;
#55858=AXIS2_PLACEMENT_3D ( 'NONE', #95746, #87663, #13744 ) ;
#55874=EDGE_CURVE ( 'NONE', #16503, #90846, #98983, .T. ) ;
#55894=ORIENTED_EDGE ( 'NONE', *, *, #37845, .T. ) ;
#55913=DIRECTION ( 'NONE',  ( -1.000000000000000000, -1.224606353822377258E-16, -0.000000000000000000 ) ) ;
#55915=CARTESIAN_POINT ( 'NONE',  ( 19.34999999999999787, 1.533819458162526451E-15, 0.000000000000000000 ) ) ;
#55924=EDGE_CURVE ( 'NONE', #74451, #53134, #36997, .T. ) ;
#55938=FACE_OUTER_BOUND ( 'NONE', #23234, .T. ) ;
#55949=VECTOR ( 'NONE', #18060, 1000.000000000000000 ) ;
#55955=CARTESIAN_POINT ( 'NONE',  ( 0.000000000000000000, 0.000000000000000000, 4.000000000000000888 ) ) ;
#55977=AXIS2_PLACEMENT_3D ( 'NONE', #18367, #16746, #27005 ) ;
#55996=ORIENTED_EDGE ( 'NONE', *, *, #90778, .F. ) ;
#55998=AXIS2_PLACEMENT_3D ( 'NONE', #62363, #62888, #61294 ) ;
#56020=CIRCLE ( 'NONE', #6085, 4.000000000000000888 ) ;
#56030=CARTESIAN_POINT ( 'NONE',  ( 6.936184427528457874, 0.000000000000000000, -8.605212085995399107 ) ) ;
#56052=DIRECTION ( 'NONE',  ( -1.000000000000000000, -1.224606353822377258E-16, -0.000000000000000000 ) ) ;
#56108=CARTESIAN_POINT ( 'NONE',  ( 0.000000000000000000, 0.000000000000000000, 0.000000000000000000 ) ) ;
#56166=DIRECTION ( 'NONE',  ( -1.000000000000000000, -0.000000000000000000, -0.000000000000000000 ) ) ;
#56180=VERTEX_POINT ( 'NONE', #105786 ) ;
#56182=AXIS2_PLACEMENT_3D ( 'NONE', #95518, #53974, #78787 ) ;
#56185=VERTEX_POINT ( 'NONE', #64801 ) ;
#56201=AXIS2_PLACEMENT_3D ( 'NONE', #18553, #78348, #84329 ) ;
#56233=ORIENTED_EDGE ( 'NONE', *, *, #17612, .T. ) ;
#56240=ORIENTED_EDGE ( 'NONE', *, *, #93282, .T. ) ;
#56247=DIRECTION ( 'NONE',  ( 0.000000000000000000, 0.000000000000000000, 1.000000000000000000 ) ) ;
#56271=AXIS2_PLACEMENT_3D ( 'NONE', #42798, #24529, #8830 ) ;
#56282=DIRECTION ( 'NONE',  ( -1.000000000000000000, -1.224606353822377258E-16, -0.000000000000000000 ) ) ;
#56289=CARTESIAN_POINT ( 'NONE',  ( 0.4033376246892507178, 7.198601258566903027, -0.5316568767328684331 ) ) ;
#56300=CONICAL_SURFACE ( 'NONE', #89052, 4.000000000000001776, 0.9599310885968774798 ) ;
#56308=DIRECTION ( 'NONE',  ( -1.000000000000000000, -1.224606353822377258E-16, -0.000000000000000000 ) ) ;
#56311=CARTESIAN_POINT ( 'NONE',  ( -9.948401965501753538E-16, 0.6351314446025491112, 6.499999999999998224 ) ) ;
#56320=ORIENTED_EDGE ( 'NONE', *, *, #44240, .T. ) ;
#56332=CARTESIAN_POINT ( 'NONE',  ( 6.162888688655347558, -7.505553499465142053, -3.129864801432410934E-16 ) ) ;
#56334=ADVANCED_FACE ( 'NONE', ( #1091 ), #16391, .T. ) ;
#56352=ORIENTED_EDGE ( 'NONE', *, *, #91917, .F. ) ;
#56364=CARTESIAN_POINT ( 'NONE',  ( 6.683837171061806082, -3.955946848495971668, -6.851900933636991375 ) ) ;
#56373=EDGE_CURVE ( 'NONE', #90846, #98221, #20211, .T. ) ;
#56384=CARTESIAN_POINT ( 'NONE',  ( 37.33349330513379982, 1.593028355512270962E-15, 0.000000000000000000 ) ) ;
#56397=CIRCLE ( 'NONE', #21964, 4.000000000000001776 ) ;
#56418=DIRECTION ( 'NONE',  ( -1.000000000000000000, -0.000000000000000000, -0.000000000000000000 ) ) ;
#56489=CARTESIAN_POINT ( 'NONE',  ( 0.000000000000000000, 0.000000000000000000, 0.000000000000000000 ) ) ;
#56496=CARTESIAN_POINT ( 'NONE',  ( 31.08349330513380693, 1.593028355512270962E-15, 0.000000000000000000 ) ) ;
#56545=EDGE_CURVE ( 'NONE', #40430, #81794, #90535, .T. ) ;
#56548=CARTESIAN_POINT ( 'NONE',  ( 0.4037800551813721661, 4.058962678540097180, -5.969670414742690667 ) ) ;
#56560=ORIENTED_EDGE ( 'NONE', *, *, #87664, .F. ) ;
#56574=CIRCLE ( 'NONE', #72147, 3.309500000000001663 ) ;
#56581=CIRCLE ( 'NONE', #61870, 4.000000000000001776 ) ;
#56583=ORIENTED_EDGE ( 'NONE', *, *, #77116, .T. ) ;
#56589=ADVANCED_FACE ( 'NONE', ( #92667 ), #92212, .T. ) ;
#56636=AXIS2_PLACEMENT_3D ( 'NONE', #73749, #98032, #40327 ) ;
#56675=EDGE_CURVE ( 'NONE', #3039, #36200, #59527, .T. ) ;
#56703=ORIENTED_EDGE ( 'NONE', *, *, #84430, .F. ) ;
#56725=DIRECTION ( 'NONE',  ( -0.5735764363510497121, 0.8191520442889892450, 1.003171929053521665E-16 ) ) ;
#56746=FACE_OUTER_BOUND ( 'NONE', #103320, .T. ) ;
#56749=EDGE_CURVE ( 'NONE', #54573, #15029, #45736, .T. ) ;
#56772=CARTESIAN_POINT ( 'NONE',  ( 15.11650669486618881, 1.474610560812782335E-15, 0.000000000000000000 ) ) ;
#56780=EDGE_LOOP ( 'NONE', ( #15392, #72636, #38489, #35815, #54741, #103393 ) ) ;
#56838=EDGE_LOOP ( 'NONE', ( #47317, #105443, #41394, #72623, #2582, #40058 ) ) ;
#56860=DIRECTION ( 'NONE',  ( 0.000000000000000000, -1.000000000000000000, 0.000000000000000000 ) ) ;
#56906=CIRCLE ( 'NONE', #105120, 4.000000000000001776 ) ;
#56908=CARTESIAN_POINT ( 'NONE',  ( 17.33349330513380693, 4.000000000000002665, 0.000000000000000000 ) ) ;
#56919=DIRECTION ( 'NONE',  ( -0.7071067811865555663, 0.000000000000000000, 0.7071067811865393571 ) ) ;
#56967=VECTOR ( 'NONE', #49244, 1000.000000000000341 ) ;
#56988=DIRECTION ( 'NONE',  ( 0.000000000000000000, -1.000000000000000000, 0.000000000000000000 ) ) ;
#57024=CARTESIAN_POINT ( 'NONE',  ( 0.5805565836007650082, -3.752776749732574135, -6.500000000000001776 ) ) ;
#57033=DIRECTION ( 'NONE',  ( 0.000000000000000000, 0.000000000000000000, 1.000000000000000000 ) ) ;
#57069=ORIENTED_EDGE ( 'NONE', *, *, #51719, .T. ) ;
#57080=LINE ( 'NONE', #106697, #20805 ) ;
#57085=ORIENTED_EDGE ( 'NONE', *, *, #77436, .T. ) ;
#57098=CARTESIAN_POINT ( 'NONE',  ( 25.11650669486618881, 1.474610560812782335E-15, 0.000000000000000000 ) ) ;
#57100=FACE_OUTER_BOUND ( 'NONE', #85535, .T. ) ;
#57106=LINE ( 'NONE', #47425, #95939 ) ;
#57110=DIRECTION ( 'NONE',  ( -1.000000000000000000, -1.224606353822377258E-16, -0.000000000000000000 ) ) ;
#57120=DIRECTION ( 'NONE',  ( -1.000000000000000000, -1.224606353822377258E-16, -0.000000000000000000 ) ) ;
#57153=ORIENTED_EDGE ( 'NONE', *, *, #83019, .F. ) ;
#57166=AXIS2_PLACEMENT_3D ( 'NONE', #16966, #49842, #15889 ) ;
#57171=ORIENTED_EDGE ( 'NONE', *, *, #60362, .F. ) ;
#57199=CARTESIAN_POINT ( 'NONE',  ( 0.000000000000000000, 0.000000000000000000, 0.000000000000000000 ) ) ;
#57224=AXIS2_PLACEMENT_3D ( 'NONE', #34114, #65382, #49173 ) ;
#57258=DIRECTION ( 'NONE',  ( 0.000000000000000000, 0.000000000000000000, 1.000000000000000000 ) ) ;
#57268=CARTESIAN_POINT ( 'NONE',  ( 6.563035550597770218, 3.302680408004402768, -6.845819698387222374 ) ) ;
#57291=EDGE_CURVE ( 'NONE', #87062, #87964, #26905, .T. ) ;
#57313=EDGE_CURVE ( 'NONE', #99443, #4316, #85470, .T. ) ;
#57319=CYLINDRICAL_SURFACE ( 'NONE', #92992, 4.000000000000000888 ) ;
#57327=DIRECTION ( 'NONE',  ( 0.000000000000000000, -1.000000000000000000, 0.000000000000000000 ) ) ;
#57359=CARTESIAN_POINT ( 'NONE',  ( 0.000000000000000000, 0.000000000000000000, 4.000000000000000888 ) ) ;
#57372=CARTESIAN_POINT ( 'NONE',  ( 24.34999999999999787, -3.309499999999999886, 0.000000000000000000 ) ) ;
#57385=( GEOMETRIC_REPRESENTATION_CONTEXT ( 3 ) GLOBAL_UNCERTAINTY_ASSIGNED_CONTEXT ( ( #51351 ) ) GLOBAL_UNIT_ASSIGNED_CONTEXT ( ( #53090, #69289, #11545 ) ) REPRESENTATION_CONTEXT ( 'NONE', 'WORKASPACE' ) );
#57389=CONICAL_SURFACE ( 'NONE', #84973, 4.000000000000001776, 0.9599310885968774798 ) ;
#57423=DIRECTION ( 'NONE',  ( 1.000000000000000000, 1.224606353822377258E-16, 0.000000000000000000 ) ) ;
#57427=MECHANICAL_DESIGN_GEOMETRIC_PRESENTATION_REPRESENTATION('',(#43665),#24823);
#57440=DIRECTION ( 'NONE',  ( -1.000000000000000000, -1.224606353822377258E-16, -0.000000000000000000 ) ) ;
#57483=LINE ( 'NONE', #75814, #34194 ) ;
#57544=EDGE_LOOP ( 'NONE', ( #58049, #33918, #102739, #72803, #27659 ) ) ;
#57553=CIRCLE ( 'NONE', #50688, 3.309500000000001663 ) ;
#57561=DIRECTION ( 'NONE',  ( 0.000000000000000000, 0.000000000000000000, 1.000000000000000000 ) ) ;
#57590=EDGE_CURVE ( 'NONE', #26910, #16434, #30433, .T. ) ;
#57591=ORIENTED_EDGE ( 'NONE', *, *, #69650, .F. ) ;
#57592=CARTESIAN_POINT ( 'NONE',  ( 6.333820801330004358, -4.275724398228958556, -5.594228103109302630 ) ) ;
#57614=EDGE_LOOP ( 'NONE', ( #1199, #46086, #19097, #85014, #100135 ) ) ;
#57650=CARTESIAN_POINT ( 'NONE',  ( 0.000000000000000000, 0.000000000000000000, 0.000000000000000000 ) ) ;
#57665=ORIENTED_EDGE ( 'NONE', *, *, #105092, .F. ) ;
#57706=DIRECTION ( 'NONE',  ( 1.000000000000000000, 1.224606353822377258E-16, 0.000000000000000000 ) ) ;
#57707=EDGE_CURVE ( 'NONE', #97355, #36385, #104461, .T. ) ;
#57724=( BOUNDED_SURFACE ( )  B_SPLINE_SURFACE ( 3, 2, ( 
 ( #24221, #32836, #104569 ),
 ( #24745, #57592, #90514 ),
 ( #47912, #6932, #16628 ),
 ( #49516, #30722, #47391 ),
 ( #6395, #105628, #51104 ),
 ( #2557, #17704, #10645 ) ),
 .UNSPECIFIED., .F., .F., .F. ) 
 B_SPLINE_SURFACE_WITH_KNOTS ( ( 4, 2, 4 ),
 ( 3, 3 ),
 ( 0.003199762745116009350, 0.007302762474435758877, 0.01140576220375550884 ),
 ( 0.000000000000000000, 1.000000000000000000 ),
 .UNSPECIFIED. ) 
 GEOMETRIC_REPRESENTATION_ITEM ( )  RATIONAL_B_SPLINE_SURFACE ( (
 ( 1.000000000000000000, 0.8047731410850426093, 1.000000000000000000),
 ( 1.000000000000000000, 0.8125552299153956382, 1.000000000000000000),
 ( 1.000000000000000000, 0.8191520442892966658, 1.000000000000000000),
 ( 1.000000000000000000, 0.8191520442886820463, 1.000000000000000000),
 ( 1.000000000000000000, 0.8125552299158568248, 1.000000000000000000),
 ( 1.000000000000000000, 0.8047731410850429423, 1.000000000000000000) ) ) 
 REPRESENTATION_ITEM ( '' )  SURFACE ( )  );
#57732=CARTESIAN_POINT ( 'NONE',  ( 9.833493305133805151, 4.898587196589411843E-16, -4.000000000000001776 ) ) ;
#57770=VERTEX_POINT ( 'NONE', #79232 ) ;
#57773=DIRECTION ( 'NONE',  ( -1.000000000000000000, -1.224606353822377258E-16, -0.000000000000000000 ) ) ;
#57802=CARTESIAN_POINT ( 'NONE',  ( 5.821933341149770236, -1.421180797415668495, 6.499999999999999112 ) ) ;
#57812=ORIENTED_EDGE ( 'NONE', *, *, #99242, .T. ) ;
#57849=FACE_OUTER_BOUND ( 'NONE', #96559, .T. ) ;
#57902=DIRECTION ( 'NONE',  ( -1.000000000000000000, -1.224606353822377258E-16, -0.000000000000000000 ) ) ;
#57928=FACE_OUTER_BOUND ( 'NONE', #18613, .T. ) ;
#57932=LINE ( 'NONE', #76249, #20590 ) ;
#58007=ORIENTED_EDGE ( 'NONE', *, *, #15874, .T. ) ;
#58049=ORIENTED_EDGE ( 'NONE', *, *, #27716, .F. ) ;
#58096=AXIS2_PLACEMENT_3D ( 'NONE', #85868, #3332, #45396 ) ;
#58107=CIRCLE ( 'NONE', #11592, 3.309500000000001663 ) ;
#58109=CARTESIAN_POINT ( 'NONE',  ( 38.09999999999998721, 0.000000000000000000, 0.000000000000000000 ) ) ;
#58123=DIRECTION ( 'NONE',  ( 0.000000000000000000, -1.000000000000000000, 0.000000000000000000 ) ) ;
#58139=DIRECTION ( 'NONE',  ( -1.000000000000000000, -1.224606353822377258E-16, -0.000000000000000000 ) ) ;
#58156=ORIENTED_EDGE ( 'NONE', *, *, #35771, .F. ) ;
#58186=ORIENTED_EDGE ( 'NONE', *, *, #39843, .F. ) ;
#58254=EDGE_CURVE ( 'NONE', #64296, #32377, #84557, .T. ) ;
#58267=AXIS2_PLACEMENT_3D ( 'NONE', #56772, #75076, #90757 ) ;
#58348=CARTESIAN_POINT ( 'NONE',  ( 25.11650669486618881, -3.999999999999998224, 0.000000000000000000 ) ) ;
#58354=CARTESIAN_POINT ( 'NONE',  ( 19.83349330513380693, -4.000000000000000888, 4.898587196589416773E-16 ) ) ;
#58361=DIRECTION ( 'NONE',  ( 0.000000000000000000, 1.000000000000000000, 0.000000000000000000 ) ) ;
#58379=CIRCLE ( 'NONE', #11863, 4.000000000000000888 ) ;
#58390=ADVANCED_FACE ( 'NONE', ( #86697 ), #35681, .T. ) ;
#58405=VECTOR ( 'NONE', #61081, 1000.000000000000000 ) ;
#58413=EDGE_CURVE ( 'NONE', #61003, #44704, #19866, .T. ) ;
#58441=CONICAL_SURFACE ( 'NONE', #60169, 3.309500000000001663, 0.9599310885968770357 ) ;
#58456=EDGE_CURVE ( 'NONE', #60761, #39211, #90773, .T. ) ;
#58465=DIRECTION ( 'NONE',  ( 0.000000000000000000, 1.000000000000000000, 0.000000000000000000 ) ) ;
#58466=DIRECTION ( 'NONE',  ( -1.000000000000000000, -0.000000000000000000, -0.000000000000000000 ) ) ;
#58483=CARTESIAN_POINT ( 'NONE',  ( -2.686788508690640676E-15, -5.948846446048903225, 2.696295709017757947 ) ) ;
#58497=DIRECTION ( 'NONE',  ( -1.000000000000000000, -1.224606353822377258E-16, -0.000000000000000000 ) ) ;
#58515=CARTESIAN_POINT ( 'NONE',  ( 31.08349330513380693, 1.593028355512270962E-15, 0.000000000000000000 ) ) ;
#58542=DIRECTION ( 'NONE',  ( 0.000000000000000000, -1.000000000000000000, 0.000000000000000000 ) ) ;
#58544=CARTESIAN_POINT ( 'NONE',  ( 20.11650669486618881, 1.474610560812782335E-15, 0.000000000000000000 ) ) ;
#58547=DIRECTION ( 'NONE',  ( 0.000000000000000000, -1.000000000000000000, 0.000000000000000000 ) ) ;
#58551=ADVANCED_FACE ( 'NONE', ( #8920 ), #99521, .T. ) ;
#58552=ORIENTED_EDGE ( 'NONE', *, *, #100555, .T. ) ;
#58554=DIRECTION ( 'NONE',  ( -1.000000000000000000, -0.000000000000000000, -0.000000000000000000 ) ) ;
#58581=DIRECTION ( 'NONE',  ( -0.5735764363510494901, -0.8191520442889894671, 0.000000000000000000 ) ) ;
#58639=CARTESIAN_POINT ( 'NONE',  ( 6.289692432696804225, 5.239086202715451002, -4.583616368338176095 ) ) ;
#58683=DIRECTION ( 'NONE',  ( 0.000000000000000000, -1.000000000000000000, 0.000000000000000000 ) ) ;
#58692=ORIENTED_EDGE ( 'NONE', *, *, #78401, .T. ) ;
#58720=DIRECTION ( 'NONE',  ( -1.000000000000000000, -1.224606353822377258E-16, -0.000000000000000000 ) ) ;
#58723=EDGE_CURVE ( 'NONE', #52343, #100664, #46613, .T. ) ;
#58737=EDGE_CURVE ( 'NONE', #60770, #19214, #56397, .T. ) ;
#58745=VERTEX_POINT ( 'NONE', #102734 ) ;
#58796=DIRECTION ( 'NONE',  ( 0.000000000000000000, 0.000000000000000000, 1.000000000000000000 ) ) ;
#58801=CARTESIAN_POINT ( 'NONE',  ( 35.11650669486618170, 1.474610560812782335E-15, 0.000000000000000000 ) ) ;
#58808=CONICAL_SURFACE ( 'NONE', #100137, 4.000000000000001776, 0.9599310885968774798 ) ;
#58837=CARTESIAN_POINT ( 'NONE',  ( 25.59999999999999787, 3.309500000000003439, 4.052968581778167743E-16 ) ) ;
#58918=B_SPLINE_CURVE_WITH_KNOTS ( 'NONE', 3,
 ( #44742, #101373, #86272, #85184, #76546 ),
 .UNSPECIFIED., .F., .F.,
 ( 4, 1, 4 ),
 ( 0.000000000000000000, 0.003752776749732570066, 0.007505553499465140131 ),
 .UNSPECIFIED. ) ;
#58942=DIRECTION ( 'NONE',  ( -0.5735764363510497121, 0.8191520442889892450, 1.003171929053521665E-16 ) ) ;
#58950=CARTESIAN_POINT ( 'NONE',  ( 24.83349330513380693, 4.000000000000002665, 0.000000000000000000 ) ) ;
#58993=DIRECTION ( 'NONE',  ( -1.000000000000000000, -0.000000000000000000, -0.000000000000000000 ) ) ;
#59003=CYLINDRICAL_SURFACE ( 'NONE', #69269, 4.000000000000000888 ) ;
#59007=ORIENTED_EDGE ( 'NONE', *, *, #75502, .T. ) ;
#59029=( BOUNDED_SURFACE ( )  B_SPLINE_SURFACE ( 3, 2, ( 
 ( #104772, #80478, #81010 ),
 ( #38470, #37959, #46019 ),
 ( #64331, #71865, #70821 ),
 ( #22825, #103711, #22295 ),
 ( #88072, #55141, #29858 ),
 ( #62736, #97201, #72402 ) ),
 .UNSPECIFIED., .F., .F., .F. ) 
 B_SPLINE_SURFACE_WITH_KNOTS ( ( 4, 2, 4 ),
 ( 3, 3 ),
 ( 0.003199762745115995472, 0.007302762474435748469, 0.01140576220375550190 ),
 ( 0.000000000000000000, 1.000000000000000000 ),
 .UNSPECIFIED. ) 
 GEOMETRIC_REPRESENTATION_ITEM ( )  RATIONAL_B_SPLINE_SURFACE ( (
 ( 1.000000000000000000, 0.8047731410850431644, 1.000000000000000000),
 ( 1.000000000000000000, 0.8125552299162031034, 1.000000000000000000),
 ( 1.000000000000000000, 0.8191520442882217479, 1.000000000000000000),
 ( 1.000000000000000000, 0.8191520442897580745, 1.000000000000000000),
 ( 1.000000000000000000, 0.8125552299150486935, 1.000000000000000000),
 ( 1.000000000000000000, 0.8047731410850426093, 1.000000000000000000) ) ) 
 REPRESENTATION_ITEM ( '' )  SURFACE ( )  );
#59037=FACE_OUTER_BOUND ( 'NONE', #102090, .T. ) ;
#59062=CARTESIAN_POINT ( 'NONE',  ( 16.08349330513380337, -4.000000000000000000, 4.898587196589415787E-16 ) ) ;
#59083=CONICAL_SURFACE ( 'NONE', #12559, 3.309500000000001663, 0.9599310885968770357 ) ;
#59118=ORIENTED_EDGE ( 'NONE', *, *, #64902, .F. ) ;
#59150=CARTESIAN_POINT ( 'NONE',  ( 6.562974947121713143, 7.579827465851454171, 0.5629870116737619723 ) ) ;
#59152=VERTEX_POINT ( 'NONE', #95572 ) ;
#59154=ORIENTED_EDGE ( 'NONE', *, *, #2047, .F. ) ;
#59159=LINE ( 'NONE', #92041, #1315 ) ;
#59167=VERTEX_POINT ( 'NONE', #36056 ) ;
#59173=CARTESIAN_POINT ( 'NONE',  ( 5.975663821521734143, 4.257391242883570293, -5.625982059626840837 ) ) ;
#59197=CARTESIAN_POINT ( 'NONE',  ( 36.84999999999999432, 1.533819458162526451E-15, 0.000000000000000000 ) ) ;
#59214=DIRECTION ( 'NONE',  ( 0.000000000000000000, -1.000000000000000000, 0.000000000000000000 ) ) ;
#59235=DIRECTION ( 'NONE',  ( 0.000000000000000000, 0.000000000000000000, 1.000000000000000000 ) ) ;
#59251=ORIENTED_EDGE ( 'NONE', *, *, #12565, .F. ) ;
#59286=AXIS2_PLACEMENT_3D ( 'NONE', #1134, #17373, #57258 ) ;
#59305=EDGE_CURVE ( 'NONE', #94819, #57770, #33972, .T. ) ;
#59322=FACE_OUTER_BOUND ( 'NONE', #35921, .T. ) ;
#59336=AXIS2_PLACEMENT_3D ( 'NONE', #72178, #88375, #31739 ) ;
#59356=EDGE_CURVE ( 'NONE', #64041, #54339, #2902, .T. ) ;
#59362=VERTEX_POINT ( 'NONE', #27843 ) ;
#59369=CIRCLE ( 'NONE', #50698, 4.000000000000001776 ) ;
#59414=CIRCLE ( 'NONE', #4276, 4.000000000000000888 ) ;
#59435=DIRECTION ( 'NONE',  ( 0.000000000000000000, 1.000000000000000000, 0.000000000000000000 ) ) ;
#59486=EDGE_CURVE ( 'NONE', #96624, #35336, #59747, .T. ) ;
#59489=ADVANCED_FACE ( 'NONE', ( #62827 ), #21857, .F. ) ;
#59503=CIRCLE ( 'NONE', #95681, 4.000000000000001776 ) ;
#59525=ORIENTED_EDGE ( 'NONE', *, *, #45792, .T. ) ;
#59527=CIRCLE ( 'NONE', #69837, 4.000000000000001776 ) ;
#59557=CARTESIAN_POINT ( 'NONE',  ( 7.500000000000001776, 0.000000000000000000, 0.000000000000000000 ) ) ;
#59582=VERTEX_POINT ( 'NONE', #94121 ) ;
#59585=FACE_OUTER_BOUND ( 'NONE', #53298, .T. ) ;
#59592=FACE_OUTER_BOUND ( 'NONE', #98996, .T. ) ;
#59600=DIRECTION ( 'NONE',  ( 0.000000000000000000, 0.000000000000000000, 1.000000000000000000 ) ) ;
#59613=CARTESIAN_POINT ( 'NONE',  ( 12.61650669486618881, 4.000000000000003553, 4.898587196589414801E-16 ) ) ;
#59623=FACE_OUTER_BOUND ( 'NONE', #40952, .T. ) ;
#59625=EDGE_CURVE ( 'NONE', #1485, #84857, #16693, .T. ) ;
#59660=EDGE_LOOP ( 'NONE', ( #86998, #87393, #48456, #71371, #85315 ) ) ;
#59664=EDGE_CURVE ( 'NONE', #30747, #3039, #80419, .T. ) ;
#59670=AXIS2_PLACEMENT_3D ( 'NONE', #61056, #62650, #95532 ) ;
#59683=DIRECTION ( 'NONE',  ( -1.000000000000000000, -1.224606353822377258E-16, -0.000000000000000000 ) ) ;
#59712=ADVANCED_FACE ( 'NONE', ( #96783 ), #14990, .T. ) ;
#59713=CARTESIAN_POINT ( 'NONE',  ( 17.33349330513380693, 1.593028355512270962E-15, 0.000000000000000000 ) ) ;
#59721=ORIENTED_EDGE ( 'NONE', *, *, #58737, .T. ) ;
#59747=CIRCLE ( 'NONE', #101081, 4.000000000000001776 ) ;
#59791=CARTESIAN_POINT ( 'NONE',  ( 37.33349330513379982, -4.000000000000000888, 4.898587196589416773E-16 ) ) ;
#59812=CIRCLE ( 'NONE', #58096, 4.000000000000000888 ) ;
#59816=DIRECTION ( 'NONE',  ( 0.000000000000000000, 0.000000000000000000, 1.000000000000000000 ) ) ;
#59821=CARTESIAN_POINT ( 'NONE',  ( 26.08349330513380693, 4.000000000000003553, 0.000000000000000000 ) ) ;
#59865=CARTESIAN_POINT ( 'NONE',  ( 18.86650669486618881, 1.474610560812782335E-15, 0.000000000000000000 ) ) ;
#59888=AXIS2_PLACEMENT_3D ( 'NONE', #69832, #4035, #19733 ) ;
#59900=CARTESIAN_POINT ( 'NONE',  ( 24.34999999999999787, 1.533819458162526451E-15, 0.000000000000000000 ) ) ;
#59906=DIRECTION ( 'NONE',  ( 1.000000000000000000, 0.000000000000000000, -0.000000000000000000 ) ) ;
#59911=AXIS2_PLACEMENT_3D ( 'NONE', #45839, #95984, #38814 ) ;
#59919=EDGE_LOOP ( 'NONE', ( #59154, #10487, #54708, #29878, #46275 ) ) ;
#59981=LINE ( 'NONE', #92843, #88349 ) ;
#59988=VERTEX_POINT ( 'NONE', #45453 ) ;
#59998=CIRCLE ( 'NONE', #72050, 4.000000000000001776 ) ;
#60016=ORIENTED_EDGE ( 'NONE', *, *, #72214, .F. ) ;
#60017=EDGE_CURVE ( 'NONE', #58745, #55679, #103672, .T. ) ;
#60032=CARTESIAN_POINT ( 'NONE',  ( 18.86650669486618881, 4.898587196589413815E-16, -4.000000000000000888 ) ) ;
#60040=ORIENTED_EDGE ( 'NONE', *, *, #18625, .T. ) ;
#60052=CARTESIAN_POINT ( 'NONE',  ( 24.83349330513380693, 1.593028355512270962E-15, 0.000000000000000000 ) ) ;
#60059=AXIS2_PLACEMENT_3D ( 'NONE', #55778, #56308, #89248 ) ;
#60071=EDGE_LOOP ( 'NONE', ( #99064, #48919, #3812, #58007, #97681, #35642 ) ) ;
#60120=AXIS2_PLACEMENT_3D ( 'NONE', #83182, #24460, #15793 ) ;
#60136=AXIS2_PLACEMENT_3D ( 'NONE', #59557, #35298, #51442 ) ;
#60166=EDGE_CURVE ( 'NONE', #81897, #99736, #23652, .T. ) ;
#60169=AXIS2_PLACEMENT_3D ( 'NONE', #25269, #35491, #90503 ) ;
#60170=CYLINDRICAL_SURFACE ( 'NONE', #20420, 4.000000000000000888 ) ;
#60208=DIRECTION ( 'NONE',  ( 0.000000000000000000, -1.000000000000000000, 0.000000000000000000 ) ) ;
#60218=DIRECTION ( 'NONE',  ( -1.000000000000000000, -0.000000000000000000, 0.000000000000000000 ) ) ;
#60220=ORIENTED_EDGE ( 'NONE', *, *, #25422, .T. ) ;
#60240=DIRECTION ( 'NONE',  ( 1.000000000000000000, 0.000000000000000000, -0.000000000000000000 ) ) ;
#60247=CONICAL_SURFACE ( 'NONE', #32680, 3.309500000000001663, 0.9599310885968770357 ) ;
#60260=ORIENTED_EDGE ( 'NONE', *, *, #58456, .F. ) ;
#60263=DIRECTION ( 'NONE',  ( -1.000000000000000000, -1.224606353822377258E-16, -0.000000000000000000 ) ) ;
#60266=CARTESIAN_POINT ( 'NONE',  ( 14.34999999999999787, 1.533819458162526451E-15, 0.000000000000000000 ) ) ;
#60289=DIRECTION ( 'NONE',  ( 0.000000000000000000, -1.000000000000000000, 0.000000000000000000 ) ) ;
#60295=CIRCLE ( 'NONE', #99908, 8.400000000000000355 ) ;
#60362=EDGE_CURVE ( 'NONE', #16458, #9982, #51232, .T. ) ;
#60393=CARTESIAN_POINT ( 'NONE',  ( 0.000000000000000000, 4.898587196589413815E-16, -4.000000000000000888 ) ) ;
#60406=CIRCLE ( 'NONE', #55205, 4.000000000000000888 ) ;
#60427=CONICAL_SURFACE ( 'NONE', #8650, 4.000000000000001776, 0.9599310885968774798 ) ;
#60432=LINE ( 'NONE', #2687, #35065 ) ;
#60445=CIRCLE ( 'NONE', #8666, 4.000000000000000888 ) ;
#60482=ORIENTED_EDGE ( 'NONE', *, *, #67120, .F. ) ;
#60492=CIRCLE ( 'NONE', #74223, 4.000000000000000888 ) ;
#60558=EDGE_CURVE ( 'NONE', #62868, #83521, #102930, .T. ) ;
#60561=ADVANCED_FACE ( 'NONE', ( #44259 ), #1336, .T. ) ;
#60578=VERTEX_POINT ( 'NONE', #93870 ) ;
#60582=CIRCLE ( 'NONE', #22717, 4.000000000000000888 ) ;
#60587=CARTESIAN_POINT ( 'NONE',  ( 0.000000000000000000, 0.000000000000000000, 0.000000000000000000 ) ) ;
#60599=CARTESIAN_POINT ( 'NONE',  ( 14.83349330513380693, 4.000000000000003553, 0.000000000000000000 ) ) ;
#60601=CARTESIAN_POINT ( 'NONE',  ( 21.36650669486618881, 1.474610560812782335E-15, 0.000000000000000000 ) ) ;
#60638=CIRCLE ( 'NONE', #55429, 3.309500000000001663 ) ;
#60683=ORIENTED_EDGE ( 'NONE', *, *, #28665, .F. ) ;
#60704=CARTESIAN_POINT ( 'NONE',  ( 22.33349330513380693, -4.000000000000000000, 4.898587196589415787E-16 ) ) ;
#60741=DIRECTION ( 'NONE',  ( -1.000000000000000000, -1.224606353822377258E-16, -0.000000000000000000 ) ) ;
#60756=CARTESIAN_POINT ( 'NONE',  ( 22.61650669486618526, -3.999999999999998224, 0.000000000000000000 ) ) ;
#60761=VERTEX_POINT ( 'NONE', #49549 ) ;
#60770=VERTEX_POINT ( 'NONE', #18282 ) ;
#60818=EDGE_CURVE ( 'NONE', #92082, #26910, #59998, .T. ) ;
#60852=DIRECTION ( 'NONE',  ( -1.000000000000000000, -1.224606353822377258E-16, -0.000000000000000000 ) ) ;
#60853=DIRECTION ( 'NONE',  ( 0.000000000000000000, -1.000000000000000000, 0.000000000000000000 ) ) ;
#60927=ADVANCED_FACE ( 'NONE', ( #68953 ), #104766, .T. ) ;
#60961=ORIENTED_EDGE ( 'NONE', *, *, #55410, .F. ) ;
#60968=DIRECTION ( 'NONE',  ( -1.000000000000000000, -0.000000000000000000, -0.000000000000000000 ) ) ;
#60982=CIRCLE ( 'NONE', #48853, 4.000000000000001776 ) ;
#60983=DIRECTION ( 'NONE',  ( -1.000000000000000000, -1.224606353822377258E-16, -0.000000000000000000 ) ) ;
#61003=VERTEX_POINT ( 'NONE', #76481 ) ;
#61009=CYLINDRICAL_SURFACE ( 'NONE', #46467, 4.000000000000000888 ) ;
#61010=DIRECTION ( 'NONE',  ( 0.5735764363510491570, -0.8191520442889895781, 1.003171929053522035E-16 ) ) ;
#61036=ORIENTED_EDGE ( 'NONE', *, *, #87186, .T. ) ;
#61048=DIRECTION ( 'NONE',  ( 0.000000000000000000, -1.000000000000000000, 0.000000000000000000 ) ) ;
#61056=CARTESIAN_POINT ( 'NONE',  ( 28.86650669486618881, 1.474610560812782335E-15, 0.000000000000000000 ) ) ;
#61081=DIRECTION ( 'NONE',  ( -0.5735764363510494901, -0.8191520442889894671, 0.000000000000000000 ) ) ;
#61100=ADVANCED_FACE ( 'NONE', ( #16399 ), #32618, .T. ) ;
#61143=AXIS2_PLACEMENT_3D ( 'NONE', #75549, #51261, #84184 ) ;
#61152=DIRECTION ( 'NONE',  ( -1.000000000000000000, -1.224606353822377258E-16, -0.000000000000000000 ) ) ;
#61159=CIRCLE ( 'NONE', #40422, 3.309500000000001663 ) ;
#61176=EDGE_CURVE ( 'NONE', #71690, #67548, #34193, .T. ) ;
#61190=FILL_AREA_STYLE ('',( #102163 ) ) ;
#61192=CARTESIAN_POINT ( 'NONE',  ( 31.36650669486618881, 1.474610560812782335E-15, 0.000000000000000000 ) ) ;
#61206=DIRECTION ( 'NONE',  ( 0.000000000000000000, -1.000000000000000000, 0.000000000000000000 ) ) ;
#61230=CARTESIAN_POINT ( 'NONE',  ( 6.644028492724100232, 3.901260126080569712, 6.757180751913672623 ) ) ;
#61248=CARTESIAN_POINT ( 'NONE',  ( 8.099999999999999645, 7.505553499465140277, 0.000000000000000000 ) ) ;
#61294=DIRECTION ( 'NONE',  ( 0.000000000000000000, -1.000000000000000000, 0.000000000000000000 ) ) ;
#61318=ADVANCED_FACE ( 'NONE', ( #17483 ), #50621, .T. ) ;
#61327=CARTESIAN_POINT ( 'NONE',  ( 27.61650669486618881, 4.000000000000003553, 4.898587196589414801E-16 ) ) ;
#61418=CARTESIAN_POINT ( 'NONE',  ( 28.58349330513380337, -3.851859888774471706E-31, 4.000000000000001776 ) ) ;
#61430=ORIENTED_EDGE ( 'NONE', *, *, #40870, .F. ) ;
#61439=EDGE_CURVE ( 'NONE', #87682, #48784, #55640, .T. ) ;
#61462=DIRECTION ( 'NONE',  ( 0.000000000000000000, 0.000000000000000000, 1.000000000000000000 ) ) ;
#61465=CIRCLE ( 'NONE', #75210, 3.309500000000001663 ) ;
#61466=DIRECTION ( 'NONE',  ( -1.000000000000000000, -1.224606353822377258E-16, -0.000000000000000000 ) ) ;
#61469=AXIS2_PLACEMENT_3D ( 'NONE', #6144, #71411, #29929 ) ;
#61476=EDGE_CURVE ( 'NONE', #34409, #60770, #60982, .T. ) ;
#61485=B_SPLINE_CURVE_WITH_KNOTS ( 'NONE', 3,
 ( #57024, #23637, #6891, #8484, #33861, #90474 ),
 .UNSPECIFIED., .F., .F.,
 ( 4, 2, 4 ),
 ( 2.380733003139562229E-07, 0.001898835937927376583, 0.003797433802554438936 ),
 .UNSPECIFIED. ) ;
#61499=CARTESIAN_POINT ( 'NONE',  ( 0.01372220897661678186, 5.309964801958117597, -3.802871176606132053 ) ) ;
#61502=ORIENTED_EDGE ( 'NONE', *, *, #60017, .T. ) ;
#61515=VERTEX_POINT ( 'NONE', #7628 ) ;
#61520=CARTESIAN_POINT ( 'NONE',  ( 33.86650669486618881, 0.000000000000000000, 4.000000000000000888 ) ) ;
#61595=CARTESIAN_POINT ( 'NONE',  ( 15.11650669486618881, 1.474610560812782335E-15, 0.000000000000000000 ) ) ;
#61710=ORIENTED_EDGE ( 'NONE', *, *, #20351, .F. ) ;
#61722=EDGE_CURVE ( 'NONE', #98362, #79927, #43714, .T. ) ;
#61730=ORIENTED_EDGE ( 'NONE', *, *, #15801, .F. ) ;
#61735=ORIENTED_EDGE ( 'NONE', *, *, #67655, .T. ) ;
#61736=CIRCLE ( 'NONE', #78857, 0.5999999999999980904 ) ;
#61773=ORIENTED_EDGE ( 'NONE', *, *, #34811, .T. ) ;
#61791=DIRECTION ( 'NONE',  ( 0.000000000000000000, -1.000000000000000000, 0.000000000000000000 ) ) ;
#61795=DIRECTION ( 'NONE',  ( 0.000000000000000000, -1.000000000000000000, 0.000000000000000000 ) ) ;
#61811=CARTESIAN_POINT ( 'NONE',  ( 28.09999999999999787, -3.309499999999999886, 0.000000000000000000 ) ) ;
#61847=ORIENTED_EDGE ( 'NONE', *, *, #85230, .T. ) ;
#61861=EDGE_CURVE ( 'NONE', #21060, #89753, #57553, .T. ) ;
#61870=AXIS2_PLACEMENT_3D ( 'NONE', #43948, #19721, #61206 ) ;
#61876=CONICAL_SURFACE ( 'NONE', #80777, 4.000000000000001776, 0.9599310885968774798 ) ;
#61878=ORIENTED_EDGE ( 'NONE', *, *, #57291, .F. ) ;
#61880=DIRECTION ( 'NONE',  ( -0.5735764363510494901, -0.8191520442889894671, 0.000000000000000000 ) ) ;
#61924=ORIENTED_EDGE ( 'NONE', *, *, #6030, .F. ) ;
#61944=DIRECTION ( 'NONE',  ( 0.000000000000000000, -1.000000000000000000, 0.000000000000000000 ) ) ;
#61999=ADVANCED_FACE ( 'NONE', ( #106340 ), #91262, .T. ) ;
#62004=DIRECTION ( 'NONE',  ( -1.000000000000000000, -1.224606353822377258E-16, -0.000000000000000000 ) ) ;
#62018=CARTESIAN_POINT ( 'NONE',  ( 6.585468679846623985, 7.640532685286893333, 0.2337908078075577600 ) ) ;
#62032=DIRECTION ( 'NONE',  ( -1.000000000000000000, -1.224606353822377258E-16, -0.000000000000000000 ) ) ;
#62035=ADVANCED_FACE ( 'NONE', ( #33036 ), #105759, .T. ) ;
#62037=CARTESIAN_POINT ( 'NONE',  ( 6.289692432696983637, 6.589071317541204564, 2.245373559999253033 ) ) ;
#62048=EDGE_CURVE ( 'NONE', #101426, #98362, #26601, .T. ) ;
#62065=CARTESIAN_POINT ( 'NONE',  ( 22.33349330513380693, 1.593028355512270962E-15, 0.000000000000000000 ) ) ;
#62110=CIRCLE ( 'NONE', #15561, 4.000000000000000888 ) ;
#62118=FACE_OUTER_BOUND ( 'NONE', #22573, .T. ) ;
#62126=CARTESIAN_POINT ( 'NONE',  ( 6.683837171061803417, -3.955946848495962787, 6.851900933636989599 ) ) ;
#62162=ORIENTED_EDGE ( 'NONE', *, *, #80456, .T. ) ;
#62163=EDGE_CURVE ( 'NONE', #2998, #83001, #28354, .T. ) ;
#62192=VECTOR ( 'NONE', #84654, 1000.000000000000341 ) ;
#62220=LINE ( 'NONE', #5021, #22983 ) ;
#62223=AXIS2_PLACEMENT_3D ( 'NONE', #94697, #28381, #28930 ) ;
#62232=DIRECTION ( 'NONE',  ( -1.000000000000000000, -1.224606353822377258E-16, -0.000000000000000000 ) ) ;
#62237=ORIENTED_EDGE ( 'NONE', *, *, #44622, .T. ) ;
#62244=AXIS2_PLACEMENT_3D ( 'NONE', #8464, #14954, #33302 ) ;
#62248=CYLINDRICAL_SURFACE ( 'NONE', #86761, 4.000000000000000888 ) ;
#62251=FACE_OUTER_BOUND ( 'NONE', #52854, .T. ) ;
#62291=DIRECTION ( 'NONE',  ( -0.5735764363510494901, -0.8191520442889894671, 0.000000000000000000 ) ) ;
#62332=VERTEX_POINT ( 'NONE', #104636 ) ;
#62339=VECTOR ( 'NONE', #49352, 1000.000000000000341 ) ;
#62359=ORIENTED_EDGE ( 'NONE', *, *, #68214, .T. ) ;
#62363=CARTESIAN_POINT ( 'NONE',  ( 19.34999999999999787, 1.533819458162526451E-15, 0.000000000000000000 ) ) ;
#62380=ORIENTED_EDGE ( 'NONE', *, *, #66206, .T. ) ;
#62407=CONICAL_SURFACE ( 'NONE', #2087, 4.000000000000001776, 0.9599310885968774798 ) ;
#62467=CIRCLE ( 'NONE', #34929, 4.000000000000001776 ) ;
#62482=DIRECTION ( 'NONE',  ( 0.000000000000000000, -1.000000000000000000, 0.000000000000000000 ) ) ;
#62548=EDGE_CURVE ( 'NONE', #94131, #81142, #102465, .T. ) ;
#62560=DIRECTION ( 'NONE',  ( -1.000000000000000000, -1.224606353822377258E-16, -0.000000000000000000 ) ) ;
#62564=AXIS2_PLACEMENT_3D ( 'NONE', #41771, #67656, #33176 ) ;
#62569=( GEOMETRIC_REPRESENTATION_CONTEXT ( 3 ) GLOBAL_UNCERTAINTY_ASSIGNED_CONTEXT ( ( #84798 ) ) GLOBAL_UNIT_ASSIGNED_CONTEXT ( ( #28863, #21284, #37475 ) ) REPRESENTATION_CONTEXT ( 'NONE', 'WORKASPACE' ) );
#62603=EDGE_LOOP ( 'NONE', ( #2986, #85612, #76279, #87888 ) ) ;
#62617=CARTESIAN_POINT ( 'NONE',  ( 21.36650669486618881, 1.474610560812782335E-15, 0.000000000000000000 ) ) ;
#62632=DIRECTION ( 'NONE',  ( 0.000000000000000000, -1.000000000000000000, 0.000000000000000000 ) ) ;
#62636=EDGE_CURVE ( 'NONE', #42319, #88074, #12835, .T. ) ;
#62642=EDGE_CURVE ( 'NONE', #42350, #94131, #46288, .T. ) ;
#62650=DIRECTION ( 'NONE',  ( -1.000000000000000000, -1.224606353822377258E-16, -0.000000000000000000 ) ) ;
#62696=CARTESIAN_POINT ( 'NONE',  ( 9.833493305133805151, -4.000000000000000000, 4.898587196589415787E-16 ) ) ;
#62736=CARTESIAN_POINT ( 'NONE',  ( 6.222742520105470021, -3.584500230190543313, 6.791463481567636684 ) ) ;
#62751=DIRECTION ( 'NONE',  ( -1.000000000000000000, -1.224606353822377258E-16, -0.000000000000000000 ) ) ;
#62769=VECTOR ( 'NONE', #24053, 1000.000000000000114 ) ;
#62772=VERTEX_POINT ( 'NONE', #72929 ) ;
#62800=VECTOR ( 'NONE', #42195, 1000.000000000000000 ) ;
#62823=ADVANCED_FACE ( 'NONE', ( #56746 ), #69754, .T. ) ;
#62827=FACE_OUTER_BOUND ( 'NONE', #36875, .T. ) ;
#62845=VECTOR ( 'NONE', #54197, 1000.000000000000000 ) ;
#62858=EDGE_CURVE ( 'NONE', #4237, #42466, #12897, .T. ) ;
#62861=CYLINDRICAL_SURFACE ( 'NONE', #55858, 4.000000000000000888 ) ;
#62868=VERTEX_POINT ( 'NONE', #5041 ) ;
#62885=AXIS2_PLACEMENT_3D ( 'NONE', #79224, #45283, #37210 ) ;
#62887=ORIENTED_EDGE ( 'NONE', *, *, #94277, .T. ) ;
#62888=DIRECTION ( 'NONE',  ( -1.000000000000000000, -1.224606353822377258E-16, -0.000000000000000000 ) ) ;
#62910=AXIS2_PLACEMENT_3D ( 'NONE', #92309, #42709, #58361 ) ;
#62927=ORIENTED_EDGE ( 'NONE', *, *, #103232, .F. ) ;
#62960=ADVANCED_FACE ( 'NONE', ( #88608 ), #93926, .T. ) ;
#62975=CARTESIAN_POINT ( 'NONE',  ( 6.332254158185369519, -2.698766916918251990, -6.500000000000001776 ) ) ;
#62978=DIRECTION ( 'NONE',  ( 0.000000000000000000, -1.000000000000000000, 0.000000000000000000 ) ) ;
#62990=AXIS2_PLACEMENT_3D ( 'NONE', #23305, #95066, #104187 ) ;
#63012=EDGE_LOOP ( 'NONE', ( #43398, #68231, #76938, #81195, #38569 ) ) ;
#63035=ADVANCED_FACE ( 'NONE', ( #65924 ), #87011, .T. ) ;
#63078=VERTEX_POINT ( 'NONE', #10330 ) ;
#63094=ORIENTED_EDGE ( 'NONE', *, *, #41183, .T. ) ;
#63108=ORIENTED_EDGE ( 'NONE', *, *, #18140, .F. ) ;
#63151=DIRECTION ( 'NONE',  ( 0.000000000000000000, -1.000000000000000000, 0.000000000000000000 ) ) ;
#63161=CARTESIAN_POINT ( 'NONE',  ( 19.83349330513380693, 1.593028355512270962E-15, 0.000000000000000000 ) ) ;
#63180=AXIS2_PLACEMENT_3D ( 'NONE', #55915, #40298, #39786 ) ;
#63192=DIRECTION ( 'NONE',  ( 0.000000000000000000, -1.000000000000000000, 0.000000000000000000 ) ) ;
#63216=CIRCLE ( 'NONE', #16703, 3.309500000000001663 ) ;
#63217=AXIS2_PLACEMENT_3D ( 'NONE', #34219, #15468, #58465 ) ;
#63229=EDGE_CURVE ( 'NONE', #62332, #25738, #21569, .T. ) ;
#63253=ADVANCED_FACE ( 'NONE', ( #5950 ), #70706, .T. ) ;
#63263=CARTESIAN_POINT ( 'NONE',  ( 0.000000000000000000, 0.000000000000000000, 0.000000000000000000 ) ) ;
#63280=CARTESIAN_POINT ( 'NONE',  ( 36.36650669486618881, 4.000000000000003553, 4.898587196589414801E-16 ) ) ;
#63304=ORIENTED_EDGE ( 'NONE', *, *, #78158, .F. ) ;
#63307=ORIENTED_EDGE ( 'NONE', *, *, #13698, .F. ) ;
#63312=AXIS2_PLACEMENT_3D ( 'NONE', #14399, #65097, #31693 ) ;
#63329=VECTOR ( 'NONE', #75438, 1000.000000000000000 ) ;
#63363=DIRECTION ( 'NONE',  ( 0.000000000000000000, 0.000000000000000000, 1.000000000000000000 ) ) ;
#63368=ORIENTED_EDGE ( 'NONE', *, *, #78975, .F. ) ;
#63374=CARTESIAN_POINT ( 'NONE',  ( 0.2573354458087839802, 6.889406814520513400, -1.067197363239225094 ) ) ;
#63465=CARTESIAN_POINT ( 'NONE',  ( 0.5805565836007617886, -3.752776749732566142, 6.499999999999999112 ) ) ;
#63466=CARTESIAN_POINT ( 'NONE',  ( 12.33349330513380693, 1.593028355512270962E-15, 0.000000000000000000 ) ) ;
#63502=EDGE_LOOP ( 'NONE', ( #19939, #36619, #5795, #84627, #61710 ) ) ;
#63530=ORIENTED_EDGE ( 'NONE', *, *, #75555, .T. ) ;
#63533=VERTEX_POINT ( 'NONE', #43639 ) ;
#63556=CYLINDRICAL_SURFACE ( 'NONE', #9538, 4.000000000000000888 ) ;
#63598=DIRECTION ( 'NONE',  ( 0.000000000000000000, -1.000000000000000000, 0.000000000000000000 ) ) ;
#63621=CARTESIAN_POINT ( 'NONE',  ( 5.819846122303830249, 6.321060697774965931, 2.051601713726983078 ) ) ;
#63622=CARTESIAN_POINT ( 'NONE',  ( 22.33349330513380693, 4.000000000000003553, 0.000000000000000000 ) ) ;
#63638=ORIENTED_EDGE ( 'NONE', *, *, #86675, .F. ) ;
#63667=ADVANCED_FACE ( 'NONE', ( #48406 ), #30267, .T. ) ;
#63669=ORIENTED_EDGE ( 'NONE', *, *, #73666, .T. ) ;
#63676=EDGE_CURVE ( 'NONE', #72268, #4316, #23639, .T. ) ;
#63687=DIRECTION ( 'NONE',  ( 0.000000000000000000, -1.000000000000000000, 0.000000000000000000 ) ) ;
#63714=DIRECTION ( 'NONE',  ( -1.000000000000000000, -1.224606353822377258E-16, -0.000000000000000000 ) ) ;
#63739=VERTEX_POINT ( 'NONE', #36540 ) ;
#63743=DIRECTION ( 'NONE',  ( -1.000000000000000000, -1.224606353822377258E-16, -0.000000000000000000 ) ) ;
#63762=CARTESIAN_POINT ( 'NONE',  ( 21.08349330513380693, 1.593028355512270962E-15, 0.000000000000000000 ) ) ;
#63777=ORIENTED_EDGE ( 'NONE', *, *, #54559, .T. ) ;
#63779=VERTEX_POINT ( 'NONE', #28435 ) ;
#63796=DIRECTION ( 'NONE',  ( -1.000000000000000000, -1.224606353822377258E-16, -0.000000000000000000 ) ) ;
#63801=CIRCLE ( 'NONE', #44865, 4.000000000000001776 ) ;
#63827=CYLINDRICAL_SURFACE ( 'NONE', #86360, 4.000000000000000888 ) ;
#63900=EDGE_CURVE ( 'NONE', #55679, #96624, #11359, .T. ) ;
#63915=DIRECTION ( 'NONE',  ( -1.000000000000000000, -0.000000000000000000, -0.000000000000000000 ) ) ;
#63927=CARTESIAN_POINT ( 'NONE',  ( 0.000000000000000000, 1.502314598737160412E-15, 6.500000000000000888 ) ) ;
#63969=CARTESIAN_POINT ( 'NONE',  ( 26.08349330513380693, 1.593028355512270962E-15, 0.000000000000000000 ) ) ;
#63972=EDGE_LOOP ( 'NONE', ( #21062, #4132, #1512, #95940, #36394 ) ) ;
#64016=AXIS2_PLACEMENT_3D ( 'NONE', #9715, #59906, #25973 ) ;
#64041=VERTEX_POINT ( 'NONE', #23668 ) ;
#64052=DIRECTION ( 'NONE',  ( -1.000000000000000000, -1.224606353822377258E-16, -0.000000000000000000 ) ) ;
#64066=EDGE_CURVE ( 'NONE', #51009, #18709, #40884, .T. ) ;
#64088=FACE_OUTER_BOUND ( 'NONE', #101287, .T. ) ;
#64099=DIRECTION ( 'NONE',  ( -1.000000000000000000, -1.224606353822377258E-16, -0.000000000000000000 ) ) ;
#64167=ORIENTED_EDGE ( 'NONE', *, *, #87186, .F. ) ;
#64194=CONICAL_SURFACE ( 'NONE', #81395, 3.309500000000001663, 0.9599310885968770357 ) ;
#64205=CARTESIAN_POINT ( 'NONE',  ( 22.33349330513380693, 4.898587196589411843E-16, -4.000000000000001776 ) ) ;
#64219=EDGE_CURVE ( 'NONE', #4198, #59152, #88758, .T. ) ;
#64296=VERTEX_POINT ( 'NONE', #95291 ) ;
#64331=CARTESIAN_POINT ( 'NONE',  ( 5.819846122303831137, -6.321060697774816717, 2.051601713727242871 ) ) ;
#64334=DIRECTION ( 'NONE',  ( -1.000000000000000000, -1.224606353822377258E-16, -0.000000000000000000 ) ) ;
#64338=CARTESIAN_POINT ( 'NONE',  ( 6.326622418652847024, 1.327077765693000178, -6.831545684615178970 ) ) ;
#64371=DIRECTION ( 'NONE',  ( -1.000000000000000000, -1.224606353822377258E-16, -0.000000000000000000 ) ) ;
#64378=DIRECTION ( 'NONE',  ( 0.000000000000000000, -1.000000000000000000, 0.000000000000000000 ) ) ;
#64420=AXIS2_PLACEMENT_3D ( 'NONE', #31351, #7546, #105205 ) ;
#64437=ORIENTED_EDGE ( 'NONE', *, *, #45847, .F. ) ;
#64457=DIRECTION ( 'NONE',  ( -1.000000000000000000, -1.224606353822377258E-16, -0.000000000000000000 ) ) ;
#64462=AXIS2_PLACEMENT_3D ( 'NONE', #34581, #50188, #25423 ) ;
#64471=EDGE_CURVE ( 'NONE', #19214, #100701, #88987, .T. ) ;
#64476=VERTEX_POINT ( 'NONE', #15948 ) ;
#64491=DIRECTION ( 'NONE',  ( 0.000000000000000000, 1.000000000000000000, 0.000000000000000000 ) ) ;
#64499=ADVANCED_FACE ( 'NONE', ( #39183 ), #40704, .T. ) ;
#64532=ORIENTED_EDGE ( 'NONE', *, *, #91917, .T. ) ;
#64567=CARTESIAN_POINT ( 'NONE',  ( 6.449780583204731244, 2.701143306770497965, -6.840188146834836225 ) ) ;
#64585=ORIENTED_EDGE ( 'NONE', *, *, #77334, .F. ) ;
#64591=EDGE_CURVE ( 'NONE', #90138, #11885, #99268, .T. ) ;
#64627=CARTESIAN_POINT ( 'NONE',  ( 12.33349330513380693, 4.898587196589411843E-16, -4.000000000000001776 ) ) ;
#64650=ORIENTED_EDGE ( 'NONE', *, *, #45945, .F. ) ;
#64687=LINE ( 'NONE', #38829, #24976 ) ;
#64696=ORIENTED_EDGE ( 'NONE', *, *, #20483, .F. ) ;
#64720=EDGE_LOOP ( 'NONE', ( #38862, #81939, #40801, #4077, #84065 ) ) ;
#64739=VERTEX_POINT ( 'NONE', #29395 ) ;
#64774=ORIENTED_EDGE ( 'NONE', *, *, #59486, .T. ) ;
#64801=CARTESIAN_POINT ( 'NONE',  ( 16.08349330513380337, 4.898587196589411843E-16, -4.000000000000001776 ) ) ;
#64805=AXIS2_PLACEMENT_3D ( 'NONE', #100997, #18515, #103134 ) ;
#64885=EDGE_CURVE ( 'NONE', #72268, #91201, #78962, .T. ) ;
#64895=AXIS2_PLACEMENT_3D ( 'NONE', #2898, #84372, #9385 ) ;
#64897=AXIS2_PLACEMENT_3D ( 'NONE', #5230, #94244, #45171 ) ;
#64902=EDGE_CURVE ( 'NONE', #66536, #24036, #59503, .T. ) ;
#64927=AXIS2_PLACEMENT_3D ( 'NONE', #18008, #58993, #99967 ) ;
#64944=EDGE_LOOP ( 'NONE', ( #49172, #9246, #69457, #10451, #99766 ) ) ;
#64964=AXIS2_PLACEMENT_3D ( 'NONE', #105907, #56282, #97824 ) ;
#64985=VECTOR ( 'NONE', #20286, 1000.000000000000000 ) ;
#65045=CARTESIAN_POINT ( 'NONE',  ( 30.11650669486618881, 0.000000000000000000, 4.000000000000000888 ) ) ;
#65049=ORIENTED_EDGE ( 'NONE', *, *, #48232, .F. ) ;
#65057=DIRECTION ( 'NONE',  ( -1.000000000000000000, -1.224606353822377258E-16, -0.000000000000000000 ) ) ;
#65062=CARTESIAN_POINT ( 'NONE',  ( 0.000000000000000000, 0.000000000000000000, 0.000000000000000000 ) ) ;
#65097=DIRECTION ( 'NONE',  ( -1.000000000000000000, -1.224606353822377258E-16, -0.000000000000000000 ) ) ;
#65138=CIRCLE ( 'NONE', #85799, 4.000000000000001776 ) ;
#65145=DIRECTION ( 'NONE',  ( 0.000000000000000000, -1.000000000000000000, 0.000000000000000000 ) ) ;
#65181=DIRECTION ( 'NONE',  ( 1.000000000000000000, 1.224606353822377258E-16, 0.000000000000000000 ) ) ;
#65187=VECTOR ( 'NONE', #25037, 1000.000000000000000 ) ;
#65218=LINE ( 'NONE', #74881, #11995 ) ;
#65227=AXIS2_PLACEMENT_3D ( 'NONE', #89929, #72674, #40314 ) ;
#65237=CARTESIAN_POINT ( 'NONE',  ( 33.58349330513380693, 4.000000000000003553, 0.000000000000000000 ) ) ;
#65250=CARTESIAN_POINT ( 'NONE',  ( 35.59999999999999432, 1.533819458162526451E-15, 0.000000000000000000 ) ) ;
#65277=CARTESIAN_POINT ( 'NONE',  ( 16.36650669486618881, 1.474610560812782335E-15, 0.000000000000000000 ) ) ;
#65301=DIRECTION ( 'NONE',  ( -1.000000000000000000, -0.000000000000000000, -0.000000000000000000 ) ) ;
#65314=EDGE_LOOP ( 'NONE', ( #48337, #95775, #296, #86401, #374, #36914 ) ) ;
#65317=FACE_OUTER_BOUND ( 'NONE', #6097, .T. ) ;
#65333=ORIENTED_EDGE ( 'NONE', *, *, #75474, .T. ) ;
#65334=FACE_OUTER_BOUND ( 'NONE', #11708, .T. ) ;
#65359=DIRECTION ( 'NONE',  ( 0.000000000000000000, -1.000000000000000000, 0.000000000000000000 ) ) ;
#65382=DIRECTION ( 'NONE',  ( -1.000000000000000000, -0.000000000000000000, -0.000000000000000000 ) ) ;
#65401=CARTESIAN_POINT ( 'NONE',  ( 16.84999999999999787, 1.533819458162526451E-15, 0.000000000000000000 ) ) ;
#65410=ORIENTED_EDGE ( 'NONE', *, *, #97724, .F. ) ;
#65441=DIRECTION ( 'NONE',  ( -1.000000000000000000, -1.224606353822377258E-16, -0.000000000000000000 ) ) ;
#65451=AXIS2_PLACEMENT_3D ( 'NONE', #388, #16080, #49506 ) ;
#65467=CARTESIAN_POINT ( 'NONE',  ( 16.36650669486618881, 1.474610560812782335E-15, 0.000000000000000000 ) ) ;
#65473=CARTESIAN_POINT ( 'NONE',  ( 6.326592304916275111, 5.253140224433044736, -4.564380808752273921 ) ) ;
#65486=CARTESIAN_POINT ( 'NONE',  ( 34.83349330513380693, 1.593028355512270962E-15, 0.000000000000000000 ) ) ;
#65491=CARTESIAN_POINT ( 'NONE',  ( 17.33349330513380693, 1.593028355512270962E-15, 0.000000000000000000 ) ) ;
#65507=ORIENTED_EDGE ( 'NONE', *, *, #55218, .F. ) ;
#65524=CIRCLE ( 'NONE', #25992, 4.000000000000001776 ) ;
#65535=AXIS2_PLACEMENT_3D ( 'NONE', #67843, #26894, #59235 ) ;
#65544=ORIENTED_EDGE ( 'NONE', *, *, #85230, .F. ) ;
#65548=CARTESIAN_POINT ( 'NONE',  ( 6.281175601187043434, -3.752776749732574579, -6.500000000000000888 ) ) ;
#65549=VERTEX_POINT ( 'NONE', #85098 ) ;
#65553=CARTESIAN_POINT ( 'NONE',  ( 6.162888688655347558, -7.505553499465142053, -3.129864801432410934E-16 ) ) ;
#65571=CARTESIAN_POINT ( 'NONE',  ( 11.84999999999999787, -3.309499999999999886, 0.000000000000000000 ) ) ;
#65611=ORIENTED_EDGE ( 'NONE', *, *, #89709, .T. ) ;
#65655=DIRECTION ( 'NONE',  ( 0.000000000000000000, 1.000000000000000000, 0.000000000000000000 ) ) ;
#65724=CARTESIAN_POINT ( 'NONE',  ( 0.06682554136337934270, -4.993536075455425660, 4.350941807883113022 ) ) ;
#65812=ORIENTED_EDGE ( 'NONE', *, *, #58723, .F. ) ;
#65858=EDGE_LOOP ( 'NONE', ( #67986, #61502, #32785, #64774, #93143 ) ) ;
#65897=DIRECTION ( 'NONE',  ( 0.000000000000000000, -1.000000000000000000, 0.000000000000000000 ) ) ;
#65918=EDGE_CURVE ( 'NONE', #11369, #93666, #61485, .T. ) ;
#65924=FACE_OUTER_BOUND ( 'NONE', #80721, .T. ) ;
#65934=CARTESIAN_POINT ( 'NONE',  ( 6.162888688655344893, -3.752776749732565253, 6.499999999999999112 ) ) ;
#65963=ORIENTED_EDGE ( 'NONE', *, *, #16598, .F. ) ;
#65997=CARTESIAN_POINT ( 'NONE',  ( 6.683837171061806082, 7.911893696991936231, -4.595687358162529387E-16 ) ) ;
#66028=VERTEX_POINT ( 'NONE', #24181 ) ;
#66061=VERTEX_POINT ( 'NONE', #106644 ) ;
#66062=CARTESIAN_POINT ( 'NONE',  ( 21.08349330513380693, 1.593028355512270962E-15, 0.000000000000000000 ) ) ;
#66094=EDGE_CURVE ( 'NONE', #70045, #64296, #44180, .T. ) ;
#66114=CARTESIAN_POINT ( 'NONE',  ( 0.000000000000000000, 0.000000000000000000, 0.000000000000000000 ) ) ;
#66129=DIRECTION ( 'NONE',  ( 0.000000000000000000, -1.000000000000000000, 0.000000000000000000 ) ) ;
#66156=PLANE ( 'NONE',  #105922 ) ;
#66172=ADVANCED_FACE ( 'NONE', ( #3600 ), #32101, .T. ) ;
#66190=CARTESIAN_POINT ( 'NONE',  ( 23.58349330513380337, 4.000000000000002665, 0.000000000000000000 ) ) ;
#66206=EDGE_CURVE ( 'NONE', #43607, #9118, #84519, .T. ) ;
#66283=AXIS2_PLACEMENT_3D ( 'NONE', #99563, #42942, #101180 ) ;
#66333=ADVANCED_FACE ( 'NONE', ( #31091 ), #56300, .T. ) ;
#66345=EDGE_CURVE ( 'NONE', #60578, #86058, #22984, .T. ) ;
#66358=VERTEX_POINT ( 'NONE', #14853 ) ;
#66363=EDGE_CURVE ( 'NONE', #42192, #61003, #4606, .T. ) ;
#66384=ADVANCED_FACE ( 'NONE', ( #68193 ), #9811, .T. ) ;
#66386=VECTOR ( 'NONE', #58942, 1000.000000000000000 ) ;
#66390=ORIENTED_EDGE ( 'NONE', *, *, #61722, .T. ) ;
#66393=DIRECTION ( 'NONE',  ( -1.000000000000000000, -1.224606353822377258E-16, -0.000000000000000000 ) ) ;
#66439=LINE ( 'NONE', #9782, #35463 ) ;
#66453=ORIENTED_EDGE ( 'NONE', *, *, #78610, .F. ) ;
#66456=ORIENTED_EDGE ( 'NONE', *, *, #41645, .F. ) ;
#66477=ORIENTED_EDGE ( 'NONE', *, *, #56749, .F. ) ;
#66536=VERTEX_POINT ( 'NONE', #26192 ) ;
#66581=AXIS2_PLACEMENT_3D ( 'NONE', #100181, #34952, #58123 ) ;
#66604=ORIENTED_EDGE ( 'NONE', *, *, #55218, .T. ) ;
#66606=AXIS2_PLACEMENT_3D ( 'NONE', #22379, #5625, #5104 ) ;
#66613=LINE ( 'NONE', #16466, #5046 ) ;
#66617=CIRCLE ( 'NONE', #56271, 4.000000000000000888 ) ;
#66625=AXIS2_PLACEMENT_3D ( 'NONE', #68013, #10815, #100898 ) ;
#66631=DIRECTION ( 'NONE',  ( -1.000000000000000000, -0.000000000000000000, -0.000000000000000000 ) ) ;
#66665=ORIENTED_EDGE ( 'NONE', *, *, #8078, .F. ) ;
#66667=DIRECTION ( 'NONE',  ( -1.000000000000000000, -1.224606353822377258E-16, -0.000000000000000000 ) ) ;
#66672=CARTESIAN_POINT ( 'NONE',  ( 6.463344223170841119, -4.601472318010342732, 5.710032555828793654 ) ) ;
#66677=AXIS2_PLACEMENT_3D ( 'NONE', #7595, #55608, #74461 ) ;
#66679=DIRECTION ( 'NONE',  ( -1.000000000000000000, -0.000000000000000000, -0.000000000000000000 ) ) ;
#66686=ORIENTED_EDGE ( 'NONE', *, *, #62636, .F. ) ;
#66703=ORIENTED_EDGE ( 'NONE', *, *, #48186, .T. ) ;
#66721=DIRECTION ( 'NONE',  ( 1.000000000000000000, 1.224606353822377258E-16, 0.000000000000000000 ) ) ;
#66764=VECTOR ( 'NONE', #27683, 1000.000000000000000 ) ;
#66767=DIRECTION ( 'NONE',  ( -1.000000000000000000, -1.224606353822377258E-16, -0.000000000000000000 ) ) ;
#66780=VECTOR ( 'NONE', #96462, 1000.000000000000000 ) ;
#66793=CARTESIAN_POINT ( 'NONE',  ( 13.86650669486618881, 1.474610560812782335E-15, 0.000000000000000000 ) ) ;
#66819=EDGE_CURVE ( 'NONE', #11120, #46974, #31998, .T. ) ;
#66841=ORIENTED_EDGE ( 'NONE', *, *, #41943, .T. ) ;
#66860=EDGE_CURVE ( 'NONE', #88074, #20995, #35740, .T. ) ;
#66884=DIRECTION ( 'NONE',  ( -1.000000000000000000, -1.224606353822377258E-16, -0.000000000000000000 ) ) ;
#66934=EDGE_LOOP ( 'NONE', ( #94744, #37198, #20800, #17503, #6520, #61730 ) ) ;
#66939=ORIENTED_EDGE ( 'NONE', *, *, #2625, .T. ) ;
#66943=AXIS2_PLACEMENT_3D ( 'NONE', #49384, #31652, #82293 ) ;
#66960=CIRCLE ( 'NONE', #92740, 4.000000000000001776 ) ;
#66963=CARTESIAN_POINT ( 'NONE',  ( 37.33349330513379982, -3.851859888774471706E-31, 4.000000000000001776 ) ) ;
#66984=ORIENTED_EDGE ( 'NONE', *, *, #68784, .T. ) ;
#67044=EDGE_CURVE ( 'NONE', #51009, #98690, #72895, .T. ) ;
#67094=CARTESIAN_POINT ( 'NONE',  ( 18.09999999999999787, -3.309499999999999886, 0.000000000000000000 ) ) ;
#67120=EDGE_CURVE ( 'NONE', #42272, #6505, #59812, .T. ) ;
#67181=EDGE_CURVE ( 'NONE', #73038, #92082, #87368, .T. ) ;
#67211=ORIENTED_EDGE ( 'NONE', *, *, #83714, .F. ) ;
#67256=ORIENTED_EDGE ( 'NONE', *, *, #38291, .T. ) ;
#67259=CIRCLE ( 'NONE', #70713, 4.000000000000000888 ) ;
#67266=CARTESIAN_POINT ( 'NONE',  ( 5.819846122303830249, 4.937269551422757807, -4.448398286272981395 ) ) ;
#67276=EDGE_CURVE ( 'NONE', #46183, #11885, #51071, .T. ) ;
#67278=ORIENTED_EDGE ( 'NONE', *, *, #90254, .F. ) ;
#67297=ORIENTED_EDGE ( 'NONE', *, *, #30809, .T. ) ;
#67327=CIRCLE ( 'NONE', #93115, 4.000000000000000888 ) ;
#67354=DIRECTION ( 'NONE',  ( -1.000000000000000000, -0.000000000000000000, -0.000000000000000000 ) ) ;
#67360=CIRCLE ( 'NONE', #91458, 4.000000000000001776 ) ;
#67363=CARTESIAN_POINT ( 'NONE',  ( 0.000000000000000000, 4.898587196589413815E-16, -4.000000000000000888 ) ) ;
#67424=CARTESIAN_POINT ( 'NONE',  ( 21.08349330513380693, 1.593028355512270962E-15, 0.000000000000000000 ) ) ;
#67449=B_SPLINE_CURVE_WITH_KNOTS ( 'NONE', 3,
 ( #12755, #54261, #36560, #87204, #71002 ),
 .UNSPECIFIED., .F., .F.,
 ( 4, 1, 4 ),
 ( 0.000000000000000000, 0.003752776749732565295, 0.007505553499465130590 ),
 .UNSPECIFIED. ) ;
#67453=ORIENTED_EDGE ( 'NONE', *, *, #92182, .F. ) ;
#67472=ORIENTED_EDGE ( 'NONE', *, *, #90865, .T. ) ;
#67538=LINE ( 'NONE', #100418, #104043 ) ;
#67545=VERTEX_POINT ( 'NONE', #39172 ) ;
#67548=VERTEX_POINT ( 'NONE', #56908 ) ;
#67550=CARTESIAN_POINT ( 'NONE',  ( 11.36650669486618881, -3.999999999999998224, 0.000000000000000000 ) ) ;
#67571=CARTESIAN_POINT ( 'NONE',  ( 31.08349330513380693, 1.593028355512270962E-15, 0.000000000000000000 ) ) ;
#67586=DIRECTION ( 'NONE',  ( 0.5735764363510490460, 0.8191520442889896891, 0.000000000000000000 ) ) ;
#67591=CYLINDRICAL_SURFACE ( 'NONE', #87328, 4.000000000000000888 ) ;
#67595=VERTEX_POINT ( 'NONE', #42329 ) ;
#67631=CYLINDRICAL_SURFACE ( 'NONE', #49017, 4.000000000000000888 ) ;
#67655=EDGE_CURVE ( 'NONE', #14445, #36519, #85762, .T. ) ;
#67656=DIRECTION ( 'NONE',  ( -1.000000000000000000, -0.000000000000000000, 0.000000000000000000 ) ) ;
#67672=ORIENTED_EDGE ( 'NONE', *, *, #5986, .T. ) ;
#67686=ADVANCED_FACE ( 'NONE', ( #44475 ), #34818, .T. ) ;
#67741=ORIENTED_EDGE ( 'NONE', *, *, #56675, .T. ) ;
#67749=CARTESIAN_POINT ( 'NONE',  ( 19.83349330513380693, -4.000000000000000000, 4.898587196589415787E-16 ) ) ;
#67750=DIRECTION ( 'NONE',  ( 0.000000000000000000, -1.000000000000000000, 0.000000000000000000 ) ) ;
#67760=ORIENTED_EDGE ( 'NONE', *, *, #78975, .T. ) ;
#67767=ORIENTED_EDGE ( 'NONE', *, *, #78695, .T. ) ;
#67778=ADVANCED_FACE ( 'NONE', ( #98322 ), #3058, .T. ) ;
#67843=CARTESIAN_POINT ( 'NONE',  ( 0.000000000000000000, 0.000000000000000000, 0.000000000000000000 ) ) ;
#67849=ADVANCED_FACE ( 'NONE', ( #11955 ), #25572, .T. ) ;
#67881=ORIENTED_EDGE ( 'NONE', *, *, #78967, .T. ) ;
#67882=CARTESIAN_POINT ( 'NONE',  ( 9.833493305133805151, 1.593028355512270962E-15, 0.000000000000000000 ) ) ;
#67883=LINE ( 'NONE', #42535, #63329 ) ;
#67903=EDGE_CURVE ( 'NONE', #43534, #22641, #51381, .T. ) ;
#67937=DIRECTION ( 'NONE',  ( -1.000000000000000000, -0.000000000000000000, -0.000000000000000000 ) ) ;
#67986=ORIENTED_EDGE ( 'NONE', *, *, #81028, .F. ) ;
#68013=CARTESIAN_POINT ( 'NONE',  ( 11.08349330513380515, 1.593028355512270962E-15, 0.000000000000000000 ) ) ;
#68040=DIRECTION ( 'NONE',  ( -1.000000000000000000, -0.000000000000000000, -0.000000000000000000 ) ) ;
#68060=FACE_OUTER_BOUND ( 'NONE', #31009, .T. ) ;
#68091=CARTESIAN_POINT ( 'NONE',  ( 35.59999999999999432, 3.309500000000003439, 0.000000000000000000 ) ) ;
#68137=DIRECTION ( 'NONE',  ( 0.000000000000000000, -1.000000000000000000, 0.000000000000000000 ) ) ;
#68140=CIRCLE ( 'NONE', #7837, 6.500000000000000888 ) ;
#68160=EDGE_CURVE ( 'NONE', #88131, #19669, #43149, .T. ) ;
#68168=CARTESIAN_POINT ( 'NONE',  ( 13.58349330513380515, -4.000000000000000000, 4.898587196589415787E-16 ) ) ;
#68175=ORIENTED_EDGE ( 'NONE', *, *, #53030, .T. ) ;
#68193=FACE_OUTER_BOUND ( 'NONE', #41555, .T. ) ;
#68214=EDGE_CURVE ( 'NONE', #36374, #66061, #42769, .T. ) ;
#68231=ORIENTED_EDGE ( 'NONE', *, *, #62636, .T. ) ;
#68232=AXIS2_PLACEMENT_3D ( 'NONE', #77209, #27642, #93405 ) ;
#68247=LINE ( 'NONE', #60704, #38457 ) ;
#68249=CIRCLE ( 'NONE', #69954, 4.000000000000000888 ) ;
#68255=ORIENTED_EDGE ( 'NONE', *, *, #41943, .F. ) ;
#68282=AXIS2_PLACEMENT_3D ( 'NONE', #42882, #35358, #58547 ) ;
#68293=FACE_OUTER_BOUND ( 'NONE', #8808, .T. ) ;
#68337=CONICAL_SURFACE ( 'NONE', #63180, 3.309500000000001663, 0.9599310885968770357 ) ;
#68339=CARTESIAN_POINT ( 'NONE',  ( 10.59999999999999609, 1.533819458162526451E-15, 0.000000000000000000 ) ) ;
#68377=VECTOR ( 'NONE', #12766, 1000.000000000000000 ) ;
#68391=ORIENTED_EDGE ( 'NONE', *, *, #90254, .T. ) ;
#68403=CIRCLE ( 'NONE', #13320, 4.000000000000000888 ) ;
#68431=DIRECTION ( 'NONE',  ( -1.000000000000000000, -0.000000000000000000, -0.000000000000000000 ) ) ;
#68432=VECTOR ( 'NONE', #98818, 1000.000000000000227 ) ;
#68440=CARTESIAN_POINT ( 'NONE',  ( 12.33349330513380693, -4.000000000000000888, 4.898587196589416773E-16 ) ) ;
#68483=DIRECTION ( 'NONE',  ( -1.000000000000000000, -0.000000000000000000, -0.000000000000000000 ) ) ;
#68523=CARTESIAN_POINT ( 'NONE',  ( 0.000000000000000000, 0.000000000000000000, 0.000000000000000000 ) ) ;
#68527=DIRECTION ( 'NONE',  ( 0.000000000000000000, -1.000000000000000000, 0.000000000000000000 ) ) ;
#68549=CARTESIAN_POINT ( 'NONE',  ( 13.86650669486618881, 0.000000000000000000, 4.000000000000000888 ) ) ;
#68570=DIRECTION ( 'NONE',  ( 1.000000000000000000, 0.000000000000000000, 0.000000000000000000 ) ) ;
#68595=CIRCLE ( 'NONE', #18630, 4.000000000000001776 ) ;
#68615=CIRCLE ( 'NONE', #58267, 4.000000000000000888 ) ;
#68649=DIRECTION ( 'NONE',  ( 0.000000000000000000, -1.000000000000000000, 0.000000000000000000 ) ) ;
#68672=DIRECTION ( 'NONE',  ( 0.5735764363510491570, -0.8191520442889895781, 1.003171929053522035E-16 ) ) ;
#68693=VERTEX_POINT ( 'NONE', #7719 ) ;
#68723=CIRCLE ( 'NONE', #106558, 4.000000000000000888 ) ;
#68775=ORIENTED_EDGE ( 'NONE', *, *, #29019, .F. ) ;
#68784=EDGE_CURVE ( 'NONE', #23042, #39006, #66960, .T. ) ;
#68804=AXIS2_PLACEMENT_3D ( 'NONE', #59865, #35606, #43133 ) ;
#68831=DIRECTION ( 'NONE',  ( 0.000000000000000000, 0.000000000000000000, -1.000000000000000000 ) ) ;
#68858=VERTEX_POINT ( 'NONE', #58950 ) ;
#68865=DIRECTION ( 'NONE',  ( -1.000000000000000000, -1.224606353822377258E-16, -0.000000000000000000 ) ) ;
#68885=EDGE_CURVE ( 'NONE', #36374, #54423, #42216, .T. ) ;
#68907=CARTESIAN_POINT ( 'NONE',  ( 23.58349330513380337, 1.593028355512270962E-15, 0.000000000000000000 ) ) ;
#68950=ORIENTED_EDGE ( 'NONE', *, *, #49364, .T. ) ;
#68953=FACE_OUTER_BOUND ( 'NONE', #93757, .T. ) ;
#68979=LINE ( 'NONE', #59821, #7061 ) ;
#69009=LINE ( 'NONE', #60393, #2003 ) ;
#69014=VECTOR ( 'NONE', #42629, 1000.000000000000000 ) ;
#69035=VECTOR ( 'NONE', #21668, 1000.000000000000000 ) ;
#69049=ORIENTED_EDGE ( 'NONE', *, *, #30809, .F. ) ;
#69079=DIRECTION ( 'NONE',  ( -1.000000000000000000, -1.224606353822377258E-16, -0.000000000000000000 ) ) ;
#69087=DIRECTION ( 'NONE',  ( 0.000000000000000000, -1.000000000000000000, 0.000000000000000000 ) ) ;
#69098=AXIS2_PLACEMENT_3D ( 'NONE', #8217, #72939, #71892 ) ;
#69136=LINE ( 'NONE', #20088, #37374 ) ;
#69266=CARTESIAN_POINT ( 'NONE',  ( 6.683837171061806082, 7.911893696991936231, -4.595687358162529387E-16 ) ) ;
#69269=AXIS2_PLACEMENT_3D ( 'NONE', #184, #58466, #33150 ) ;
#69289=( NAMED_UNIT ( * ) PLANE_ANGLE_UNIT ( ) SI_UNIT ( $, .RADIAN. ) );
#69321=ORIENTED_EDGE ( 'NONE', *, *, #52806, .T. ) ;
#69457=ORIENTED_EDGE ( 'NONE', *, *, #81881, .F. ) ;
#69500=FACE_OUTER_BOUND ( 'NONE', #79786, .T. ) ;
#69585=ORIENTED_EDGE ( 'NONE', *, *, #79405, .F. ) ;
#69621=AXIS2_PLACEMENT_3D ( 'NONE', #24014, #54732, #96297 ) ;
#69626=CARTESIAN_POINT ( 'NONE',  ( 8.866506694866188809, 1.474610560812782335E-15, 0.000000000000000000 ) ) ;
#69640=DIRECTION ( 'NONE',  ( 0.000000000000000000, -1.000000000000000000, 0.000000000000000000 ) ) ;
#69650=EDGE_CURVE ( 'NONE', #16458, #11369, #89336, .T. ) ;
#69680=DIRECTION ( 'NONE',  ( 0.000000000000000000, -1.000000000000000000, 0.000000000000000000 ) ) ;
#69717=AXIS2_PLACEMENT_3D ( 'NONE', #50944, #83858, #77371 ) ;
#69736=ORIENTED_EDGE ( 'NONE', *, *, #91290, .F. ) ;
#69754=CONICAL_SURFACE ( 'NONE', #23262, 4.000000000000001776, 0.9599310885968774798 ) ;
#69763=CIRCLE ( 'NONE', #104156, 4.000000000000001776 ) ;
#69832=CARTESIAN_POINT ( 'NONE',  ( 27.61650669486618881, 1.474610560812782335E-15, 0.000000000000000000 ) ) ;
#69837=AXIS2_PLACEMENT_3D ( 'NONE', #54303, #60852, #79137 ) ;
#69838=CIRCLE ( 'NONE', #62990, 4.000000000000001776 ) ;
#69852=DIRECTION ( 'NONE',  ( 0.000000000000000000, -1.000000000000000000, 0.000000000000000000 ) ) ;
#69891=EDGE_LOOP ( 'NONE', ( #39696, #97873, #24944, #66984, #77298 ) ) ;
#69908=ORIENTED_EDGE ( 'NONE', *, *, #61476, .F. ) ;
#69911=LINE ( 'NONE', #86119, #41427 ) ;
#69915=DIRECTION ( 'NONE',  ( -1.000000000000000000, -1.224606353822377258E-16, -0.000000000000000000 ) ) ;
#69954=AXIS2_PLACEMENT_3D ( 'NONE', #46517, #57773, #91766 ) ;
#69980=CONICAL_SURFACE ( 'NONE', #30431, 4.000000000000001776, 0.9599310885968774798 ) ;
#69987=AXIS2_PLACEMENT_3D ( 'NONE', #29832, #44944, #5522 ) ;
#70032=ORIENTED_EDGE ( 'NONE', *, *, #18487, .T. ) ;
#70045=VERTEX_POINT ( 'NONE', #1904 ) ;
#70062=EDGE_LOOP ( 'NONE', ( #21373, #25087, #69908, #63108, #95326 ) ) ;
#70099=CARTESIAN_POINT ( 'NONE',  ( 6.169949891408088583, 6.308465495020067593, 2.073417244832475692 ) ) ;
#70100=DIRECTION ( 'NONE',  ( 0.5735764363510490460, 0.8191520442889896891, 0.000000000000000000 ) ) ;
#70152=EDGE_CURVE ( 'NONE', #59988, #86797, #21330, .T. ) ;
#70171=AXIS2_PLACEMENT_3D ( 'NONE', #73962, #40019, #72890 ) ;
#70183=CARTESIAN_POINT ( 'NONE',  ( 24.34999999999999787, 1.533819458162526451E-15, 0.000000000000000000 ) ) ;
#70184=DIRECTION ( 'NONE',  ( -1.000000000000000000, -1.224606353822377258E-16, -0.000000000000000000 ) ) ;
#70188=CARTESIAN_POINT ( 'NONE',  ( 6.644028492724103785, -3.901260126079907575, 6.757180751914056316 ) ) ;
#70208=DIRECTION ( 'NONE',  ( 0.000000000000000000, -1.000000000000000000, 0.000000000000000000 ) ) ;
#70225=DIRECTION ( 'NONE',  ( -0.5735764363510494901, -0.8191520442889894671, 0.000000000000000000 ) ) ;
#70249=VECTOR ( 'NONE', #14752, 1000.000000000000341 ) ;
#70312=VECTOR ( 'NONE', #73245, 1000.000000000000341 ) ;
#70321=DIRECTION ( 'NONE',  ( 0.000000000000000000, 0.000000000000000000, 1.000000000000000000 ) ) ;
#70337=AXIS2_PLACEMENT_3D ( 'NONE', #23830, #30859, #15689 ) ;
#70367=CARTESIAN_POINT ( 'NONE',  ( 12.61650669486618881, 1.474610560812782335E-15, 0.000000000000000000 ) ) ;
#70396=CARTESIAN_POINT ( 'NONE',  ( 35.59999999999999432, 1.533819458162526451E-15, 0.000000000000000000 ) ) ;
#70412=EDGE_CURVE ( 'NONE', #29177, #40203, #74090, .T. ) ;
#70438=EDGE_CURVE ( 'NONE', #93666, #16458, #105071, .T. ) ;
#70446=DIRECTION ( 'NONE',  ( 0.000000000000000000, 0.000000000000000000, 1.000000000000000000 ) ) ;
#70453=CARTESIAN_POINT ( 'NONE',  ( 30.11650669486618881, 4.000000000000003553, 4.898587196589414801E-16 ) ) ;
#70475=B_SPLINE_CURVE_WITH_KNOTS ( 'NONE', 3,
 ( #387, #74832, #50036, #8514, #48438, #97510 ),
 .UNSPECIFIED., .F., .F.,
 ( 4, 2, 4 ),
 ( 2.380733003137416059E-07, 0.001898835937927372897, 0.003797433802554431997 ),
 .UNSPECIFIED. ) ;
#70480=DIRECTION ( 'NONE',  ( -1.000000000000000000, -1.224606353822377258E-16, -0.000000000000000000 ) ) ;
#70510=ORIENTED_EDGE ( 'NONE', *, *, #77867, .F. ) ;
#70524=ORIENTED_EDGE ( 'NONE', *, *, #104404, .T. ) ;
#70528=CARTESIAN_POINT ( 'NONE',  ( 23.58349330513380337, 1.593028355512270962E-15, 0.000000000000000000 ) ) ;
#70533=CONICAL_SURFACE ( 'NONE', #92917, 3.309500000000001663, 0.9599310885968770357 ) ;
#70595=CIRCLE ( 'NONE', #91234, 0.5999999999999980904 ) ;
#70596=EDGE_CURVE ( 'NONE', #30663, #67595, #46373, .T. ) ;
#70608=VECTOR ( 'NONE', #53295, 1000.000000000000227 ) ;
#70628=ORIENTED_EDGE ( 'NONE', *, *, #64066, .F. ) ;
#70635=DIRECTION ( 'NONE',  ( 0.000000000000000000, 0.000000000000000000, -1.000000000000000000 ) ) ;
#70654=DIRECTION ( 'NONE',  ( 0.000000000000000000, -1.000000000000000000, 0.000000000000000000 ) ) ;
#70690=ORIENTED_EDGE ( 'NONE', *, *, #75502, .F. ) ;
#70706=CYLINDRICAL_SURFACE ( 'NONE', #81803, 4.000000000000000888 ) ;
#70713=AXIS2_PLACEMENT_3D ( 'NONE', #88916, #80271, #63598 ) ;
#70734=AXIS2_PLACEMENT_3D ( 'NONE', #19590, #102583, #28731 ) ;
#70753=ORIENTED_EDGE ( 'NONE', *, *, #93557, .F. ) ;
#70754=DIRECTION ( 'NONE',  ( 0.000000000000000000, 1.000000000000000000, 0.000000000000000000 ) ) ;
#70757=ORIENTED_EDGE ( 'NONE', *, *, #80750, .T. ) ;
#70761=UNCERTAINTY_MEASURE_WITH_UNIT (LENGTH_MEASURE( 1.000000000000000082E-05 ), #14790, 'distance_accuracy_value', 'NONE');
#70777=VECTOR ( 'NONE', #70225, 1000.000000000000000 ) ;
#70819=ADVANCED_FACE ( 'NONE', ( #74750 ), #60427, .T. ) ;
#70821=CARTESIAN_POINT ( 'NONE',  ( 6.289692432696817548, -6.589071317540658335, 2.245373559999283231 ) ) ;
#70825=FACE_OUTER_BOUND ( 'NONE', #33085, .T. ) ;
#70833=DIRECTION ( 'NONE',  ( 0.000000000000000000, -1.000000000000000000, 0.000000000000000000 ) ) ;
#70838=CIRCLE ( 'NONE', #62244, 3.309500000000001663 ) ;
#70856=EDGE_CURVE ( 'NONE', #81142, #83206, #98496, .T. ) ;
#70878=CARTESIAN_POINT ( 'NONE',  ( 36.08349330513379982, -4.000000000000000000, 4.898587196589415787E-16 ) ) ;
#70885=DIRECTION ( 'NONE',  ( -0.5735764363510494901, -0.8191520442889894671, 0.000000000000000000 ) ) ;
#70897=DIRECTION ( 'NONE',  ( 0.000000000000000000, -1.000000000000000000, 0.000000000000000000 ) ) ;
#70917=FACE_OUTER_BOUND ( 'NONE', #94989, .T. ) ;
#70929=FACE_OUTER_BOUND ( 'NONE', #43516, .T. ) ;
#70939=AXIS2_PLACEMENT_3D ( 'NONE', #25608, #7772, #50352 ) ;
#70973=AXIS2_PLACEMENT_3D ( 'NONE', #5103, #38545, #95184 ) ;
#70998=AXIS2_PLACEMENT_3D ( 'NONE', #67424, #92745, #98695 ) ;
#71002=CARTESIAN_POINT ( 'NONE',  ( 6.162888688655344005, 3.752776749732565253, 6.499999999999997335 ) ) ;
#71006=EDGE_CURVE ( 'NONE', #88800, #51129, #89504, .T. ) ;
#71035=ORIENTED_EDGE ( 'NONE', *, *, #25067, .T. ) ;
#71041=CARTESIAN_POINT ( 'NONE',  ( 6.936184427528457874, 1.053834543709838281E-15, 8.605212085995399107 ) ) ;
#71055=CARTESIAN_POINT ( 'NONE',  ( 6.692429545713704186, 4.002214399422197033, -6.852332219948825021 ) ) ;
#71062=ADVANCED_FACE ( 'NONE', ( #70929 ), #22414, .F. ) ;
#71064=CARTESIAN_POINT ( 'NONE',  ( 18.58349330513380693, -4.000000000000000000, 4.898587196589415787E-16 ) ) ;
#71080=ORIENTED_EDGE ( 'NONE', *, *, #8078, .T. ) ;
#71083=VERTEX_POINT ( 'NONE', #21883 ) ;
#71085=CARTESIAN_POINT ( 'NONE',  ( 25.59999999999999787, -3.309499999999999886, 0.000000000000000000 ) ) ;
#71145=CARTESIAN_POINT ( 'NONE',  ( 0.000000000000000000, 0.000000000000000000, 4.000000000000000888 ) ) ;
#71157=CARTESIAN_POINT ( 'NONE',  ( 23.58349330513380337, 4.898587196589411843E-16, -4.000000000000001776 ) ) ;
#71165=VECTOR ( 'NONE', #39823, 1000.000000000000341 ) ;
#71166=ORIENTED_EDGE ( 'NONE', *, *, #47551, .F. ) ;
#71252=EDGE_CURVE ( 'NONE', #17049, #28856, #20179, .T. ) ;
#71266=ORIENTED_EDGE ( 'NONE', *, *, #75581, .F. ) ;
#71276=DIRECTION ( 'NONE',  ( -1.000000000000000000, -1.224606353822377258E-16, -0.000000000000000000 ) ) ;
#71318=CIRCLE ( 'NONE', #7627, 4.000000000000001776 ) ;
#71329=LINE ( 'NONE', #38981, #49587 ) ;
#71367=ORIENTED_EDGE ( 'NONE', *, *, #65918, .T. ) ;
#71369=AXIS2_PLACEMENT_3D ( 'NONE', #88718, #73032, #105942 ) ;
#71371=ORIENTED_EDGE ( 'NONE', *, *, #1013, .T. ) ;
#71388=VECTOR ( 'NONE', #56919, 1000.000000000000114 ) ;
#71411=DIRECTION ( 'NONE',  ( -1.000000000000000000, -1.224606353822377258E-16, -0.000000000000000000 ) ) ;
#71420=DIRECTION ( 'NONE',  ( 0.5735764363510490460, 0.8191520442889896891, 0.000000000000000000 ) ) ;
#71423=FACE_OUTER_BOUND ( 'NONE', #8589, .T. ) ;
#71430=ORIENTED_EDGE ( 'NONE', *, *, #17612, .F. ) ;
#71432=DIRECTION ( 'NONE',  ( 0.000000000000000000, -1.000000000000000000, 0.000000000000000000 ) ) ;
#71449=ADVANCED_FACE ( 'NONE', ( #79419 ), #79939, .T. ) ;
#71452=DIRECTION ( 'NONE',  ( 0.000000000000000000, -1.000000000000000000, 0.000000000000000000 ) ) ;
#71475=AXIS2_PLACEMENT_3D ( 'NONE', #11273, #62004, #28056 ) ;
#71494=DIRECTION ( 'NONE',  ( 1.000000000000000000, 1.224606353822377258E-16, 0.000000000000000000 ) ) ;
#71503=CARTESIAN_POINT ( 'NONE',  ( 6.162888688655347558, -3.752776749732574135, -6.500000000000001776 ) ) ;
#71505=ORIENTED_EDGE ( 'NONE', *, *, #60362, .T. ) ;
#71510=CIRCLE ( 'NONE', #99071, 3.309500000000001663 ) ;
#71549=CARTESIAN_POINT ( 'NONE',  ( 31.08349330513380693, 1.593028355512270962E-15, 0.000000000000000000 ) ) ;
#71641=CARTESIAN_POINT ( 'NONE',  ( 24.83349330513380693, -3.851859888774471706E-31, 4.000000000000001776 ) ) ;
#71649=CARTESIAN_POINT ( 'NONE',  ( 26.84999999999999787, 3.309500000000003439, 4.052968581778167743E-16 ) ) ;
#71672=CARTESIAN_POINT ( 'NONE',  ( 5.975663821521244756, 4.257391242883541871, 5.625982059626890575 ) ) ;
#71690=VERTEX_POINT ( 'NONE', #52354 ) ;
#71742=EDGE_CURVE ( 'NONE', #88131, #83796, #31022, .T. ) ;
#71749=ADVANCED_FACE ( 'NONE', ( #34095 ), #61009, .T. ) ;
#71822=CARTESIAN_POINT ( 'NONE',  ( 26.08349330513380693, -4.000000000000000888, 4.898587196589416773E-16 ) ) ;
#71865=CARTESIAN_POINT ( 'NONE',  ( 6.169949891409288512, -6.308465495019287772, 2.073417244830710437 ) ) ;
#71892=DIRECTION ( 'NONE',  ( 0.000000000000000000, -1.000000000000000000, 0.000000000000000000 ) ) ;
#71901=AXIS2_PLACEMENT_3D ( 'NONE', #38885, #96057, #15648 ) ;
#72018=FACE_OUTER_BOUND ( 'NONE', #7479, .T. ) ;
#72024=EDGE_CURVE ( 'NONE', #90625, #75208, #13227, .T. ) ;
#72029=CYLINDRICAL_SURFACE ( 'NONE', #103414, 4.000000000000000888 ) ;
#72044=ORIENTED_EDGE ( 'NONE', *, *, #72686, .F. ) ;
#72050=AXIS2_PLACEMENT_3D ( 'NONE', #9084, #24776, #92134 ) ;
#72062=CARTESIAN_POINT ( 'NONE',  ( 9.349999999999997868, 1.533819458162526451E-15, 0.000000000000000000 ) ) ;
#72080=ORIENTED_EDGE ( 'NONE', *, *, #34197, .T. ) ;
#72114=DIRECTION ( 'NONE',  ( -1.000000000000000000, -1.224606353822377258E-16, -0.000000000000000000 ) ) ;
#72132=DIRECTION ( 'NONE',  ( 0.000000000000000000, -1.000000000000000000, 0.000000000000000000 ) ) ;
#72147=AXIS2_PLACEMENT_3D ( 'NONE', #14465, #32291, #6383 ) ;
#72178=CARTESIAN_POINT ( 'NONE',  ( 8.866506694866188809, 1.474610560812782335E-15, 0.000000000000000000 ) ) ;
#72214=EDGE_CURVE ( 'NONE', #40203, #29177, #29408, .T. ) ;
#72229=FACE_OUTER_BOUND ( 'NONE', #88717, .T. ) ;
#72268=VERTEX_POINT ( 'NONE', #16420 ) ;
#72298=DIRECTION ( 'NONE',  ( 0.000000000000000000, 0.000000000000000000, 1.000000000000000000 ) ) ;
#72310=DIRECTION ( 'NONE',  ( 0.000000000000000000, 1.000000000000000000, 0.000000000000000000 ) ) ;
#72343=ORIENTED_EDGE ( 'NONE', *, *, #83019, .T. ) ;
#72344=AXIS2_PLACEMENT_3D ( 'NONE', #46590, #4015, #53097 ) ;
#72358=ORIENTED_EDGE ( 'NONE', *, *, #98081, .T. ) ;
#72376=VERTEX_POINT ( 'NONE', #13096 ) ;
#72384=AXIS2_PLACEMENT_3D ( 'NONE', #66114, #33776, #8933 ) ;
#72402=CARTESIAN_POINT ( 'NONE',  ( 6.692588830498425345, -3.932766476276031486, 6.892929031562514020 ) ) ;
#72445=CARTESIAN_POINT ( 'NONE',  ( 6.562934840145641324, -4.277581483015143071, -6.282640795011896984 ) ) ;
#72446=ORIENTED_EDGE ( 'NONE', *, *, #51491, .F. ) ;
#72461=DIRECTION ( 'NONE',  ( 0.000000000000000000, -1.000000000000000000, 0.000000000000000000 ) ) ;
#72468=EDGE_CURVE ( 'NONE', #94380, #47192, #46023, .T. ) ;
#72474=EDGE_CURVE ( 'NONE', #84766, #22594, #63801, .T. ) ;
#72487=DIRECTION ( 'NONE',  ( -1.000000000000000000, -0.000000000000000000, -0.000000000000000000 ) ) ;
#72497=CARTESIAN_POINT ( 'NONE',  ( 15.59999999999999787, 3.309500000000003439, 4.052968581778167743E-16 ) ) ;
#72510=DIRECTION ( 'NONE',  ( -1.000000000000000000, -1.224606353822377258E-16, -0.000000000000000000 ) ) ;
#72531=DIRECTION ( 'NONE',  ( 1.000000000000000000, 1.224606353822377258E-16, 0.000000000000000000 ) ) ;
#72576=VECTOR ( 'NONE', #44223, 1000.000000000000000 ) ;
#72595=ADVANCED_FACE ( 'NONE', ( #49722 ), #3579, .F. ) ;
#72618=AXIS2_PLACEMENT_3D ( 'NONE', #10112, #83466, #74829 ) ;
#72623=ORIENTED_EDGE ( 'NONE', *, *, #103836, .F. ) ;
#72636=ORIENTED_EDGE ( 'NONE', *, *, #80919, .T. ) ;
#72641=CARTESIAN_POINT ( 'NONE',  ( 6.167866516170009028, -1.339763354874886181, -6.500000000000000000 ) ) ;
#72674=DIRECTION ( 'NONE',  ( 1.000000000000000000, 1.224606353822377258E-16, 0.000000000000000000 ) ) ;
#72686=EDGE_CURVE ( 'NONE', #52389, #18709, #54129, .T. ) ;
#72707=ORIENTED_EDGE ( 'NONE', *, *, #15874, .F. ) ;
#72734=CARTESIAN_POINT ( 'NONE',  ( 0.1061556211655333148, 4.836380039389418961, -4.623144047065555817 ) ) ;
#72735=DIRECTION ( 'NONE',  ( 0.000000000000000000, -1.000000000000000000, 0.000000000000000000 ) ) ;
#72741=CARTESIAN_POINT ( 'NONE',  ( 28.86650669486618881, 4.000000000000003553, 4.898587196589414801E-16 ) ) ;
#72748=CARTESIAN_POINT ( 'NONE',  ( 27.33349330513380693, 4.000000000000003553, 0.000000000000000000 ) ) ;
#72750=B_SPLINE_CURVE_WITH_KNOTS ( 'NONE', 3,
 ( #56364, #39695, #73619, #49345, #65548, #71503 ),
 .UNSPECIFIED., .F., .F.,
 ( 4, 2, 4 ),
 ( -4.698498716301074466E-06, 0.0003457374136928007598, 0.0006961733261019026602 ),
 .UNSPECIFIED. ) ;
#72802=EDGE_CURVE ( 'NONE', #45785, #84766, #57080, .T. ) ;
#72803=ORIENTED_EDGE ( 'NONE', *, *, #54122, .T. ) ;
#72826=VECTOR ( 'NONE', #61880, 1000.000000000000000 ) ;
#72855=ADVANCED_FACE ( 'NONE', ( #68060 ), #37960, .T. ) ;
#72857=CARTESIAN_POINT ( 'NONE',  ( 36.36650669486618881, 4.898587196589413815E-16, -4.000000000000000888 ) ) ;
#72858=CARTESIAN_POINT ( 'NONE',  ( 27.61650669486618881, 1.474610560812782335E-15, 0.000000000000000000 ) ) ;
#72890=DIRECTION ( 'NONE',  ( 0.000000000000000000, 1.000000000000000000, 0.000000000000000000 ) ) ;
#72895=B_SPLINE_CURVE_WITH_KNOTS ( 'NONE', 3,
 ( #53478, #93941, #95017, #54503, #70188, #62126 ),
 .UNSPECIFIED., .F., .F.,
 ( 4, 2, 4 ),
 ( 0.000000000000000000, 0.0003491763592121710546, 0.0006983527184243421091 ),
 .UNSPECIFIED. ) ;
#72920=CARTESIAN_POINT ( 'NONE',  ( 6.692649838135033669, 4.003395468798082391, 6.852343244299697211 ) ) ;
#72929=CARTESIAN_POINT ( 'NONE',  ( 14.83349330513380693, -4.000000000000000888, 4.898587196589416773E-16 ) ) ;
#72939=DIRECTION ( 'NONE',  ( -1.000000000000000000, -1.224606353822377258E-16, -0.000000000000000000 ) ) ;
#72960=CARTESIAN_POINT ( 'NONE',  ( 6.463481858019718196, -4.600809706232204199, -5.711197301637628065 ) ) ;
#72971=DIRECTION ( 'NONE',  ( 0.000000000000000000, 0.000000000000000000, 1.000000000000000000 ) ) ;
#72972=CARTESIAN_POINT ( 'NONE',  ( 18.09999999999999787, 1.533819458162526451E-15, 0.000000000000000000 ) ) ;
#72977=ORIENTED_EDGE ( 'NONE', *, *, #16901, .F. ) ;
#72980=FACE_OUTER_BOUND ( 'NONE', #38323, .T. ) ;
#72996=ORIENTED_EDGE ( 'NONE', *, *, #46707, .T. ) ;
#73006=ORIENTED_EDGE ( 'NONE', *, *, #87722, .T. ) ;
#73019=ORIENTED_EDGE ( 'NONE', *, *, #41160, .F. ) ;
#73020=B_SPLINE_CURVE_WITH_KNOTS ( 'NONE', 3,
 ( #46920, #15083, #6452, #82885, #104629, #87930 ),
 .UNSPECIFIED., .F., .F.,
 ( 4, 2, 4 ),
 ( 0.006874058789394425426, 0.008773169699889938472, 0.01067228061038545325 ),
 .UNSPECIFIED. ) ;
#73028=LINE ( 'NONE', #67094, #4923 ) ;
#73030=AXIS2_PLACEMENT_3D ( 'NONE', #50247, #91783, #90180 ) ;
#73032=DIRECTION ( 'NONE',  ( -1.000000000000000000, -1.224606353822377258E-16, -0.000000000000000000 ) ) ;
#73038=VERTEX_POINT ( 'NONE', #86920 ) ;
#73101=EDGE_CURVE ( 'NONE', #43534, #66536, #93939, .T. ) ;
#73115=ORIENTED_EDGE ( 'NONE', *, *, #74349, .F. ) ;
#73128=CARTESIAN_POINT ( 'NONE',  ( 0.000000000000000000, 0.000000000000000000, 0.000000000000000000 ) ) ;
#73156=CARTESIAN_POINT ( 'NONE',  ( 6.683837171061803417, 3.955946848495959234, -6.851900933636991375 ) ) ;
#73180=EDGE_CURVE ( 'NONE', #55436, #74451, #77647, .T. ) ;
#73212=ORIENTED_EDGE ( 'NONE', *, *, #51491, .T. ) ;
#73224=ORIENTED_EDGE ( 'NONE', *, *, #57590, .T. ) ;
#73245=DIRECTION ( 'NONE',  ( 0.5735764363510490460, 0.8191520442889896891, 0.000000000000000000 ) ) ;
#73256=CARTESIAN_POINT ( 'NONE',  ( 0.5805565836007616776, 3.752776749732562589, -6.500000000000000888 ) ) ;
#73288=CARTESIAN_POINT ( 'NONE',  ( 24.83349330513380693, 1.593028355512270962E-15, 0.000000000000000000 ) ) ;
#73299=DIRECTION ( 'NONE',  ( -1.000000000000000000, -1.224606353822377258E-16, -0.000000000000000000 ) ) ;
#73306=LINE ( 'NONE', #65237, #94082 ) ;
#73315=ORIENTED_EDGE ( 'NONE', *, *, #57313, .T. ) ;
#73323=DIRECTION ( 'NONE',  ( 0.000000000000000000, -1.000000000000000000, 0.000000000000000000 ) ) ;
#73348=ORIENTED_EDGE ( 'NONE', *, *, #52278, .T. ) ;
#73373=AXIS2_PLACEMENT_3D ( 'NONE', #22803, #23325, #30900 ) ;
#73378=DIRECTION ( 'NONE',  ( 0.000000000000000000, -1.000000000000000000, 0.000000000000000000 ) ) ;
#73402=VECTOR ( 'NONE', #31753, 1000.000000000000000 ) ;
#73404=DIRECTION ( 'NONE',  ( -1.000000000000000000, -1.224606353822377258E-16, -0.000000000000000000 ) ) ;
#73406=CIRCLE ( 'NONE', #59670, 4.000000000000000888 ) ;
#73408=FACE_OUTER_BOUND ( 'NONE', #40142, .T. ) ;
#73409=DIRECTION ( 'NONE',  ( 0.000000000000000000, 1.000000000000000000, 0.000000000000000000 ) ) ;
#73429=CARTESIAN_POINT ( 'NONE',  ( 37.33349330513379982, 1.593028355512270962E-15, 0.000000000000000000 ) ) ;
#73454=CARTESIAN_POINT ( 'NONE',  ( 6.449804269883611774, -2.701269212710093459, 6.840189325177291835 ) ) ;
#73459=AXIS2_PLACEMENT_3D ( 'NONE', #21438, #86701, #102864 ) ;
#73478=ORIENTED_EDGE ( 'NONE', *, *, #1825, .T. ) ;
#73491=EDGE_CURVE ( 'NONE', #71083, #35336, #19436, .T. ) ;
#73536=CARTESIAN_POINT ( 'NONE',  ( 21.08349330513380693, 1.593028355512270962E-15, 0.000000000000000000 ) ) ;
#73565=DIRECTION ( 'NONE',  ( -1.000000000000000000, -1.224606353822377258E-16, -0.000000000000000000 ) ) ;
#73576=CARTESIAN_POINT ( 'NONE',  ( 11.84999999999999787, 1.533819458162526451E-15, 0.000000000000000000 ) ) ;
#73588=CARTESIAN_POINT ( 'NONE',  ( 6.683837171061803417, -3.955946848495962787, 6.851900933636989599 ) ) ;
#73605=ORIENTED_EDGE ( 'NONE', *, *, #78564, .F. ) ;
#73619=CARTESIAN_POINT ( 'NONE',  ( 6.575918192882435065, -3.850883087735915922, -6.669925161966313354 ) ) ;
#73653=CONICAL_SURFACE ( 'NONE', #46125, 3.309500000000001663, 0.9599310885968770357 ) ;
#73654=B_SPLINE_CURVE_WITH_KNOTS ( 'NONE', 3,
 ( #28618, #94390, #61499, #29162, #72734, #80294, #56548, #73256 ),
 .UNSPECIFIED., .F., .F.,
 ( 4, 2, 2, 4 ),
 ( 0.003797433802554452380, 0.004743183970586247432, 0.005688934138618043784, 0.007580434474681633887 ),
 .UNSPECIFIED. ) ;
#73666=EDGE_CURVE ( 'NONE', #93357, #88074, #24390, .T. ) ;
#73694=ORIENTED_EDGE ( 'NONE', *, *, #8243, .F. ) ;
#73736=EDGE_LOOP ( 'NONE', ( #23318, #90455, #86435, #66939, #50911, #59118 ) ) ;
#73739=DIRECTION ( 'NONE',  ( 0.000000000000000000, -1.000000000000000000, 0.000000000000000000 ) ) ;
#73749=CARTESIAN_POINT ( 'NONE',  ( 0.000000000000000000, 0.000000000000000000, 0.000000000000000000 ) ) ;
#73759=DIRECTION ( 'NONE',  ( -1.000000000000000000, -0.000000000000000000, -0.000000000000000000 ) ) ;
#73763=EDGE_LOOP ( 'NONE', ( #17789, #49259, #9908, #9601, #16961 ) ) ;
#73785=CIRCLE ( 'NONE', #87595, 4.000000000000001776 ) ;
#73846=CARTESIAN_POINT ( 'NONE',  ( 36.08349330513379982, 1.593028355512270962E-15, 0.000000000000000000 ) ) ;
#73861=ORIENTED_EDGE ( 'NONE', *, *, #37039, .T. ) ;
#73905=CIRCLE ( 'NONE', #27466, 4.000000000000001776 ) ;
#73921=EDGE_LOOP ( 'NONE', ( #32600, #7585, #1203, #54889, #74978 ) ) ;
#73938=EDGE_CURVE ( 'NONE', #77629, #3065, #35480, .T. ) ;
#73962=CARTESIAN_POINT ( 'NONE',  ( 9.833493305133805151, 1.593028355512270962E-15, 0.000000000000000000 ) ) ;
#73985=CONICAL_SURFACE ( 'NONE', #75679, 4.000000000000001776, 0.9599310885968774798 ) ;
#74002=EDGE_LOOP ( 'NONE', ( #39920, #26646, #66453, #43688, #21168 ) ) ;
#74081=AXIS2_PLACEMENT_3D ( 'NONE', #102013, #18471, #61048 ) ;
#74086=CARTESIAN_POINT ( 'NONE',  ( 16.36650669486618881, 4.000000000000003553, 4.898587196589414801E-16 ) ) ;
#74090=CIRCLE ( 'NONE', #27656, 4.000000000000001776 ) ;
#74097=DIRECTION ( 'NONE',  ( -0.5735764363510497121, 0.8191520442889892450, 1.003171929053521665E-16 ) ) ;
#74110=EDGE_LOOP ( 'NONE', ( #81903, #102783, #13897, #92769 ) ) ;
#74116=CARTESIAN_POINT ( 'NONE',  ( 32.33349330513380693, -4.000000000000000000, 4.898587196589415787E-16 ) ) ;
#74139=ORIENTED_EDGE ( 'NONE', *, *, #6506, .T. ) ;
#74176=CARTESIAN_POINT ( 'NONE',  ( 34.83349330513380693, -4.000000000000000000, 4.898587196589415787E-16 ) ) ;
#74197=AXIS2_PLACEMENT_3D ( 'NONE', #93772, #75982, #44160 ) ;
#74206=DIRECTION ( 'NONE',  ( -1.000000000000000000, -1.224606353822377258E-16, -0.000000000000000000 ) ) ;
#74223=AXIS2_PLACEMENT_3D ( 'NONE', #32116, #87699, #30008 ) ;
#74272=AXIS2_PLACEMENT_3D ( 'NONE', #55817, #39685, #55304 ) ;
#74309=DIRECTION ( 'NONE',  ( -0.000000000000000000, 0.000000000000000000, -1.000000000000000000 ) ) ;
#74349=EDGE_CURVE ( 'NONE', #96401, #1420, #92477, .T. ) ;
#74447=ORIENTED_EDGE ( 'NONE', *, *, #51284, .F. ) ;
#74451=VERTEX_POINT ( 'NONE', #84932 ) ;
#74455=CARTESIAN_POINT ( 'NONE',  ( 0.000000000000000000, 0.000000000000000000, 4.000000000000000888 ) ) ;
#74461=DIRECTION ( 'NONE',  ( 0.000000000000000000, 0.000000000000000000, 1.000000000000000000 ) ) ;
#74472=EDGE_CURVE ( 'NONE', #43607, #36441, #80535, .T. ) ;
#74495=ORIENTED_EDGE ( 'NONE', *, *, #31661, .F. ) ;
#74503=FACE_OUTER_BOUND ( 'NONE', #10725, .T. ) ;
#74504=CARTESIAN_POINT ( 'NONE',  ( 23.86650669486618881, 1.474610560812782335E-15, 0.000000000000000000 ) ) ;
#74523=CARTESIAN_POINT ( 'NONE',  ( 6.352644769543715597, 2.685840869108905071, 6.499999999999998224 ) ) ;
#74542=AXIS2_PLACEMENT_3D ( 'NONE', #84762, #68040, #94462 ) ;
#74560=AXIS2_PLACEMENT_3D ( 'NONE', #74836, #41421, #8517 ) ;
#74579=CARTESIAN_POINT ( 'NONE',  ( 31.36650669486618881, 4.000000000000003553, 4.898587196589414801E-16 ) ) ;
#74587=LINE ( 'NONE', #48188, #56967 ) ;
#74605=CARTESIAN_POINT ( 'NONE',  ( 17.33349330513380693, 1.593028355512270962E-15, 0.000000000000000000 ) ) ;
#74618=ADVANCED_FACE ( 'NONE', ( #92624 ), #25267, .F. ) ;
#74653=VERTEX_POINT ( 'NONE', #75911 ) ;
#74670=LINE ( 'NONE', #753, #62769 ) ;
#74713=DIRECTION ( 'NONE',  ( 0.000000000000000000, 0.000000000000000000, 1.000000000000000000 ) ) ;
#74745=ORIENTED_EDGE ( 'NONE', *, *, #1355, .F. ) ;
#74750=FACE_OUTER_BOUND ( 'NONE', #99506, .T. ) ;
#74771=CARTESIAN_POINT ( 'NONE',  ( 6.463344223170841119, 7.245769408789096033, 1.129975644293424120 ) ) ;
#74829=DIRECTION ( 'NONE',  ( 0.000000000000000000, -0.5000000000000009992, -0.8660254037844380415 ) ) ;
#74832=CARTESIAN_POINT ( 'NONE',  ( 0.4033376246892471650, 4.059728990630802947, 5.968343123267131567 ) ) ;
#74836=CARTESIAN_POINT ( 'NONE',  ( 10.11650669486618881, 1.474610560812782335E-15, 0.000000000000000000 ) ) ;
#74849=FACE_OUTER_BOUND ( 'NONE', #46036, .T. ) ;
#74850=ADVANCED_FACE ( 'NONE', ( #5739 ), #62407, .T. ) ;
#74871=DIRECTION ( 'NONE',  ( 1.000000000000000000, 1.224606353822377258E-16, 0.000000000000000000 ) ) ;
#74881=CARTESIAN_POINT ( 'NONE',  ( 13.09999999999999787, -3.309499999999999886, 0.000000000000000000 ) ) ;
#74887=VECTOR ( 'NONE', #44549, 1000.000000000000227 ) ;
#74957=DIRECTION ( 'NONE',  ( -1.000000000000000000, -1.224606353822377258E-16, -0.000000000000000000 ) ) ;
#74974=DIRECTION ( 'NONE',  ( -0.5735764363510497121, 0.8191520442889892450, 1.003171929053521665E-16 ) ) ;
#74978=ORIENTED_EDGE ( 'NONE', *, *, #27606, .F. ) ;
#75013=ORIENTED_EDGE ( 'NONE', *, *, #18641, .F. ) ;
#75045=CARTESIAN_POINT ( 'NONE',  ( 6.291779652043022253, -1.386462189980468773, 6.829130021847237053 ) ) ;
#75049=DIRECTION ( 'NONE',  ( 0.000000000000000000, -1.000000000000000000, 0.000000000000000000 ) ) ;
#75054=CIRCLE ( 'NONE', #25131, 4.000000000000001776 ) ;
#75076=DIRECTION ( 'NONE',  ( -1.000000000000000000, -1.224606353822377258E-16, -0.000000000000000000 ) ) ;
#75111=VECTOR ( 'NONE', #100782, 1000.000000000000000 ) ;
#75119=DIRECTION ( 'NONE',  ( 0.000000000000000000, -1.000000000000000000, 0.000000000000000000 ) ) ;
#75121=ORIENTED_EDGE ( 'NONE', *, *, #98815, .F. ) ;
#75140=ORIENTED_EDGE ( 'NONE', *, *, #77329, .F. ) ;
#75148=ORIENTED_EDGE ( 'NONE', *, *, #31364, .T. ) ;
#75151=EDGE_CURVE ( 'NONE', #104988, #78191, #786, .T. ) ;
#75172=CARTESIAN_POINT ( 'NONE',  ( 30.59999999999999787, 1.533819458162526451E-15, 0.000000000000000000 ) ) ;
#75183=CARTESIAN_POINT ( 'NONE',  ( 23.86650669486618881, 1.474610560812782335E-15, 0.000000000000000000 ) ) ;
#75191=LINE ( 'NONE', #35860, #39750 ) ;
#75208=VERTEX_POINT ( 'NONE', #82814 ) ;
#75210=AXIS2_PLACEMENT_3D ( 'NONE', #91489, #93073, #36477 ) ;
#75224=EDGE_CURVE ( 'NONE', #48529, #79927, #26223, .T. ) ;
#75251=EDGE_LOOP ( 'NONE', ( #11781, #48892, #17844, #95001, #62162 ) ) ;
#75265=ADVANCED_FACE ( 'NONE', ( #27286 ), #60170, .T. ) ;
#75281=CARTESIAN_POINT ( 'NONE',  ( 6.326592304916277776, -5.253140224433048289, 4.564380808752273033 ) ) ;
#75285=ADVANCED_FACE ( 'NONE', ( #59623 ), #83341, .F. ) ;
#75300=DIRECTION ( 'NONE',  ( -1.000000000000000000, -0.000000000000000000, -0.000000000000000000 ) ) ;
#75341=DIRECTION ( 'NONE',  ( -1.000000000000000000, -1.224606353822377258E-16, -0.000000000000000000 ) ) ;
#75367=CIRCLE ( 'NONE', #63312, 4.000000000000001776 ) ;
#75403=VERTEX_POINT ( 'NONE', #44498 ) ;
#75408=CARTESIAN_POINT ( 'NONE',  ( 17.61650669486618881, 1.474610560812782335E-15, 0.000000000000000000 ) ) ;
#75417=EDGE_CURVE ( 'NONE', #14833, #31177, #78437, .T. ) ;
#75438=DIRECTION ( 'NONE',  ( -0.5735764363510497121, 0.8191520442889892450, 1.003171929053521665E-16 ) ) ;
#75474=EDGE_CURVE ( 'NONE', #9148, #86058, #61736, .T. ) ;
#75502=EDGE_CURVE ( 'NONE', #42319, #25738, #88142, .T. ) ;
#75549=CARTESIAN_POINT ( 'NONE',  ( 23.58349330513380337, 1.593028355512270962E-15, 0.000000000000000000 ) ) ;
#75555=EDGE_CURVE ( 'NONE', #90250, #22641, #104300, .T. ) ;
#75580=CARTESIAN_POINT ( 'NONE',  ( 25.59999999999999787, -3.309499999999999886, 4.475777889183790779E-16 ) ) ;
#75581=EDGE_CURVE ( 'NONE', #8034, #94433, #32575, .T. ) ;
#75616=AXIS2_PLACEMENT_3D ( 'NONE', #102770, #4078, #45612 ) ;
#75639=CARTESIAN_POINT ( 'NONE',  ( 16.84999999999999787, 3.309500000000003439, 0.000000000000000000 ) ) ;
#75679=AXIS2_PLACEMENT_3D ( 'NONE', #74605, #685, #26125 ) ;
#75694=LINE ( 'NONE', #57372, #99244 ) ;
#75715=AXIS2_PLACEMENT_3D ( 'NONE', #80070, #37543, #13206 ) ;
#75762=CARTESIAN_POINT ( 'NONE',  ( 0.000000000000000000, 0.000000000000000000, 4.000000000000000888 ) ) ;
#75776=ORIENTED_EDGE ( 'NONE', *, *, #48512, .F. ) ;
#75814=CARTESIAN_POINT ( 'NONE',  ( 15.59999999999999787, -3.309499999999999886, 0.000000000000000000 ) ) ;
#75831=LINE ( 'NONE', #67749, #74887 ) ;
#75863=AXIS2_PLACEMENT_3D ( 'NONE', #36383, #61152, #53055 ) ;
#75894=AXIS2_PLACEMENT_3D ( 'NONE', #5475, #30304, #63192 ) ;
#75905=DIRECTION ( 'NONE',  ( 0.000000000000000000, 1.000000000000000000, 0.000000000000000000 ) ) ;
#75911=CARTESIAN_POINT ( 'NONE',  ( 33.86650669486618881, 4.000000000000003553, 4.898587196589414801E-16 ) ) ;
#75915=DIRECTION ( 'NONE',  ( 0.000000000000000000, -1.000000000000000000, 0.000000000000000000 ) ) ;
#75930=AXIS2_PLACEMENT_3D ( 'NONE', #29494, #69915, #102816 ) ;
#75939=ADVANCED_FACE ( 'NONE', ( #104707 ), #44551, .T. ) ;
#75981=DIRECTION ( 'NONE',  ( -1.000000000000000000, -1.224606353822377258E-16, -0.000000000000000000 ) ) ;
#75982=DIRECTION ( 'NONE',  ( -1.000000000000000000, -1.224606353822377258E-16, -0.000000000000000000 ) ) ;
#75988=CARTESIAN_POINT ( 'NONE',  ( 21.08349330513380693, -4.000000000000000888, 4.898587196589416773E-16 ) ) ;
#76032=CARTESIAN_POINT ( 'NONE',  ( 0.000000000000000000, 0.000000000000000000, 4.000000000000000888 ) ) ;
#76041=CARTESIAN_POINT ( 'NONE',  ( 15.59999999999999787, 1.533819458162526451E-15, 0.000000000000000000 ) ) ;
#76048=B_SPLINE_CURVE_WITH_KNOTS ( 'NONE', 3,
 ( #63927, #56311, #89250, #81137, #5669, #22421 ),
 .UNSPECIFIED., .F., .F.,
 ( 4, 2, 4 ),
 ( 0.01067228061038545325, 0.01257272967564229682, 0.01447317874089914212 ),
 .UNSPECIFIED. ) ;
#76054=DIRECTION ( 'NONE',  ( -0.5735764363510497121, 0.8191520442889892450, 1.003171929053521665E-16 ) ) ;
#76069=ADVANCED_FACE ( 'NONE', ( #65317 ), #32971, .T. ) ;
#76074=DIRECTION ( 'NONE',  ( 1.000000000000000000, 0.000000000000000000, -0.000000000000000000 ) ) ;
#76101=DIRECTION ( 'NONE',  ( 0.000000000000000000, -1.000000000000000000, 0.000000000000000000 ) ) ;
#76113=CIRCLE ( 'NONE', #77814, 3.309500000000001663 ) ;
#76121=DIRECTION ( 'NONE',  ( 0.5735764363510491570, -0.8191520442889895781, 1.003171929053522035E-16 ) ) ;
#76132=ORIENTED_EDGE ( 'NONE', *, *, #64591, .F. ) ;
#76152=CARTESIAN_POINT ( 'NONE',  ( 5.691929483231187525, -5.629165124598856984, -3.250000000000002220 ) ) ;
#76160=ADVANCED_FACE ( 'NONE', ( #27020 ), #54831, .T. ) ;
#76166=DIRECTION ( 'NONE',  ( -1.000000000000000000, -1.224606353822377258E-16, -0.000000000000000000 ) ) ;
#76249=CARTESIAN_POINT ( 'NONE',  ( 31.08349330513380693, 4.000000000000003553, 0.000000000000000000 ) ) ;
#76252=LINE ( 'NONE', #68168, #26401 ) ;
#76279=ORIENTED_EDGE ( 'NONE', *, *, #90736, .T. ) ;
#76292=DIRECTION ( 'NONE',  ( -1.000000000000000000, -0.000000000000000000, -0.000000000000000000 ) ) ;
#76314=CARTESIAN_POINT ( 'NONE',  ( 31.84999999999999787, 3.309500000000003439, 0.000000000000000000 ) ) ;
#76402=ORIENTED_EDGE ( 'NONE', *, *, #81398, .T. ) ;
#76431=ADVANCED_FACE ( 'NONE', ( #89863 ), #40771, .T. ) ;
#76433=CARTESIAN_POINT ( 'NONE',  ( 26.08349330513380693, 1.593028355512270962E-15, 0.000000000000000000 ) ) ;
#76447=ORIENTED_EDGE ( 'NONE', *, *, #84430, .T. ) ;
#76481=CARTESIAN_POINT ( 'NONE',  ( 20.11650669486618881, 0.000000000000000000, 4.000000000000000888 ) ) ;
#76485=LINE ( 'NONE', #83515, #45967 ) ;
#76546=CARTESIAN_POINT ( 'NONE',  ( 6.162888688655344893, 3.752776749732562589, -6.500000000000000888 ) ) ;
#76562=EDGE_CURVE ( 'NONE', #8034, #63533, #6726, .T. ) ;
#76584=PRODUCT_DEFINITION ( 'UNKNOWN', '', #43929, #15473 ) ;
#76589=DIRECTION ( 'NONE',  ( 0.000000000000000000, -1.000000000000000000, 0.000000000000000000 ) ) ;
#76629=CARTESIAN_POINT ( 'NONE',  ( 6.936184427528457874, 0.000000000000000000, 0.000000000000000000 ) ) ;
#76655=CARTESIAN_POINT ( 'NONE',  ( 18.09999999999999787, 3.309500000000003439, 0.000000000000000000 ) ) ;
#76674=AXIS2_PLACEMENT_3D ( 'NONE', #93340, #20026, #18954 ) ;
#76714=FACE_OUTER_BOUND ( 'NONE', #82738, .T. ) ;
#76740=ORIENTED_EDGE ( 'NONE', *, *, #36645, .F. ) ;
#76843=ORIENTED_EDGE ( 'NONE', *, *, #67120, .T. ) ;
#76886=ORIENTED_EDGE ( 'NONE', *, *, #76562, .T. ) ;
#76938=ORIENTED_EDGE ( 'NONE', *, *, #73666, .F. ) ;
#77012=ORIENTED_EDGE ( 'NONE', *, *, #40929, .T. ) ;
#77031=ORIENTED_EDGE ( 'NONE', *, *, #18904, .F. ) ;
#77034=LINE ( 'NONE', #67363, #106299 ) ;
#77037=EDGE_CURVE ( 'NONE', #37114, #42466, #98171, .T. ) ;
#77116=EDGE_CURVE ( 'NONE', #59152, #43534, #79097, .T. ) ;
#77128=CARTESIAN_POINT ( 'NONE',  ( 16.36650669486618881, -3.999999999999998224, 0.000000000000000000 ) ) ;
#77164=VERTEX_POINT ( 'NONE', #11269 ) ;
#77177=DIRECTION ( 'NONE',  ( 0.000000000000000000, -1.000000000000000000, 0.000000000000000000 ) ) ;
#77209=CARTESIAN_POINT ( 'NONE',  ( 10.11650669486618881, 1.474610560812782335E-15, 0.000000000000000000 ) ) ;
#77217=ADVANCED_FACE ( 'NONE', ( #59322 ), #51524, .T. ) ;
#77267=CARTESIAN_POINT ( 'NONE',  ( 25.11650669486618881, 4.898587196589413815E-16, -4.000000000000000888 ) ) ;
#77298=ORIENTED_EDGE ( 'NONE', *, *, #43117, .T. ) ;
#77329=EDGE_CURVE ( 'NONE', #32616, #20548, #82104, .T. ) ;
#77334=EDGE_CURVE ( 'NONE', #48529, #82621, #66613, .T. ) ;
#77363=SURFACE_SIDE_STYLE ('',( #94632 ) ) ;
#77371=DIRECTION ( 'NONE',  ( 0.000000000000000000, -1.000000000000000000, 0.000000000000000000 ) ) ;
#77406=CARTESIAN_POINT ( 'NONE',  ( 18.09999999999999787, 1.533819458162526451E-15, 0.000000000000000000 ) ) ;
#77423=CARTESIAN_POINT ( 'NONE',  ( 6.289692432696790014, -0.6629690750393451015, -6.828989928337169779 ) ) ;
#77427=ORIENTED_EDGE ( 'NONE', *, *, #8679, .T. ) ;
#77436=EDGE_CURVE ( 'NONE', #83791, #46974, #8491, .T. ) ;
#77461=ORIENTED_EDGE ( 'NONE', *, *, #80919, .F. ) ;
#77474=DIRECTION ( 'NONE',  ( 0.5735764363510491570, -0.8191520442889895781, 1.003171929053522035E-16 ) ) ;
#77483=CARTESIAN_POINT ( 'NONE',  ( 11.84999999999999787, -3.309499999999999886, 4.475777889183790779E-16 ) ) ;
#77487=DIRECTION ( 'NONE',  ( -1.000000000000000000, -1.224606353822377258E-16, -0.000000000000000000 ) ) ;
#77496=ORIENTED_EDGE ( 'NONE', *, *, #102807, .F. ) ;
#77535=ORIENTED_EDGE ( 'NONE', *, *, #80711, .T. ) ;
#77554=CIRCLE ( 'NONE', #31097, 4.000000000000000888 ) ;
#77555=CARTESIAN_POINT ( 'NONE',  ( 32.61650669486618881, 1.474610560812782335E-15, 0.000000000000000000 ) ) ;
#77558=ADVANCED_FACE ( 'NONE', ( #49890 ), #41272, .T. ) ;
#77572=AXIS2_PLACEMENT_3D ( 'NONE', #200, #40691, #89789 ) ;
#77629=VERTEX_POINT ( 'NONE', #94081 ) ;
#77641=CIRCLE ( 'NONE', #48363, 4.000000000000000888 ) ;
#77647=CIRCLE ( 'NONE', #44936, 4.000000000000000888 ) ;
#77652=CARTESIAN_POINT ( 'NONE',  ( 5.819846122303830249, 6.321060697774945503, -2.051601713727019494 ) ) ;
#77671=AXIS2_PLACEMENT_3D ( 'NONE', #32121, #71494, #31087 ) ;
#77676=DIRECTION ( 'NONE',  ( -1.000000000000000000, -1.224606353822377258E-16, -0.000000000000000000 ) ) ;
#77745=CONICAL_SURFACE ( 'NONE', #50164, 4.000000000000001776, 0.9599310885968774798 ) ;
#77750=CARTESIAN_POINT ( 'NONE',  ( 6.162888688655347558, -7.505553499465142053, -3.129864801432410934E-16 ) ) ;
#77764=CARTESIAN_POINT ( 'NONE',  ( 0.000000000000000000, 0.000000000000000000, 0.000000000000000000 ) ) ;
#77800=CARTESIAN_POINT ( 'NONE',  ( 6.289692432696789126, 0.6629690750393447685, 6.828989928337166226 ) ) ;
#77814=AXIS2_PLACEMENT_3D ( 'NONE', #80084, #64457, #7254 ) ;
#77853=CARTESIAN_POINT ( 'NONE',  ( 19.83349330513380693, 1.593028355512270962E-15, 0.000000000000000000 ) ) ;
#77867=EDGE_CURVE ( 'NONE', #65549, #90138, #34485, .T. ) ;
#77921=ORIENTED_EDGE ( 'NONE', *, *, #13306, .F. ) ;
#77950=VERTEX_POINT ( 'NONE', #82125 ) ;
#78006=VERTEX_POINT ( 'NONE', #90232 ) ;
#78060=EDGE_LOOP ( 'NONE', ( #59251, #48411, #44033, #103366, #54921 ) ) ;
#78077=CIRCLE ( 'NONE', #23051, 4.000000000000000888 ) ;
#78092=CARTESIAN_POINT ( 'NONE',  ( 28.58349330513380337, -4.000000000000000000, 4.898587196589415787E-16 ) ) ;
#78098=CARTESIAN_POINT ( 'NONE',  ( 13.09999999999999787, 1.533819458162526451E-15, 0.000000000000000000 ) ) ;
#78113=ORIENTED_EDGE ( 'NONE', *, *, #25422, .F. ) ;
#78137=ORIENTED_EDGE ( 'NONE', *, *, #58456, .T. ) ;
#78153=CARTESIAN_POINT ( 'NONE',  ( 6.683837171061803417, -3.955946848495962787, 6.851900933636989599 ) ) ;
#78158=EDGE_CURVE ( 'NONE', #47612, #66358, #56906, .T. ) ;
#78177=CONICAL_SURFACE ( 'NONE', #36882, 4.000000000000001776, 0.9599310885968774798 ) ;
#78191=VERTEX_POINT ( 'NONE', #36819 ) ;
#78219=VERTEX_POINT ( 'NONE', #52415 ) ;
#78226=EDGE_LOOP ( 'NONE', ( #90580, #88870, #24377, #20147, #57085 ) ) ;
#78242=ORIENTED_EDGE ( 'NONE', *, *, #8628, .T. ) ;
#78260=ORIENTED_EDGE ( 'NONE', *, *, #49800, .T. ) ;
#78325=CARTESIAN_POINT ( 'NONE',  ( 28.09999999999999787, -3.309499999999999886, 4.475777889183790779E-16 ) ) ;
#78348=DIRECTION ( 'NONE',  ( -1.000000000000000000, -0.000000000000000000, -0.000000000000000000 ) ) ;
#78385=CARTESIAN_POINT ( 'NONE',  ( 21.08349330513380693, -3.851859888774471706E-31, 4.000000000000001776 ) ) ;
#78401=EDGE_CURVE ( 'NONE', #45187, #96540, #5203, .T. ) ;
#78412=AXIS2_PLACEMENT_3D ( 'NONE', #4013, #20249, #37482 ) ;
#78434=AXIS2_PLACEMENT_3D ( 'NONE', #6614, #39540, #17390 ) ;
#78436=ORIENTED_EDGE ( 'NONE', *, *, #68784, .F. ) ;
#78437=LINE ( 'NONE', #38026, #1386 ) ;
#78447=CIRCLE ( 'NONE', #49178, 3.309500000000001663 ) ;
#78448=CONICAL_SURFACE ( 'NONE', #100846, 4.000000000000001776, 0.9599310885968774798 ) ;
#78502=CARTESIAN_POINT ( 'NONE',  ( -3.184843881676170261E-16, -5.788408252967908396, -2.974182810908594821 ) ) ;
#78510=CARTESIAN_POINT ( 'NONE',  ( 10.11650669486618881, 0.000000000000000000, 4.000000000000000888 ) ) ;
#78532=EDGE_CURVE ( 'NONE', #44978, #51593, #79752, .T. ) ;
#78548=AXIS2_PLACEMENT_3D ( 'NONE', #9955, #93007, #26720 ) ;
#78564=EDGE_CURVE ( 'NONE', #46974, #11179, #6939, .T. ) ;
#78610=EDGE_CURVE ( 'NONE', #37114, #91829, #67259, .T. ) ;
#78617=EDGE_LOOP ( 'NONE', ( #10589, #5186, #59007, #27602, #105075 ) ) ;
#78651=ORIENTED_EDGE ( 'NONE', *, *, #70412, .F. ) ;
#78658=AXIS2_PLACEMENT_3D ( 'NONE', #73536, #88684, #39087 ) ;
#78672=CARTESIAN_POINT ( 'NONE',  ( 29.34999999999999787, -3.309499999999999886, 4.475777889183790779E-16 ) ) ;
#78689=AXIS2_PLACEMENT_3D ( 'NONE', #93491, #19638, #68137 ) ;
#78695=EDGE_CURVE ( 'NONE', #64476, #90846, #70475, .T. ) ;
#78704=CARTESIAN_POINT ( 'NONE',  ( 0.000000000000000000, 0.000000000000000000, 0.000000000000000000 ) ) ;
#78714=ORIENTED_EDGE ( 'NONE', *, *, #46707, .F. ) ;
#78738=CIRCLE ( 'NONE', #33984, 3.309500000000001663 ) ;
#78750=DIRECTION ( 'NONE',  ( -1.000000000000000000, -1.224606353822377258E-16, -0.000000000000000000 ) ) ;
#78787=DIRECTION ( 'NONE',  ( 0.000000000000000000, 0.000000000000000000, 1.000000000000000000 ) ) ;
#78825=VERTEX_POINT ( 'NONE', #15009 ) ;
#78832=CARTESIAN_POINT ( 'NONE',  ( 22.33349330513380693, -4.000000000000000888, 4.898587196589416773E-16 ) ) ;
#78837=EDGE_LOOP ( 'NONE', ( #98116, #80794, #53972, #26139, #70690 ) ) ;
#78857=AXIS2_PLACEMENT_3D ( 'NONE', #96762, #88662, #31517 ) ;
#78878=ORIENTED_EDGE ( 'NONE', *, *, #40929, .F. ) ;
#78887=CARTESIAN_POINT ( 'NONE',  ( 31.84999999999999787, 1.533819458162526451E-15, 0.000000000000000000 ) ) ;
#78892=VERTEX_POINT ( 'NONE', #2013 ) ;
#78893=CARTESIAN_POINT ( 'NONE',  ( 21.36650669486618881, -3.999999999999998224, 0.000000000000000000 ) ) ;
#78962=LINE ( 'NONE', #70878, #30260 ) ;
#78967=EDGE_CURVE ( 'NONE', #88573, #102768, #8719, .T. ) ;
#78975=EDGE_CURVE ( 'NONE', #11885, #3128, #1856, .T. ) ;
#78998=CARTESIAN_POINT ( 'NONE',  ( 31.36650669486618881, 4.898587196589413815E-16, -4.000000000000000888 ) ) ;
#79008=DIRECTION ( 'NONE',  ( 0.000000000000000000, -1.000000000000000000, 0.000000000000000000 ) ) ;
#79021=ORIENTED_EDGE ( 'NONE', *, *, #72024, .F. ) ;
#79071=AXIS2_PLACEMENT_3D ( 'NONE', #103508, #86291, #21049 ) ;
#79097=CIRCLE ( 'NONE', #68804, 4.000000000000000888 ) ;
#79121=EDGE_CURVE ( 'NONE', #94380, #39211, #32702, .T. ) ;
#79132=ORIENTED_EDGE ( 'NONE', *, *, #41150, .F. ) ;
#79137=DIRECTION ( 'NONE',  ( 0.000000000000000000, -1.000000000000000000, 0.000000000000000000 ) ) ;
#79214=VERTEX_POINT ( 'NONE', #78832 ) ;
#79224=CARTESIAN_POINT ( 'NONE',  ( 27.33349330513380693, 1.593028355512270962E-15, 0.000000000000000000 ) ) ;
#79232=CARTESIAN_POINT ( 'NONE',  ( 27.61650669486618881, 0.000000000000000000, 4.000000000000000888 ) ) ;
#79245=ORIENTED_EDGE ( 'NONE', *, *, #86010, .F. ) ;
#79270=DIRECTION ( 'NONE',  ( -1.000000000000000000, -0.000000000000000000, -0.000000000000000000 ) ) ;
#79298=AXIS2_PLACEMENT_3D ( 'NONE', #33551, #50752, #65897 ) ;
#79368=CARTESIAN_POINT ( 'NONE',  ( 29.83349330513380693, 1.593028355512270962E-15, 0.000000000000000000 ) ) ;
#79405=EDGE_CURVE ( 'NONE', #30305, #87682, #67327, .T. ) ;
#79412=CARTESIAN_POINT ( 'NONE',  ( 35.11650669486618170, 1.474610560812782335E-15, 0.000000000000000000 ) ) ;
#79419=FACE_OUTER_BOUND ( 'NONE', #40435, .T. ) ;
#79438=CARTESIAN_POINT ( 'NONE',  ( 12.33349330513380693, -4.000000000000000000, 4.898587196589415787E-16 ) ) ;
#79459=EDGE_CURVE ( 'NONE', #7599, #14445, #25966, .T. ) ;
#79462=EDGE_LOOP ( 'NONE', ( #71266, #76886, #22207, #15600, #78878, #35269 ) ) ;
#79466=VECTOR ( 'NONE', #105766, 1000.000000000000000 ) ;
#79508=CIRCLE ( 'NONE', #81187, 4.000000000000000888 ) ;
#79529=DIRECTION ( 'NONE',  ( -0.5735764363510494901, -0.8191520442889894671, 0.000000000000000000 ) ) ;
#79539=ORIENTED_EDGE ( 'NONE', *, *, #8243, .T. ) ;
#79563=ORIENTED_EDGE ( 'NONE', *, *, #84386, .T. ) ;
#79582=FACE_OUTER_BOUND ( 'NONE', #17703, .T. ) ;
#79614=CIRCLE ( 'NONE', #70998, 4.000000000000001776 ) ;
#79675=FACE_OUTER_BOUND ( 'NONE', #24402, .T. ) ;
#79678=CARTESIAN_POINT ( 'NONE',  ( 24.83349330513380693, 1.593028355512270962E-15, 0.000000000000000000 ) ) ;
#79703=ORIENTED_EDGE ( 'NONE', *, *, #72024, .T. ) ;
#79752=LINE ( 'NONE', #13946, #93036 ) ;
#79760=CIRCLE ( 'NONE', #40197, 4.000000000000000888 ) ;
#79786=EDGE_LOOP ( 'NONE', ( #94982, #48796, #26423, #80964, #78714 ) ) ;
#79787=DIRECTION ( 'NONE',  ( 0.000000000000000000, -1.000000000000000000, 0.000000000000000000 ) ) ;
#79874=CONICAL_SURFACE ( 'NONE', #102299, 4.000000000000001776, 0.9599310885968774798 ) ;
#79878=DIRECTION ( 'NONE',  ( 0.000000000000000000, -1.000000000000000000, 0.000000000000000000 ) ) ;
#79916=ADVANCED_FACE ( 'NONE', ( #25841 ), #53611, .T. ) ;
#79927=VERTEX_POINT ( 'NONE', #98074 ) ;
#79932=DIRECTION ( 'NONE',  ( -1.000000000000000000, -1.224606353822377258E-16, -0.000000000000000000 ) ) ;
#79939=CYLINDRICAL_SURFACE ( 'NONE', #11961, 4.000000000000000888 ) ;
#79964=CARTESIAN_POINT ( 'NONE',  ( 10.11650669486618881, 4.000000000000003553, 4.898587196589414801E-16 ) ) ;
#79984=AXIS2_PLACEMENT_3D ( 'NONE', #28, #66393, #32998 ) ;
#80023=CARTESIAN_POINT ( 'NONE',  ( 19.34999999999999787, -3.309499999999999886, 0.000000000000000000 ) ) ;
#80066=CARTESIAN_POINT ( 'NONE',  ( 20.59999999999999787, 1.533819458162526451E-15, 0.000000000000000000 ) ) ;
#80070=CARTESIAN_POINT ( 'NONE',  ( 11.08349330513380515, 1.593028355512270962E-15, 0.000000000000000000 ) ) ;
#80073=FACE_OUTER_BOUND ( 'NONE', #84091, .T. ) ;
#80084=CARTESIAN_POINT ( 'NONE',  ( 16.84999999999999787, 1.533819458162526451E-15, 0.000000000000000000 ) ) ;
#80086=DIRECTION ( 'NONE',  ( 0.000000000000000000, 1.000000000000000000, 0.000000000000000000 ) ) ;
#80112=CARTESIAN_POINT ( 'NONE',  ( 0.05613245601036612881, 1.278525034529252924, -6.499999999999999112 ) ) ;
#80113=ORIENTED_EDGE ( 'NONE', *, *, #45887, .F. ) ;
#80122=ORIENTED_EDGE ( 'NONE', *, *, #17425, .F. ) ;
#80126=ADVANCED_FACE ( 'NONE', ( #49385 ), #41308, .T. ) ;
#80168=ORIENTED_EDGE ( 'NONE', *, *, #13698, .T. ) ;
#80196=CARTESIAN_POINT ( 'NONE',  ( 5.980073869852059687, 2.767359234582687844, -6.500000000000000888 ) ) ;
#80208=FACE_OUTER_BOUND ( 'NONE', #52927, .T. ) ;
#80223=VERTEX_POINT ( 'NONE', #15435 ) ;
#80241=ORIENTED_EDGE ( 'NONE', *, *, #75151, .T. ) ;
#80257=CARTESIAN_POINT ( 'NONE',  ( 6.643884894376899553, -7.802125718944354027, -9.232358214956412824E-13 ) ) ;
#80267=CONICAL_SURFACE ( 'NONE', #64805, 3.309500000000001663, 0.9599310885968770357 ) ;
#80271=DIRECTION ( 'NONE',  ( -1.000000000000000000, -1.224606353822377258E-16, -0.000000000000000000 ) ) ;
#80294=CARTESIAN_POINT ( 'NONE',  ( 0.2578475836320693881, 4.367703157927328661, -5.434916218090833695 ) ) ;
#80295=DIRECTION ( 'NONE',  ( 0.000000000000000000, 0.000000000000000000, -1.000000000000000000 ) ) ;
#80303=ORIENTED_EDGE ( 'NONE', *, *, #28525, .F. ) ;
#80347=CONICAL_SURFACE ( 'NONE', #101079, 6.500000000000000000, 1.047197551196600296 ) ;
#80371=CARTESIAN_POINT ( 'NONE',  ( 26.08349330513380693, -3.851859888774471706E-31, 4.000000000000001776 ) ) ;
#80378=DIRECTION ( 'NONE',  ( 0.000000000000000000, -1.000000000000000000, 0.000000000000000000 ) ) ;
#80383=ADVANCED_FACE ( 'NONE', ( #42435 ), #8866, .T. ) ;
#80386=ORIENTED_EDGE ( 'NONE', *, *, #67181, .F. ) ;
#80406=VECTOR ( 'NONE', #88756, 1000.000000000000114 ) ;
#80416=CARTESIAN_POINT ( 'NONE',  ( 31.08349330513380693, 4.898587196589411843E-16, -4.000000000000001776 ) ) ;
#80418=AXIS2_PLACEMENT_3D ( 'NONE', #71549, #54288, #31142 ) ;
#80419=CIRCLE ( 'NONE', #78658, 4.000000000000001776 ) ;
#80456=EDGE_CURVE ( 'NONE', #30441, #79214, #41589, .T. ) ;
#80460=ORIENTED_EDGE ( 'NONE', *, *, #24838, .F. ) ;
#80478=CARTESIAN_POINT ( 'NONE',  ( 6.585468679846625761, -7.640532685286896886, -0.2337908078075601470 ) ) ;
#80493=CARTESIAN_POINT ( 'NONE',  ( 13.58349330513380515, 1.593028355512270962E-15, 0.000000000000000000 ) ) ;
#80495=EDGE_LOOP ( 'NONE', ( #91452, #90829, #81675, #48737, #61430 ) ) ;
#80526=CARTESIAN_POINT ( 'NONE',  ( 6.326445470157512574, -5.253846677262524523, -4.563138989068577622 ) ) ;
#80535=LINE ( 'NONE', #11281, #51996 ) ;
#80571=DIRECTION ( 'NONE',  ( 0.000000000000000000, 0.000000000000000000, 1.000000000000000000 ) ) ;
#80583=( NAMED_UNIT ( * ) PLANE_ANGLE_UNIT ( ) SI_UNIT ( $, .RADIAN. ) );
#80608=EDGE_LOOP ( 'NONE', ( #39558, #51279, #19919, #84917, #31004, #52401 ) ) ;
#80618=CONICAL_SURFACE ( 'NONE', #65227, 4.000000000000001776, 0.9599310885968774798 ) ;
#80641=EDGE_LOOP ( 'NONE', ( #82180, #16258, #71505 ) ) ;
#80645=DIRECTION ( 'NONE',  ( -1.000000000000000000, -1.224606353822377258E-16, -0.000000000000000000 ) ) ;
#80647=AXIS2_PLACEMENT_3D ( 'NONE', #29781, #103630, #69680 ) ;
#80650=EDGE_CURVE ( 'NONE', #98662, #48969, #30003, .T. ) ;
#80711=EDGE_CURVE ( 'NONE', #87062, #16434, #69911, .T. ) ;
#80721=EDGE_LOOP ( 'NONE', ( #8656, #11914, #65611, #44799, #30225 ) ) ;
#80750=EDGE_CURVE ( 'NONE', #8828, #88306, #100025, .T. ) ;
#80761=VECTOR ( 'NONE', #32824, 1000.000000000000000 ) ;
#80777=AXIS2_PLACEMENT_3D ( 'NONE', #17384, #82630, #59435 ) ;
#80794=ORIENTED_EDGE ( 'NONE', *, *, #80650, .T. ) ;
#80800=DIRECTION ( 'NONE',  ( -1.000000000000000000, -1.224606353822377258E-16, -0.000000000000000000 ) ) ;
#80801=DIRECTION ( 'NONE',  ( 0.000000000000000000, 1.000000000000000000, 0.000000000000000000 ) ) ;
#80803=ADVANCED_FACE ( 'NONE', ( #41246 ), #72029, .T. ) ;
#80828=ORIENTED_EDGE ( 'NONE', *, *, #74349, .T. ) ;
#80845=DIRECTION ( 'NONE',  ( 0.5735764363510490460, 0.8191520442889896891, 0.000000000000000000 ) ) ;
#80846=EDGE_CURVE ( 'NONE', #52343, #88800, #75191, .T. ) ;
#80881=ORIENTED_EDGE ( 'NONE', *, *, #78532, .T. ) ;
#80908=AXIS2_PLACEMENT_3D ( 'NONE', #73288, #32347, #42001 ) ;
#80909=CARTESIAN_POINT ( 'NONE',  ( 23.86650669486618881, 0.000000000000000000, 4.000000000000000888 ) ) ;
#80910=EDGE_LOOP ( 'NONE', ( #7471, #49346, #51572, #22104, #20541 ) ) ;
#80919=EDGE_CURVE ( 'NONE', #101499, #97355, #60406, .T. ) ;
#80922=VERTEX_POINT ( 'NONE', #91926 ) ;
#80964=ORIENTED_EDGE ( 'NONE', *, *, #19163, .F. ) ;
#81010=CARTESIAN_POINT ( 'NONE',  ( 6.692588830498429786, -7.935834885954432316, -0.04058884017440450576 ) ) ;
#81022=VECTOR ( 'NONE', #66679, 1000.000000000000000 ) ;
#81028=EDGE_CURVE ( 'NONE', #58745, #71083, #34547, .T. ) ;
#81063=EDGE_CURVE ( 'NONE', #91446, #27343, #27701, .T. ) ;
#81064=DIRECTION ( 'NONE',  ( -1.000000000000000000, -1.224606353822377258E-16, -0.000000000000000000 ) ) ;
#81114=DIRECTION ( 'NONE',  ( 0.000000000000000000, -1.000000000000000000, 0.000000000000000000 ) ) ;
#81137=CARTESIAN_POINT ( 'NONE',  ( 0.2595206531158508190, 2.531175536751804067, 6.499999999999995559 ) ) ;
#81141=ORIENTED_EDGE ( 'NONE', *, *, #19941, .F. ) ;
#81142=VERTEX_POINT ( 'NONE', #40062 ) ;
#81143=DIRECTION ( 'NONE',  ( -1.000000000000000000, -1.224606353822377258E-16, -0.000000000000000000 ) ) ;
#81147=DIRECTION ( 'NONE',  ( 0.5735764363510491570, -0.8191520442889895781, 1.003171929053522035E-16 ) ) ;
#81149=ORIENTED_EDGE ( 'NONE', *, *, #93544, .T. ) ;
#81168=CARTESIAN_POINT ( 'NONE',  ( 7.724940478959218106E-16, 0.6351314446025488891, -6.500000000000000888 ) ) ;
#81171=EDGE_CURVE ( 'NONE', #16558, #59167, #43215, .T. ) ;
#81183=ORIENTED_EDGE ( 'NONE', *, *, #46512, .T. ) ;
#81187=AXIS2_PLACEMENT_3D ( 'NONE', #17701, #922, #82954 ) ;
#81191=DIRECTION ( 'NONE',  ( 0.000000000000000000, -1.000000000000000000, 0.000000000000000000 ) ) ;
#81195=ORIENTED_EDGE ( 'NONE', *, *, #47799, .F. ) ;
#81196=CARTESIAN_POINT ( 'NONE',  ( 38.09999999999998721, 0.000000000000000000, 3.309499999999999886 ) ) ;
#81217=AXIS2_PLACEMENT_3D ( 'NONE', #98564, #16595, #49486 ) ;
#81251=CARTESIAN_POINT ( 'NONE',  ( 6.692649149972420553, -4.003391779698787900, -6.852343209863739126 ) ) ;
#81262=CIRCLE ( 'NONE', #70973, 4.000000000000001776 ) ;
#81278=ORIENTED_EDGE ( 'NONE', *, *, #49212, .T. ) ;
#81285=EDGE_LOOP ( 'NONE', ( #62359, #44571, #34376, #79132, #45919 ) ) ;
#81311=VECTOR ( 'NONE', #66631, 1000.000000000000000 ) ;
#81317=EDGE_CURVE ( 'NONE', #90625, #16689, #84562, .T. ) ;
#81391=DIRECTION ( 'NONE',  ( 0.000000000000000000, -1.000000000000000000, 0.000000000000000000 ) ) ;
#81395=AXIS2_PLACEMENT_3D ( 'NONE', #35894, #1867, #17557 ) ;
#81398=EDGE_CURVE ( 'NONE', #20548, #51009, #34105, .T. ) ;
#81408=EDGE_CURVE ( 'NONE', #14483, #48969, #15635, .T. ) ;
#81431=DIRECTION ( 'NONE',  ( -1.000000000000000000, -1.224606353822377258E-16, -0.000000000000000000 ) ) ;
#81492=EDGE_CURVE ( 'NONE', #12821, #44704, #91495, .T. ) ;
#81530=CARTESIAN_POINT ( 'NONE',  ( 6.585531397294616340, 4.023063057964797018, 6.499999999999997335 ) ) ;
#81559=LINE ( 'NONE', #7687, #29944 ) ;
#81588=ORIENTED_EDGE ( 'NONE', *, *, #3641, .F. ) ;
#81591=CARTESIAN_POINT ( 'NONE',  ( 18.58349330513380693, 1.593028355512270962E-15, 0.000000000000000000 ) ) ;
#81598=CARTESIAN_POINT ( 'NONE',  ( 0.000000000000000000, 4.898587196589413815E-16, -4.000000000000000888 ) ) ;
#81620=DIRECTION ( 'NONE',  ( 1.000000000000000000, 0.000000000000000000, -0.000000000000000000 ) ) ;
#81650=ORIENTED_EDGE ( 'NONE', *, *, #44240, .F. ) ;
#81675=ORIENTED_EDGE ( 'NONE', *, *, #39193, .F. ) ;
#81690=DIRECTION ( 'NONE',  ( -1.000000000000000000, -1.224606353822377258E-16, -0.000000000000000000 ) ) ;
#81701=CIRCLE ( 'NONE', #59336, 4.000000000000000888 ) ;
#81714=CARTESIAN_POINT ( 'NONE',  ( 13.86650669486618881, 1.474610560812782335E-15, 0.000000000000000000 ) ) ;
#81715=EDGE_LOOP ( 'NONE', ( #27366, #85946, #103338, #338, #5020, #35986 ) ) ;
#81718=DIRECTION ( 'NONE',  ( 0.000000000000000000, -1.000000000000000000, 0.000000000000000000 ) ) ;
#81756=VERTEX_POINT ( 'NONE', #93270 ) ;
#81767=DIRECTION ( 'NONE',  ( 0.000000000000000000, 1.000000000000000000, 0.000000000000000000 ) ) ;
#81794=VERTEX_POINT ( 'NONE', #20506 ) ;
#81803=AXIS2_PLACEMENT_3D ( 'NONE', #22176, #87957, #22712 ) ;
#81814=CARTESIAN_POINT ( 'NONE',  ( 12.61650669486618881, 1.474610560812782335E-15, 0.000000000000000000 ) ) ;
#81838=EDGE_CURVE ( 'NONE', #78825, #51255, #69009, .T. ) ;
#81868=CARTESIAN_POINT ( 'NONE',  ( 17.33349330513380693, 1.593028355512270962E-15, 0.000000000000000000 ) ) ;
#81881=EDGE_CURVE ( 'NONE', #96201, #3065, #8859, .T. ) ;
#81895=VERTEX_POINT ( 'NONE', #102424 ) ;
#81897=VERTEX_POINT ( 'NONE', #28565 ) ;
#81903=ORIENTED_EDGE ( 'NONE', *, *, #3641, .T. ) ;
#81939=ORIENTED_EDGE ( 'NONE', *, *, #54014, .T. ) ;
#81981=AXIS2_PLACEMENT_3D ( 'NONE', #34573, #25412, #26482 ) ;
#82016=DIRECTION ( 'NONE',  ( 0.000000000000000000, -1.000000000000000000, 0.000000000000000000 ) ) ;
#82072=CONICAL_SURFACE ( 'NONE', #56182, 3.309499999999999886, 0.7853981633974369547 ) ;
#82082=CARTESIAN_POINT ( 'NONE',  ( 6.222803527742078344, 4.089662073612393201, 6.499999999999997335 ) ) ;
#82104=B_SPLINE_CURVE_WITH_KNOTS ( 'NONE', 3,
 ( #30155, #80257, #29641, #13930, #90357, #65553 ),
 .UNSPECIFIED., .F., .F.,
 ( 4, 2, 4 ),
 ( -4.698498716301610638E-06, 0.0003457374136928005972, 0.0006961733261019028771 ),
 .UNSPECIFIED. ) ;
#82125=CARTESIAN_POINT ( 'NONE',  ( 8.099999999999999645, 4.898587196589413815E-16, -4.000000000000000888 ) ) ;
#82180=ORIENTED_EDGE ( 'NONE', *, *, #8428, .T. ) ;
#82185=CARTESIAN_POINT ( 'NONE',  ( 0.000000000000000000, 0.000000000000000000, 0.000000000000000000 ) ) ;
#82251=ORIENTED_EDGE ( 'NONE', *, *, #88667, .T. ) ;
#82261=CARTESIAN_POINT ( 'NONE',  ( 23.09999999999999432, 1.533819458162526451E-15, 0.000000000000000000 ) ) ;
#82293=DIRECTION ( 'NONE',  ( 0.000000000000000000, 0.000000000000000000, 1.000000000000000000 ) ) ;
#82303=DIRECTION ( 'NONE',  ( -1.000000000000000000, -0.000000000000000000, -0.000000000000000000 ) ) ;
#82322=VERTEX_POINT ( 'NONE', #61327 ) ;
#82358=CARTESIAN_POINT ( 'NONE',  ( 22.33349330513380693, -3.851859888774471706E-31, 4.000000000000001776 ) ) ;
#82377=CARTESIAN_POINT ( 'NONE',  ( 0.000000000000000000, 0.000000000000000000, 0.000000000000000000 ) ) ;
#82379=DIRECTION ( 'NONE',  ( -1.000000000000000000, -1.224606353822377258E-16, -0.000000000000000000 ) ) ;
#82399=CARTESIAN_POINT ( 'NONE',  ( 21.36650669486618881, 4.898587196589413815E-16, -4.000000000000000888 ) ) ;
#82408=EDGE_CURVE ( 'NONE', #64296, #67545, #33075, .T. ) ;
#82411=DIRECTION ( 'NONE',  ( 1.000000000000000000, 0.000000000000000000, -0.000000000000000000 ) ) ;
#82423=FACE_OUTER_BOUND ( 'NONE', #50623, .T. ) ;
#82460=CONICAL_SURFACE ( 'NONE', #101408, 4.000000000000001776, 0.9599310885968774798 ) ;
#82489=ORIENTED_EDGE ( 'NONE', *, *, #29019, .T. ) ;
#82517=CYLINDRICAL_SURFACE ( 'NONE', #50595, 4.000000000000000888 ) ;
#82525=ORIENTED_EDGE ( 'NONE', *, *, #100937, .F. ) ;
#82536=AXIS2_PLACEMENT_3D ( 'NONE', #76433, #66767, #59214 ) ;
#82538=FACE_OUTER_BOUND ( 'NONE', #19782, .T. ) ;
#82546=EDGE_CURVE ( 'NONE', #46570, #20548, #99564, .T. ) ;
#82575=VERTEX_POINT ( 'NONE', #2252 ) ;
#82583=DIRECTION ( 'NONE',  ( -1.000000000000000000, -0.000000000000000000, -0.000000000000000000 ) ) ;
#82590=ORIENTED_EDGE ( 'NONE', *, *, #24204, .F. ) ;
#82621=VERTEX_POINT ( 'NONE', #19038 ) ;
#82625=ORIENTED_EDGE ( 'NONE', *, *, #21083, .F. ) ;
#82630=DIRECTION ( 'NONE',  ( 1.000000000000000000, 1.224606353822377258E-16, 0.000000000000000000 ) ) ;
#82693=CARTESIAN_POINT ( 'NONE',  ( 33.86650669486618881, 4.898587196589413815E-16, -4.000000000000000888 ) ) ;
#82700=ADVANCED_FACE ( 'NONE', ( #13538 ), #88178, .T. ) ;
#82702=AXIS2_PLACEMENT_3D ( 'NONE', #93120, #27372, #2503 ) ;
#82727=CYLINDRICAL_SURFACE ( 'NONE', #64927, 4.000000000000000888 ) ;
#82735=EDGE_CURVE ( 'NONE', #48529, #63779, #60638, .T. ) ;
#82738=EDGE_LOOP ( 'NONE', ( #61924, #86800, #83772, #75121, #69585 ) ) ;
#82795=LINE ( 'NONE', #75762, #24766 ) ;
#82814=CARTESIAN_POINT ( 'NONE',  ( 23.86650669486618881, 4.000000000000003553, 4.898587196589414801E-16 ) ) ;
#82879=DIRECTION ( 'NONE',  ( 0.000000000000000000, -1.000000000000000000, 0.000000000000000000 ) ) ;
#82883=ORIENTED_EDGE ( 'NONE', *, *, #21083, .T. ) ;
#82885=CARTESIAN_POINT ( 'NONE',  ( 0.05458999538772667942, -1.264741368073333483, 6.499999999999999112 ) ) ;
#82954=DIRECTION ( 'NONE',  ( 0.000000000000000000, -1.000000000000000000, 0.000000000000000000 ) ) ;
#82997=FACE_OUTER_BOUND ( 'NONE', #94616, .T. ) ;
#83001=VERTEX_POINT ( 'NONE', #501 ) ;
#83011=CARTESIAN_POINT ( 'NONE',  ( 31.08349330513380693, -4.000000000000000000, 4.898587196589415787E-16 ) ) ;
#83019=EDGE_CURVE ( 'NONE', #52034, #30747, #79614, .T. ) ;
#83081=EDGE_CURVE ( 'NONE', #8054, #55679, #62467, .T. ) ;
#83105=DIRECTION ( 'NONE',  ( 0.000000000000000000, -1.000000000000000000, 0.000000000000000000 ) ) ;
#83113=DIRECTION ( 'NONE',  ( 0.000000000000000000, -1.000000000000000000, 0.000000000000000000 ) ) ;
#83166=CIRCLE ( 'NONE', #14317, 4.000000000000000888 ) ;
#83170=ORIENTED_EDGE ( 'NONE', *, *, #29325, .T. ) ;
#83182=CARTESIAN_POINT ( 'NONE',  ( 36.36650669486618881, 1.474610560812782335E-15, 0.000000000000000000 ) ) ;
#83202=DIRECTION ( 'NONE',  ( 1.000000000000000000, 0.000000000000000000, 0.000000000000000000 ) ) ;
#83206=VERTEX_POINT ( 'NONE', #71641 ) ;
#83238=DIRECTION ( 'NONE',  ( 1.000000000000000000, 1.224606353822377258E-16, 0.000000000000000000 ) ) ;
#83327=FACE_OUTER_BOUND ( 'NONE', #106469, .T. ) ;
#83341=PLANE ( 'NONE',  #18621 ) ;
#83397=DIRECTION ( 'NONE',  ( 0.000000000000000000, 0.000000000000000000, 1.000000000000000000 ) ) ;
#83424=EDGE_LOOP ( 'NONE', ( #79021, #23176, #51934, #55996, #21734 ) ) ;
#83437=DIRECTION ( 'NONE',  ( 0.000000000000000000, -1.000000000000000000, 0.000000000000000000 ) ) ;
#83440=DIRECTION ( 'NONE',  ( 0.000000000000000000, -1.000000000000000000, 0.000000000000000000 ) ) ;
#83465=ADVANCED_FACE ( 'NONE', ( #91048 ), #43017, .T. ) ;
#83466=DIRECTION ( 'NONE',  ( 0.000000000000000000, -0.8660254037844380415, 0.5000000000000009992 ) ) ;
#83515=CARTESIAN_POINT ( 'NONE',  ( 0.000000000000000000, 4.898587196589413815E-16, -4.000000000000000888 ) ) ;
#83521=VERTEX_POINT ( 'NONE', #103378 ) ;
#83524=DIRECTION ( 'NONE',  ( -0.5735764363510494901, -0.8191520442889894671, 0.000000000000000000 ) ) ;
#83525=CARTESIAN_POINT ( 'NONE',  ( 0.000000000000000000, 0.000000000000000000, 4.000000000000000888 ) ) ;
#83587=EDGE_CURVE ( 'NONE', #11120, #92773, #28460, .T. ) ;
#83628=CARTESIAN_POINT ( 'NONE',  ( -3.605819256461556543E-15, 5.788408252967900403, 2.974182810908597929 ) ) ;
#83629=ORIENTED_EDGE ( 'NONE', *, *, #66345, .T. ) ;
#83684=DIRECTION ( 'NONE',  ( 0.000000000000000000, -1.000000000000000000, 0.000000000000000000 ) ) ;
#83709=CIRCLE ( 'NONE', #73373, 4.000000000000000888 ) ;
#83714=EDGE_CURVE ( 'NONE', #61003, #31318, #83166, .T. ) ;
#83715=CARTESIAN_POINT ( 'NONE',  ( 0.000000000000000000, 0.000000000000000000, 0.000000000000000000 ) ) ;
#83761=DIRECTION ( 'NONE',  ( -1.000000000000000000, -1.224606353822377258E-16, -0.000000000000000000 ) ) ;
#83772=ORIENTED_EDGE ( 'NONE', *, *, #83587, .T. ) ;
#83784=VECTOR ( 'NONE', #68431, 1000.000000000000000 ) ;
#83791=VERTEX_POINT ( 'NONE', #100578 ) ;
#83796=VERTEX_POINT ( 'NONE', #59613 ) ;
#83802=CARTESIAN_POINT ( 'NONE',  ( 0.4033376246892514394, -7.198601258566903915, 0.5316568767328679890 ) ) ;
#83821=ORIENTED_EDGE ( 'NONE', *, *, #74472, .T. ) ;
#83844=ORIENTED_EDGE ( 'NONE', *, *, #52739, .F. ) ;
#83855=DIRECTION ( 'NONE',  ( -1.000000000000000000, -0.000000000000000000, -0.000000000000000000 ) ) ;
#83858=DIRECTION ( 'NONE',  ( -1.000000000000000000, -1.224606353822377258E-16, -0.000000000000000000 ) ) ;
#83911=CARTESIAN_POINT ( 'NONE',  ( 6.463178677061754307, -2.643201791673487122, -6.839998497243183095 ) ) ;
#83918=ORIENTED_EDGE ( 'NONE', *, *, #25067, .F. ) ;
#83931=LINE ( 'NONE', #49965, #25 ) ;
#83945=ORIENTED_EDGE ( 'NONE', *, *, #40870, .T. ) ;
#84029=EDGE_LOOP ( 'NONE', ( #5629, #40189, #68775, #32236, #9756 ) ) ;
#84031=ORIENTED_EDGE ( 'NONE', *, *, #6203, .T. ) ;
#84037=ORIENTED_EDGE ( 'NONE', *, *, #96914, .T. ) ;
#84050=ORIENTED_EDGE ( 'NONE', *, *, #33471, .F. ) ;
#84060=CIRCLE ( 'NONE', #97829, 4.000000000000001776 ) ;
#84065=ORIENTED_EDGE ( 'NONE', *, *, #4409, .F. ) ;
#84091=EDGE_LOOP ( 'NONE', ( #11506, #5368, #86628, #3645, #49776, #31253 ) ) ;
#84107=CARTESIAN_POINT ( 'NONE',  ( 33.58349330513380693, 1.593028355512270962E-15, 0.000000000000000000 ) ) ;
#84123=DIRECTION ( 'NONE',  ( 0.000000000000000000, 0.000000000000000000, 1.000000000000000000 ) ) ;
#84184=DIRECTION ( 'NONE',  ( 0.000000000000000000, -1.000000000000000000, 0.000000000000000000 ) ) ;
#84232=CARTESIAN_POINT ( 'NONE',  ( 10.59999999999999609, 1.533819458162526451E-15, 0.000000000000000000 ) ) ;
#84241=DIRECTION ( 'NONE',  ( 0.000000000000000000, -1.000000000000000000, 0.000000000000000000 ) ) ;
#84258=CARTESIAN_POINT ( 'NONE',  ( 6.162888688655347558, -7.505553499465142053, -3.129864801432410934E-16 ) ) ;
#84296=CARTESIAN_POINT ( 'NONE',  ( 26.36650669486618881, 4.898587196589413815E-16, -4.000000000000000888 ) ) ;
#84329=DIRECTION ( 'NONE',  ( 0.000000000000000000, 0.000000000000000000, 1.000000000000000000 ) ) ;
#84364=DIRECTION ( 'NONE',  ( -1.000000000000000000, -1.224606353822377258E-16, -0.000000000000000000 ) ) ;
#84372=DIRECTION ( 'NONE',  ( -1.000000000000000000, -0.000000000000000000, -0.000000000000000000 ) ) ;
#84374=DIRECTION ( 'NONE',  ( 0.000000000000000000, -1.000000000000000000, 0.000000000000000000 ) ) ;
#84386=EDGE_CURVE ( 'NONE', #75403, #71690, #12616, .T. ) ;
#84419=DIRECTION ( 'NONE',  ( -1.000000000000000000, 0.000000000000000000, -0.000000000000000000 ) ) ;
#84423=EDGE_CURVE ( 'NONE', #16221, #87702, #12911, .T. ) ;
#84424=ADVANCED_FACE ( 'NONE', ( #93323 ), #100471, .T. ) ;
#84430=EDGE_CURVE ( 'NONE', #7161, #42192, #79760, .T. ) ;
#84448=DIRECTION ( 'NONE',  ( 0.000000000000000000, -1.000000000000000000, 0.000000000000000000 ) ) ;
#84509=ORIENTED_EDGE ( 'NONE', *, *, #55410, .T. ) ;
#84518=VECTOR ( 'NONE', #80845, 1000.000000000000341 ) ;
#84519=LINE ( 'NONE', #86662, #18326 ) ;
#84539=CARTESIAN_POINT ( 'NONE',  ( 24.34999999999999787, 3.309500000000003439, 0.000000000000000000 ) ) ;
#84557=LINE ( 'NONE', #26361, #8070 ) ;
#84562=CIRCLE ( 'NONE', #27792, 3.309500000000001663 ) ;
#84576=ORIENTED_EDGE ( 'NONE', *, *, #72468, .T. ) ;
#84607=DIRECTION ( 'NONE',  ( -1.000000000000000000, -0.000000000000000000, -0.000000000000000000 ) ) ;
#84627=ORIENTED_EDGE ( 'NONE', *, *, #57313, .F. ) ;
#84650=CARTESIAN_POINT ( 'NONE',  ( 20.11650669486618881, 1.474610560812782335E-15, 0.000000000000000000 ) ) ;
#84654=DIRECTION ( 'NONE',  ( 0.5735764363510490460, 0.8191520442889896891, 0.000000000000000000 ) ) ;
#84679=CARTESIAN_POINT ( 'NONE',  ( 0.000000000000000000, 4.898587196589413815E-16, -4.000000000000000888 ) ) ;
#84717=CONICAL_SURFACE ( 'NONE', #45162, 3.309500000000001663, 0.9599310885968770357 ) ;
#84762=CARTESIAN_POINT ( 'NONE',  ( 6.936184427528457874, 0.000000000000000000, 0.000000000000000000 ) ) ;
#84766=VERTEX_POINT ( 'NONE', #42508 ) ;
#84798=UNCERTAINTY_MEASURE_WITH_UNIT (LENGTH_MEASURE( 1.000000000000000082E-05 ), #28863, 'distance_accuracy_value', 'NONE');
#84857=VERTEX_POINT ( 'NONE', #102883 ) ;
#84896=ADVANCED_FACE ( 'NONE', ( #35523 ), #54029, .T. ) ;
#84909=CARTESIAN_POINT ( 'NONE',  ( 30.59999999999999787, -3.309499999999999886, 4.475777889183790779E-16 ) ) ;
#84917=ORIENTED_EDGE ( 'NONE', *, *, #51750, .T. ) ;
#84932=CARTESIAN_POINT ( 'NONE',  ( 16.36650669486618881, 0.000000000000000000, 4.000000000000000888 ) ) ;
#84952=ADVANCED_FACE ( 'NONE', ( #14372 ), #7531, .T. ) ;
#84965=AXIS2_PLACEMENT_3D ( 'NONE', #72972, #15816, #10241 ) ;
#84973=AXIS2_PLACEMENT_3D ( 'NONE', #84107, #26444, #36136 ) ;
#84999=ORIENTED_EDGE ( 'NONE', *, *, #28229, .F. ) ;
#85014=ORIENTED_EDGE ( 'NONE', *, *, #31479, .F. ) ;
#85023=AXIS2_PLACEMENT_3D ( 'NONE', #89880, #7880, #40787 ) ;
#85030=FACE_OUTER_BOUND ( 'NONE', #63012, .T. ) ;
#85098=CARTESIAN_POINT ( 'NONE',  ( 22.61650669486618526, 4.000000000000003553, 4.898587196589414801E-16 ) ) ;
#85114=ORIENTED_EDGE ( 'NONE', *, *, #73491, .T. ) ;
#85129=ORIENTED_EDGE ( 'NONE', *, *, #41488, .F. ) ;
#85130=DIRECTION ( 'NONE',  ( 1.000000000000000000, 1.224606353822377258E-16, 0.000000000000000000 ) ) ;
#85141=CARTESIAN_POINT ( 'NONE',  ( 0.000000000000000000, 0.000000000000000000, 4.000000000000000888 ) ) ;
#85150=ORIENTED_EDGE ( 'NONE', *, *, #28397, .F. ) ;
#85176=DIRECTION ( 'NONE',  ( -1.000000000000000000, -1.224606353822377258E-16, -0.000000000000000000 ) ) ;
#85184=CARTESIAN_POINT ( 'NONE',  ( 5.947762761376476526, 4.378239541354660425, -5.416666666666668739 ) ) ;
#85204=CARTESIAN_POINT ( 'NONE',  ( 32.33349330513380693, -3.851859888774471706E-31, 4.000000000000001776 ) ) ;
#85209=CARTESIAN_POINT ( 'NONE',  ( 32.61650669486618881, 0.000000000000000000, 4.000000000000000888 ) ) ;
#85230=EDGE_CURVE ( 'NONE', #60761, #22594, #101183, .T. ) ;
#85240=EDGE_CURVE ( 'NONE', #16503, #64476, #76048, .T. ) ;
#85255=DIRECTION ( 'NONE',  ( -1.000000000000000000, -1.224606353822377258E-16, -0.000000000000000000 ) ) ;
#85283=CARTESIAN_POINT ( 'NONE',  ( 21.08349330513380693, 1.593028355512270962E-15, 0.000000000000000000 ) ) ;
#85315=ORIENTED_EDGE ( 'NONE', *, *, #54559, .F. ) ;
#85335=ADVANCED_FACE ( 'NONE', ( #21890 ), #105780, .T. ) ;
#85346=EDGE_CURVE ( 'NONE', #8297, #62772, #11071, .T. ) ;
#85373=CIRCLE ( 'NONE', #52648, 3.309500000000001663 ) ;
#85393=ORIENTED_EDGE ( 'NONE', *, *, #37845, .F. ) ;
#85440=CARTESIAN_POINT ( 'NONE',  ( 13.09999999999999787, 3.309500000000003439, 4.052968581778167743E-16 ) ) ;
#85470=CIRCLE ( 'NONE', #99217, 4.000000000000000888 ) ;
#85501=CARTESIAN_POINT ( 'NONE',  ( 34.83349330513380693, 4.000000000000003553, 0.000000000000000000 ) ) ;
#85532=EDGE_CURVE ( 'NONE', #66358, #30441, #35306, .T. ) ;
#85535=EDGE_LOOP ( 'NONE', ( #41198, #30860, #99619, #43601, #36873 ) ) ;
#85591=AXIS2_PLACEMENT_3D ( 'NONE', #2323, #35811, #86481 ) ;
#85593=EDGE_LOOP ( 'NONE', ( #65049, #45843, #17260, #104506, #19548 ) ) ;
#85607=CARTESIAN_POINT ( 'NONE',  ( 23.09999999999999432, -3.309499999999999886, 0.000000000000000000 ) ) ;
#85612=ORIENTED_EDGE ( 'NONE', *, *, #91290, .T. ) ;
#85617=CIRCLE ( 'NONE', #80418, 4.000000000000001776 ) ;
#85618=AXIS2_PLACEMENT_3D ( 'NONE', #104323, #54166, #69852 ) ;
#85672=CIRCLE ( 'NONE', #99406, 4.000000000000000888 ) ;
#85679=LINE ( 'NONE', #18294, #28873 ) ;
#85684=EDGE_LOOP ( 'NONE', ( #55894, #46128, #53140, #76740 ) ) ;
#85695=ORIENTED_EDGE ( 'NONE', *, *, #78610, .T. ) ;
#85733=CIRCLE ( 'NONE', #23678, 4.000000000000000888 ) ;
#85762=CIRCLE ( 'NONE', #49538, 4.000000000000000888 ) ;
#85774=AXIS2_PLACEMENT_3D ( 'NONE', #36207, #60983, #12929 ) ;
#85784=CIRCLE ( 'NONE', #1348, 3.309500000000001663 ) ;
#85786=DIRECTION ( 'NONE',  ( -1.000000000000000000, -0.000000000000000000, -0.000000000000000000 ) ) ;
#85799=AXIS2_PLACEMENT_3D ( 'NONE', #81868, #32304, #8525 ) ;
#85865=DIRECTION ( 'NONE',  ( -0.5735764363510497121, 0.8191520442889892450, 1.003171929053521665E-16 ) ) ;
#85868=CARTESIAN_POINT ( 'NONE',  ( 8.866506694866188809, 1.474610560812782335E-15, 0.000000000000000000 ) ) ;
#85943=CARTESIAN_POINT ( 'NONE',  ( 37.40949999999997289, 0.000000000000000000, 4.000000000000001776 ) ) ;
#85944=ORIENTED_EDGE ( 'NONE', *, *, #64066, .T. ) ;
#85946=ORIENTED_EDGE ( 'NONE', *, *, #96592, .T. ) ;
#86010=EDGE_CURVE ( 'NONE', #54573, #92082, #64687, .T. ) ;
#86037=CONICAL_SURFACE ( 'NONE', #1600, 4.000000000000001776, 0.9599310885968774798 ) ;
#86042=CIRCLE ( 'NONE', #25793, 4.000000000000000888 ) ;
#86052=EDGE_LOOP ( 'NONE', ( #93880, #98671, #56320, #66841, #64532 ) ) ;
#86058=VERTEX_POINT ( 'NONE', #56030 ) ;
#86068=ORIENTED_EDGE ( 'NONE', *, *, #58413, .F. ) ;
#86084=LINE ( 'NONE', #61811, #62845 ) ;
#86119=CARTESIAN_POINT ( 'NONE',  ( 0.000000000000000000, 4.898587196589413815E-16, -4.000000000000000888 ) ) ;
#86129=DIRECTION ( 'NONE',  ( 0.000000000000000000, -1.000000000000000000, 0.000000000000000000 ) ) ;
#86151=CARTESIAN_POINT ( 'NONE',  ( 7.500000000000001776, 0.000000000000000000, 8.400000000000000355 ) ) ;
#86183=DIRECTION ( 'NONE',  ( 0.000000000000000000, -1.000000000000000000, 0.000000000000000000 ) ) ;
#86198=ORIENTED_EDGE ( 'NONE', *, *, #62048, .F. ) ;
#86267=EDGE_CURVE ( 'NONE', #17393, #45061, #91644, .T. ) ;
#86272=CARTESIAN_POINT ( 'NONE',  ( 5.691929483231184861, 5.629165124598851655, -3.249999999999999556 ) ) ;
#86291=DIRECTION ( 'NONE',  ( -1.000000000000000000, -1.224606353822377258E-16, -0.000000000000000000 ) ) ;
#86298=ORIENTED_EDGE ( 'NONE', *, *, #57707, .T. ) ;
#86300=CARTESIAN_POINT ( 'NONE',  ( 0.000000000000000000, 4.898587196589413815E-16, -4.000000000000000888 ) ) ;
#86304=B_SPLINE_CURVE_WITH_KNOTS ( 'NONE', 3,
 ( #29287, #96106, #55089, #11447, #77800, #29809 ),
 .UNSPECIFIED., .F., .F.,
 ( 4, 2, 4 ),
 ( 0.000000000000000000, 0.001995463903526787514, 0.003990927807053575027 ),
 .UNSPECIFIED. ) ;
#86319=DIRECTION ( 'NONE',  ( 0.000000000000000000, -1.000000000000000000, 0.000000000000000000 ) ) ;
#86360=AXIS2_PLACEMENT_3D ( 'NONE', #88097, #6096, #70321 ) ;
#86371=VECTOR ( 'NONE', #51072, 1000.000000000000000 ) ;
#86387=CARTESIAN_POINT ( 'NONE',  ( 0.000000000000000000, 0.000000000000000000, 4.000000000000000888 ) ) ;
#86401=ORIENTED_EDGE ( 'NONE', *, *, #41989, .F. ) ;
#86408=DIRECTION ( 'NONE',  ( 0.000000000000000000, -1.000000000000000000, 0.000000000000000000 ) ) ;
#86433=CONICAL_SURFACE ( 'NONE', #8931, 3.309499999999999886, 0.7853981633974369547 ) ;
#86435=ORIENTED_EDGE ( 'NONE', *, *, #100591, .T. ) ;
#86463=CONICAL_SURFACE ( 'NONE', #57166, 3.309500000000001663, 0.9599310885968770357 ) ;
#86481=DIRECTION ( 'NONE',  ( -0.000000000000000000, 0.000000000000000000, -1.000000000000000000 ) ) ;
#86524=CARTESIAN_POINT ( 'NONE',  ( 6.644028492724102897, 7.802520252160764613, 9.720400798523309454E-13 ) ) ;
#86585=CARTESIAN_POINT ( 'NONE',  ( 6.162888688655344005, 3.752776749732565253, 6.499999999999997335 ) ) ;
#86589=DIRECTION ( 'NONE',  ( 0.000000000000000000, -1.000000000000000000, 0.000000000000000000 ) ) ;
#86602=FILL_AREA_STYLE ('',( #88695 ) ) ;
#86614=AXIS2_PLACEMENT_3D ( 'NONE', #28575, #2658, #61462 ) ;
#86628=ORIENTED_EDGE ( 'NONE', *, *, #58254, .T. ) ;
#86640=EDGE_CURVE ( 'NONE', #16503, #52389, #68140, .T. ) ;
#86662=CARTESIAN_POINT ( 'NONE',  ( 36.08349330513379982, 4.000000000000003553, 0.000000000000000000 ) ) ;
#86675=EDGE_CURVE ( 'NONE', #55271, #19214, #66439, .T. ) ;
#86689=B_SPLINE_CURVE_WITH_KNOTS ( 'NONE', 3,
 ( #7917, #59150, #74771, #849, #41354, #33288, #40820, #16018, #9503, #91518 ),
 .UNSPECIFIED., .F., .F.,
 ( 4, 2, 2, 2, 4 ),
 ( 0.000000000000000000, 0.001993803085173303895, 0.003987606170346607790, 0.005981409255519911684, 0.007975212340693215579 ),
 .UNSPECIFIED. ) ;
#86697=FACE_OUTER_BOUND ( 'NONE', #73763, .T. ) ;
#86701=DIRECTION ( 'NONE',  ( -1.000000000000000000, -1.224606353822377258E-16, -0.000000000000000000 ) ) ;
#86720=DIRECTION ( 'NONE',  ( 0.5735764363510490460, 0.8191520442889896891, 0.000000000000000000 ) ) ;
#86726=ADVANCED_FACE ( 'NONE', ( #55938 ), #63556, .T. ) ;
#86728=FACE_OUTER_BOUND ( 'NONE', #15480, .T. ) ;
#86755=VECTOR ( 'NONE', #99630, 1000.000000000000000 ) ;
#86761=AXIS2_PLACEMENT_3D ( 'NONE', #12061, #20216, #29357 ) ;
#86797=VERTEX_POINT ( 'NONE', #66190 ) ;
#86800=ORIENTED_EDGE ( 'NONE', *, *, #3652, .T. ) ;
#86853=DIRECTION ( 'NONE',  ( -1.000000000000000000, -1.224606353822377258E-16, -0.000000000000000000 ) ) ;
#86920=CARTESIAN_POINT ( 'NONE',  ( 32.33349330513380693, -4.000000000000000888, 4.898587196589416773E-16 ) ) ;
#86974=ADVANCED_FACE ( 'NONE', ( #45652 ), #92217, .T. ) ;
#86998=ORIENTED_EDGE ( 'NONE', *, *, #34197, .F. ) ;
#87011=CONICAL_SURFACE ( 'NONE', #62910, 4.000000000000001776, 0.9599310885968774798 ) ;
#87044=CARTESIAN_POINT ( 'NONE',  ( 28.58349330513380337, 4.000000000000003553, 0.000000000000000000 ) ) ;
#87062=VERTEX_POINT ( 'NONE', #88755 ) ;
#87065=EDGE_CURVE ( 'NONE', #23216, #71690, #21925, .T. ) ;
#87118=LINE ( 'NONE', #61248, #1593 ) ;
#87129=EDGE_CURVE ( 'NONE', #98079, #36198, #74670, .T. ) ;
#87138=ORIENTED_EDGE ( 'NONE', *, *, #72474, .F. ) ;
#87186=EDGE_CURVE ( 'NONE', #99203, #68693, #59369, .T. ) ;
#87204=CARTESIAN_POINT ( 'NONE',  ( 5.947762761376476526, 2.501851166488377576, 6.500000000000000000 ) ) ;
#87241=VERTEX_POINT ( 'NONE', #101631 ) ;
#87245=CIRCLE ( 'NONE', #61469, 3.309500000000001663 ) ;
#87257=CONICAL_SURFACE ( 'NONE', #32140, 3.309500000000001663, 0.9599310885968770357 ) ;
#87265=ORIENTED_EDGE ( 'NONE', *, *, #51061, .F. ) ;
#87286=EDGE_LOOP ( 'NONE', ( #2872, #100545, #15618, #54448, #6734 ) ) ;
#87298=AXIS2_PLACEMENT_3D ( 'NONE', #44459, #25655, #34803 ) ;
#87312=AXIS2_PLACEMENT_3D ( 'NONE', #2975, #35932, #1362 ) ;
#87328=AXIS2_PLACEMENT_3D ( 'NONE', #34180, #17978, #11448 ) ;
#87338=CARTESIAN_POINT ( 'NONE',  ( 33.09999999999999432, 3.309500000000003439, 0.000000000000000000 ) ) ;
#87340=ADVANCED_FACE ( 'NONE', ( #99823 ), #19761, .T. ) ;
#87357=CARTESIAN_POINT ( 'NONE',  ( 6.585468679846621320, 3.617797563910810865, 6.733790807807553236 ) ) ;
#87368=CIRCLE ( 'NONE', #21946, 4.000000000000001776 ) ;
#87372=ORIENTED_EDGE ( 'NONE', *, *, #66363, .F. ) ;
#87378=VERTEX_POINT ( 'NONE', #99272 ) ;
#87384=AXIS2_PLACEMENT_3D ( 'NONE', #78704, #37773, #70635 ) ;
#87393=ORIENTED_EDGE ( 'NONE', *, *, #16250, .T. ) ;
#87397=ORIENTED_EDGE ( 'NONE', *, *, #1716, .F. ) ;
#87438=ORIENTED_EDGE ( 'NONE', *, *, #41488, .T. ) ;
#87463=AXIS2_PLACEMENT_3D ( 'NONE', #53922, #86853, #70654 ) ;
#87525=DIRECTION ( 'NONE',  ( -1.000000000000000000, -1.224606353822377258E-16, -0.000000000000000000 ) ) ;
#87531=CARTESIAN_POINT ( 'NONE',  ( 8.866506694866188809, -3.999999999999998224, 0.000000000000000000 ) ) ;
#87532=EDGE_CURVE ( 'NONE', #96201, #35207, #42652, .T. ) ;
#87583=EDGE_CURVE ( 'NONE', #876, #826, #42181, .T. ) ;
#87595=AXIS2_PLACEMENT_3D ( 'NONE', #15465, #72114, #14928 ) ;
#87603=ORIENTED_EDGE ( 'NONE', *, *, #28229, .T. ) ;
#87630=VECTOR ( 'NONE', #101417, 1000.000000000000000 ) ;
#87631=CARTESIAN_POINT ( 'NONE',  ( 8.099999999999999645, -3.752776749732574135, -6.500000000000001776 ) ) ;
#87640=CIRCLE ( 'NONE', #101412, 3.309500000000001663 ) ;
#87641=DIRECTION ( 'NONE',  ( -0.5735764363510497121, 0.8191520442889892450, 1.003171929053521665E-16 ) ) ;
#87647=SURFACE_STYLE_FILL_AREA ( #86602 ) ;
#87663=DIRECTION ( 'NONE',  ( -1.000000000000000000, -0.000000000000000000, -0.000000000000000000 ) ) ;
#87664=EDGE_CURVE ( 'NONE', #26284, #83206, #69763, .T. ) ;
#87682=VERTEX_POINT ( 'NONE', #84296 ) ;
#87699=DIRECTION ( 'NONE',  ( -1.000000000000000000, -1.224606353822377258E-16, -0.000000000000000000 ) ) ;
#87702=VERTEX_POINT ( 'NONE', #91854 ) ;
#87722=EDGE_CURVE ( 'NONE', #96540, #45187, #31887, .T. ) ;
#87728=EDGE_CURVE ( 'NONE', #89753, #21060, #71510, .T. ) ;
#87799=CARTESIAN_POINT ( 'NONE',  ( 26.08349330513380693, 4.898587196589411843E-16, -4.000000000000001776 ) ) ;
#87844=CONICAL_SURFACE ( 'NONE', #49932, 8.605212085995399107, 1.221730476396037490 ) ;
#87888=ORIENTED_EDGE ( 'NONE', *, *, #15775, .F. ) ;
#87915=ORIENTED_EDGE ( 'NONE', *, *, #16250, .F. ) ;
#87930=CARTESIAN_POINT ( 'NONE',  ( 0.000000000000000000, 1.502314598737160412E-15, 6.500000000000000888 ) ) ;
#87957=DIRECTION ( 'NONE',  ( -1.000000000000000000, -0.000000000000000000, -0.000000000000000000 ) ) ;
#87958=CIRCLE ( 'NONE', #75930, 4.000000000000001776 ) ;
#87964=VERTEX_POINT ( 'NONE', #45315 ) ;
#88072=CARTESIAN_POINT ( 'NONE',  ( 5.975663821520919683, -4.257391242883398874, 5.625982059627139265 ) ) ;
#88074=VERTEX_POINT ( 'NONE', #72741 ) ;
#88087=ORIENTED_EDGE ( 'NONE', *, *, #62163, .T. ) ;
#88097=CARTESIAN_POINT ( 'NONE',  ( 0.000000000000000000, 0.000000000000000000, 0.000000000000000000 ) ) ;
#88131=VERTEX_POINT ( 'NONE', #47931 ) ;
#88139=AXIS2_PLACEMENT_3D ( 'NONE', #63762, #40007, #73409 ) ;
#88142=LINE ( 'NONE', #47126, #70249 ) ;
#88178=CONICAL_SURFACE ( 'NONE', #15869, 6.500000000000000000, 1.047197551196600296 ) ;
#88197=EDGE_CURVE ( 'NONE', #67545, #23216, #47485, .T. ) ;
#88201=LINE ( 'NONE', #39127, #43408 ) ;
#88207=ORIENTED_EDGE ( 'NONE', *, *, #96914, .F. ) ;
#88219=DIRECTION ( 'NONE',  ( -1.000000000000000000, -0.000000000000000000, -0.000000000000000000 ) ) ;
#88239=CARTESIAN_POINT ( 'NONE',  ( 9.833493305133805151, 1.593028355512270962E-15, 0.000000000000000000 ) ) ;
#88240=DIRECTION ( 'NONE',  ( 0.000000000000000000, 1.000000000000000000, 0.000000000000000000 ) ) ;
#88288=CARTESIAN_POINT ( 'NONE',  ( 0.05458999538772899701, -1.264741368073337036, -6.500000000000000888 ) ) ;
#88295=ORIENTED_EDGE ( 'NONE', *, *, #60558, .T. ) ;
#88306=VERTEX_POINT ( 'NONE', #102347 ) ;
#88334=ORIENTED_EDGE ( 'NONE', *, *, #14307, .T. ) ;
#88349=VECTOR ( 'NONE', #26566, 1000.000000000000000 ) ;
#88365=CARTESIAN_POINT ( 'NONE',  ( 14.83349330513380693, 1.593028355512270962E-15, 0.000000000000000000 ) ) ;
#88375=DIRECTION ( 'NONE',  ( -1.000000000000000000, -1.224606353822377258E-16, -0.000000000000000000 ) ) ;
#88406=DIRECTION ( 'NONE',  ( -1.000000000000000000, -0.000000000000000000, -0.000000000000000000 ) ) ;
#88411=EDGE_LOOP ( 'NONE', ( #36731, #6572, #78113, #90366, #28981 ) ) ;
#88415=CARTESIAN_POINT ( 'NONE',  ( 6.692588830498428898, 7.935834885954428763, -0.04058884017440173020 ) ) ;
#88573=VERTEX_POINT ( 'NONE', #2873 ) ;
#88594=ORIENTED_EDGE ( 'NONE', *, *, #97724, .T. ) ;
#88602=CARTESIAN_POINT ( 'NONE',  ( 6.289692432696785573, -1.240526984323783911E-13, -6.828989928337169779 ) ) ;
#88608=FACE_OUTER_BOUND ( 'NONE', #80641, .T. ) ;
#88621=VERTEX_POINT ( 'NONE', #98128 ) ;
#88622=EDGE_CURVE ( 'NONE', #96540, #82575, #73306, .T. ) ;
#88647=FACE_OUTER_BOUND ( 'NONE', #73921, .T. ) ;
#88662=DIRECTION ( 'NONE',  ( -0.000000000000000000, 1.000000000000000000, 1.224646799147353207E-16 ) ) ;
#88667=EDGE_CURVE ( 'NONE', #87378, #99203, #92696, .T. ) ;
#88673=FACE_OUTER_BOUND ( 'NONE', #24999, .T. ) ;
#88684=DIRECTION ( 'NONE',  ( -1.000000000000000000, -1.224606353822377258E-16, -0.000000000000000000 ) ) ;
#88695=FILL_AREA_STYLE_COLOUR ( '', #90168 ) ;
#88697=AXIS2_PLACEMENT_3D ( 'NONE', #105951, #24023, #105438 ) ;
#88714=EDGE_CURVE ( 'NONE', #67595, #83791, #99216, .T. ) ;
#88716=DIRECTION ( 'NONE',  ( 0.000000000000000000, -1.000000000000000000, 0.000000000000000000 ) ) ;
#88717=EDGE_LOOP ( 'NONE', ( #44868, #49859, #42664, #104932, #80386, #20960 ) ) ;
#88718=CARTESIAN_POINT ( 'NONE',  ( 14.83349330513380693, 1.593028355512270962E-15, 0.000000000000000000 ) ) ;
#88755=CARTESIAN_POINT ( 'NONE',  ( 32.61650669486618881, 4.898587196589413815E-16, -4.000000000000000888 ) ) ;
#88756=DIRECTION ( 'NONE',  ( 0.3420201433256622736, 0.000000000000000000, -0.9396926207859106484 ) ) ;
#88758=CIRCLE ( 'NONE', #66581, 4.000000000000000888 ) ;
#88791=CARTESIAN_POINT ( 'NONE',  ( 37.33349330513379982, 4.000000000000002665, 0.000000000000000000 ) ) ;
#88800=VERTEX_POINT ( 'NONE', #50439 ) ;
#88851=AXIS2_PLACEMENT_3D ( 'NONE', #30331, #13044, #45449 ) ;
#88870=ORIENTED_EDGE ( 'NONE', *, *, #3652, .F. ) ;
#88875=ORIENTED_EDGE ( 'NONE', *, *, #43625, .T. ) ;
#88876=CARTESIAN_POINT ( 'NONE',  ( 19.34999999999999787, 1.533819458162526451E-15, 0.000000000000000000 ) ) ;
#88916=CARTESIAN_POINT ( 'NONE',  ( 13.86650669486618881, 1.474610560812782335E-15, 0.000000000000000000 ) ) ;
#88955=DIRECTION ( 'NONE',  ( 0.000000000000000000, -1.000000000000000000, 0.000000000000000000 ) ) ;
#88987=CIRCLE ( 'NONE', #38790, 4.000000000000001776 ) ;
#89000=ORIENTED_EDGE ( 'NONE', *, *, #28390, .T. ) ;
#89012=AXIS2_PLACEMENT_3D ( 'NONE', #54687, #13705, #53645 ) ;
#89052=AXIS2_PLACEMENT_3D ( 'NONE', #63969, #57423, #64491 ) ;
#89084=FACE_OUTER_BOUND ( 'NONE', #14977, .T. ) ;
#89103=EDGE_LOOP ( 'NONE', ( #16942, #51199, #17519, #39144, #63304, #82525 ) ) ;
#89211=VERTEX_POINT ( 'NONE', #80371 ) ;
#89248=DIRECTION ( 'NONE',  ( 0.000000000000000000, -1.000000000000000000, 0.000000000000000000 ) ) ;
#89250=CARTESIAN_POINT ( 'NONE',  ( 0.05613245601036472715, 1.278525034529253590, 6.499999999999997335 ) ) ;
#89278=ORIENTED_EDGE ( 'NONE', *, *, #34126, .F. ) ;
#89287=CARTESIAN_POINT ( 'NONE',  ( 0.4053525175236821210, 3.145852061456245519, -6.500000000000001776 ) ) ;
#89290=ORIENTED_EDGE ( 'NONE', *, *, #77037, .F. ) ;
#89294=AXIS2_PLACEMENT_3D ( 'NONE', #7366, #103427, #95876 ) ;
#89317=DIRECTION ( 'NONE',  ( 1.000000000000000000, 1.224606353822377258E-16, 0.000000000000000000 ) ) ;
#89336=B_SPLINE_CURVE_WITH_KNOTS ( 'NONE', 3,
 ( #30601, #29554, #88288, #55358, #39737, #95317 ),
 .UNSPECIFIED., .F., .F.,
 ( 4, 2, 4 ),
 ( 0.02294124189247801621, 0.02484059228080999493, 0.02673994266914197365 ),
 .UNSPECIFIED. ) ;
#89351=FACE_OUTER_BOUND ( 'NONE', #89103, .T. ) ;
#89371=EDGE_LOOP ( 'NONE', ( #44310, #65410, #45200, #28041, #84509 ) ) ;
#89376=CARTESIAN_POINT ( 'NONE',  ( 6.585530689845733754, -4.023059358968673394, -6.500000000000002665 ) ) ;
#89417=CARTESIAN_POINT ( 'NONE',  ( 18.58349330513380693, 1.593028355512270962E-15, 0.000000000000000000 ) ) ;
#89474=CARTESIAN_POINT ( 'NONE',  ( 0.1061556211655338700, -4.836380039389421626, 4.623144047065555817 ) ) ;
#89497=VECTOR ( 'NONE', #34010, 1000.000000000000000 ) ;
#89504=CIRCLE ( 'NONE', #75715, 4.000000000000001776 ) ;
#89516=CARTESIAN_POINT ( 'NONE',  ( 0.5805565836007664515, -7.505553499465142053, -1.357586595304856736E-16 ) ) ;
#89633=ORIENTED_EDGE ( 'NONE', *, *, #61176, .T. ) ;
#89636=CARTESIAN_POINT ( 'NONE',  ( 10.11650669486618881, -3.999999999999998224, 0.000000000000000000 ) ) ;
#89647=ADVANCED_FACE ( 'NONE', ( #31216 ), #30821, .T. ) ;
#89651=ADVANCED_FACE ( 'NONE', ( #48930 ), #16050, .T. ) ;
#89690=CARTESIAN_POINT ( 'NONE',  ( 27.33349330513380693, -4.000000000000000000, 4.898587196589415787E-16 ) ) ;
#89709=EDGE_CURVE ( 'NONE', #62772, #81897, #23967, .T. ) ;
#89731=DIRECTION ( 'NONE',  ( -0.5735764363510494901, -0.8191520442889894671, 0.000000000000000000 ) ) ;
#89752=DIRECTION ( 'NONE',  ( 0.000000000000000000, 0.000000000000000000, -1.000000000000000000 ) ) ;
#89753=VERTEX_POINT ( 'NONE', #15518 ) ;
#89787=DIRECTION ( 'NONE',  ( 0.000000000000000000, -1.000000000000000000, 0.000000000000000000 ) ) ;
#89789=DIRECTION ( 'NONE',  ( 0.000000000000000000, 0.000000000000000000, 1.000000000000000000 ) ) ;
#89805=ORIENTED_EDGE ( 'NONE', *, *, #86267, .T. ) ;
#89811=CIRCLE ( 'NONE', #15721, 4.000000000000001776 ) ;
#89863=FACE_OUTER_BOUND ( 'NONE', #66934, .T. ) ;
#89880=CARTESIAN_POINT ( 'NONE',  ( 18.58349330513380693, 1.593028355512270962E-15, 0.000000000000000000 ) ) ;
#89912=ORIENTED_EDGE ( 'NONE', *, *, #1716, .T. ) ;
#89924=EDGE_LOOP ( 'NONE', ( #67453, #17182, #102328, #106235, #2389 ) ) ;
#89929=CARTESIAN_POINT ( 'NONE',  ( 32.33349330513380693, 1.593028355512270962E-15, 0.000000000000000000 ) ) ;
#89932=EDGE_LOOP ( 'NONE', ( #103406, #42537, #90992 ) ) ;
#90006=ORIENTED_EDGE ( 'NONE', *, *, #48925, .T. ) ;
#90023=DIRECTION ( 'NONE',  ( 0.000000000000000000, -1.000000000000000000, 0.000000000000000000 ) ) ;
#90030=VERTEX_POINT ( 'NONE', #103364 ) ;
#90053=ORIENTED_EDGE ( 'NONE', *, *, #5394, .T. ) ;
#90138=VERTEX_POINT ( 'NONE', #52669 ) ;
#90141=VERTEX_POINT ( 'NONE', #28437 ) ;
#90168=COLOUR_RGB ( '', 0.08235294, 0.09019608, 0.10196078) ;
#90180=DIRECTION ( 'NONE',  ( 0.000000000000000000, 1.000000000000000000, 0.000000000000000000 ) ) ;
#90190=CARTESIAN_POINT ( 'NONE',  ( 6.466227039643135832, 2.668354129823745868, 6.840182550749494439 ) ) ;
#90221=DIRECTION ( 'NONE',  ( 0.000000000000000000, -1.000000000000000000, 0.000000000000000000 ) ) ;
#90232=CARTESIAN_POINT ( 'NONE',  ( 16.36650669486618881, 4.898587196589413815E-16, -4.000000000000000888 ) ) ;
#90238=DIRECTION ( 'NONE',  ( -1.000000000000000000, -0.000000000000000000, -0.000000000000000000 ) ) ;
#90245=AXIS2_PLACEMENT_3D ( 'NONE', #97303, #96277, #71432 ) ;
#90250=VERTEX_POINT ( 'NONE', #48283 ) ;
#90254=EDGE_CURVE ( 'NONE', #99250, #46570, #72750, .T. ) ;
#90263=AXIS2_PLACEMENT_3D ( 'NONE', #35486, #41940, #75905 ) ;
#90276=CARTESIAN_POINT ( 'NONE',  ( 6.463481858019718196, 7.246446802359423067, -1.128819432756289487 ) ) ;
#90299=AXIS2_PLACEMENT_3D ( 'NONE', #105549, #103044, #6306 ) ;
#90357=CARTESIAN_POINT ( 'NONE',  ( 6.281175601187045210, -7.505553499465143830, -3.129864801432403538E-16 ) ) ;
#90366=ORIENTED_EDGE ( 'NONE', *, *, #59305, .F. ) ;
#90385=AXIS2_PLACEMENT_3D ( 'NONE', #9356, #44414, #51425 ) ;
#90401=VERTEX_POINT ( 'NONE', #82399 ) ;
#90455=ORIENTED_EDGE ( 'NONE', *, *, #67903, .T. ) ;
#90474=CARTESIAN_POINT ( 'NONE',  ( 0.000000000000000000, -5.629165124598850767, -3.249999999999999556 ) ) ;
#90495=ORIENTED_EDGE ( 'NONE', *, *, #21149, .F. ) ;
#90503=DIRECTION ( 'NONE',  ( 0.000000000000000000, -1.000000000000000000, 0.000000000000000000 ) ) ;
#90514=CARTESIAN_POINT ( 'NONE',  ( 6.445370176741570312, -4.584736124523163703, -5.738941594273955893 ) ) ;
#90535=CIRCLE ( 'NONE', #9596, 4.000000000000001776 ) ;
#90542=VECTOR ( 'NONE', #34688, 1000.000000000000000 ) ;
#90568=CARTESIAN_POINT ( 'NONE',  ( 28.09999999999999787, 3.309500000000003439, 0.000000000000000000 ) ) ;
#90580=ORIENTED_EDGE ( 'NONE', *, *, #66819, .F. ) ;
#90625=VERTEX_POINT ( 'NONE', #84539 ) ;
#90655=CARTESIAN_POINT ( 'NONE',  ( 36.84999999999999432, -3.309499999999999886, 4.475777889183790779E-16 ) ) ;
#90676=ORIENTED_EDGE ( 'NONE', *, *, #5155, .F. ) ;
#90692=AXIS2_PLACEMENT_3D ( 'NONE', #100371, #25829, #58683 ) ;
#90707=CIRCLE ( 'NONE', #89012, 4.000000000000001776 ) ;
#90719=DIRECTION ( 'NONE',  ( -1.000000000000000000, -0.000000000000000000, -0.000000000000000000 ) ) ;
#90722=CYLINDRICAL_SURFACE ( 'NONE', #57224, 4.000000000000000888 ) ;
#90726=CARTESIAN_POINT ( 'NONE',  ( 5.818834259648335561, 0.6677920147389573291, 6.499999999999999112 ) ) ;
#90736=EDGE_CURVE ( 'NONE', #38226, #36198, #70595, .T. ) ;
#90755=ORIENTED_EDGE ( 'NONE', *, *, #19349, .F. ) ;
#90757=DIRECTION ( 'NONE',  ( 0.000000000000000000, -1.000000000000000000, 0.000000000000000000 ) ) ;
#90773=CIRCLE ( 'NONE', #32188, 4.000000000000000888 ) ;
#90778=EDGE_CURVE ( 'NONE', #17393, #63739, #55008, .T. ) ;
#90790=CARTESIAN_POINT ( 'NONE',  ( 37.40949999999997289, 4.898587196589414801E-16, -4.000000000000001776 ) ) ;
#90812=CARTESIAN_POINT ( 'NONE',  ( 37.40949999999997289, 0.000000000000000000, 0.000000000000000000 ) ) ;
#90829=ORIENTED_EDGE ( 'NONE', *, *, #41160, .T. ) ;
#90841=AXIS2_PLACEMENT_3D ( 'NONE', #15182, #73404, #22252 ) ;
#90846=VERTEX_POINT ( 'NONE', #106534 ) ;
#90855=DIRECTION ( 'NONE',  ( 0.5735764363510491570, -0.8191520442889895781, 1.003171929053522035E-16 ) ) ;
#90863=VERTEX_POINT ( 'NONE', #48817 ) ;
#90865=EDGE_CURVE ( 'NONE', #46183, #59988, #25825, .T. ) ;
#90868=ORIENTED_EDGE ( 'NONE', *, *, #91862, .F. ) ;
#90879=ORIENTED_EDGE ( 'NONE', *, *, #61439, .T. ) ;
#90904=B_SPLINE_CURVE_WITH_KNOTS ( 'NONE', 3,
 ( #86585, #36979, #94116, #15174, #61230, #31915 ),
 .UNSPECIFIED., .F., .F.,
 ( 4, 2, 4 ),
 ( 0.000000000000000000, 0.0003491763592121711088, 0.0006983527184243422175 ),
 .UNSPECIFIED. ) ;
#90939=ORIENTED_EDGE ( 'NONE', *, *, #49800, .F. ) ;
#90955=CARTESIAN_POINT ( 'NONE',  ( 0.000000000000000000, 4.898587196589413815E-16, -4.000000000000000888 ) ) ;
#90961=CARTESIAN_POINT ( 'NONE',  ( 24.83349330513380693, 1.593028355512270962E-15, 0.000000000000000000 ) ) ;
#90978=AXIS2_PLACEMENT_3D ( 'NONE', #57650, #35026, #59816 ) ;
#90992=ORIENTED_EDGE ( 'NONE', *, *, #72686, .T. ) ;
#91002=ORIENTED_EDGE ( 'NONE', *, *, #38471, .T. ) ;
#91048=FACE_OUTER_BOUND ( 'NONE', #6466, .T. ) ;
#91083=ORIENTED_EDGE ( 'NONE', *, *, #8935, .T. ) ;
#91155=EDGE_CURVE ( 'NONE', #93202, #35657, #19045, .T. ) ;
#91184=VECTOR ( 'NONE', #41946, 1000.000000000000000 ) ;
#91201=VERTEX_POINT ( 'NONE', #95160 ) ;
#91222=ORIENTED_EDGE ( 'NONE', *, *, #8848, .T. ) ;
#91224=CARTESIAN_POINT ( 'NONE',  ( 17.33349330513380693, 1.593028355512270962E-15, 0.000000000000000000 ) ) ;
#91234=AXIS2_PLACEMENT_3D ( 'NONE', #86151, #95816, #28455 ) ;
#91238=EDGE_LOOP ( 'NONE', ( #15644, #75148, #5561, #22538, #42738, #10573 ) ) ;
#91262=CYLINDRICAL_SURFACE ( 'NONE', #59286, 4.000000000000000888 ) ;
#91273=DIRECTION ( 'NONE',  ( -1.000000000000000000, -1.224606353822377258E-16, -0.000000000000000000 ) ) ;
#91290=EDGE_CURVE ( 'NONE', #9148, #38226, #60295, .T. ) ;
#91316=ADVANCED_FACE ( 'NONE', ( #6656 ), #57319, .T. ) ;
#91352=CARTESIAN_POINT ( 'NONE',  ( 6.683837171061803417, 3.955946848495959234, -6.851900933636991375 ) ) ;
#91381=CIRCLE ( 'NONE', #70734, 4.000000000000001776 ) ;
#91393=CARTESIAN_POINT ( 'NONE',  ( 21.08349330513380693, -4.000000000000000000, 4.898587196589415787E-16 ) ) ;
#91446=VERTEX_POINT ( 'NONE', #75639 ) ;
#91452=ORIENTED_EDGE ( 'NONE', *, *, #81171, .T. ) ;
#91454=DIRECTION ( 'NONE',  ( 0.5735764363510491570, -0.8191520442889895781, 1.003171929053522035E-16 ) ) ;
#91458=AXIS2_PLACEMENT_3D ( 'NONE', #59713, #25233, #18194 ) ;
#91489=CARTESIAN_POINT ( 'NONE',  ( 34.35000000000000142, 1.533819458162526451E-15, 0.000000000000000000 ) ) ;
#91495=CIRCLE ( 'NONE', #103496, 4.000000000000001776 ) ;
#91518=CARTESIAN_POINT ( 'NONE',  ( 6.683837171061802529, 3.955946848495962787, 6.851900933636986935 ) ) ;
#91536=FACE_OUTER_BOUND ( 'NONE', #69891, .T. ) ;
#91539=ADVANCED_FACE ( 'NONE', ( #57849 ), #87844, .T. ) ;
#91540=CARTESIAN_POINT ( 'NONE',  ( 6.445370176741902490, 4.584736124523943523, -5.738941594274561631 ) ) ;
#91597=CARTESIAN_POINT ( 'NONE',  ( 37.33349330513379982, 1.593028355512270962E-15, 0.000000000000000000 ) ) ;
#91605=DIRECTION ( 'NONE',  ( 0.5735764363510490460, 0.8191520442889896891, 0.000000000000000000 ) ) ;
#91644=LINE ( 'NONE', #49028, #12919 ) ;
#91659=EDGE_CURVE ( 'NONE', #45575, #56185, #91381, .T. ) ;
#91751=DIRECTION ( 'NONE',  ( 0.000000000000000000, 1.000000000000000000, 0.000000000000000000 ) ) ;
#91766=DIRECTION ( 'NONE',  ( 0.000000000000000000, -1.000000000000000000, 0.000000000000000000 ) ) ;
#91770=DIRECTION ( 'NONE',  ( 0.000000000000000000, 0.000000000000000000, 1.000000000000000000 ) ) ;
#91783=DIRECTION ( 'NONE',  ( 1.000000000000000000, 1.224606353822377258E-16, 0.000000000000000000 ) ) ;
#91829=VERTEX_POINT ( 'NONE', #104696 ) ;
#91840=CARTESIAN_POINT ( 'NONE',  ( 30.59999999999999787, 3.309500000000003439, 4.052968581778167743E-16 ) ) ;
#91854=CARTESIAN_POINT ( 'NONE',  ( 34.83349330513380693, -3.851859888774471706E-31, 4.000000000000001776 ) ) ;
#91862=EDGE_CURVE ( 'NONE', #36519, #40430, #7572, .T. ) ;
#91905=CARTESIAN_POINT ( 'NONE',  ( 0.2573354458087849794, -6.889406814520515177, 1.067197363239225538 ) ) ;
#91917=EDGE_CURVE ( 'NONE', #51593, #4237, #96534, .T. ) ;
#91926=CARTESIAN_POINT ( 'NONE',  ( 28.58349330513380337, 4.000000000000002665, 0.000000000000000000 ) ) ;
#91947=DIRECTION ( 'NONE',  ( 0.5735764363510491570, -0.8191520442889895781, 1.003171929053522035E-16 ) ) ;
#91951=DIRECTION ( 'NONE',  ( 0.000000000000000000, 0.000000000000000000, 1.000000000000000000 ) ) ;
#91969=DIRECTION ( 'NONE',  ( -0.000000000000000000, 0.000000000000000000, 1.000000000000000000 ) ) ;
#91978=EDGE_LOOP ( 'NONE', ( #50653, #40342, #67278, #72446 ) ) ;
#91979=DIRECTION ( 'NONE',  ( 0.5735764363510491570, -0.8191520442889895781, 1.003171929053522035E-16 ) ) ;
#92000=DIRECTION ( 'NONE',  ( -1.000000000000000000, -0.000000000000000000, -0.000000000000000000 ) ) ;
#92006=CARTESIAN_POINT ( 'NONE',  ( 6.562974947121711367, -4.277474787035888681, 6.282829635893496523 ) ) ;
#92040=AXIS2_PLACEMENT_3D ( 'NONE', #52156, #26347, #60289 ) ;
#92041=CARTESIAN_POINT ( 'NONE',  ( 8.099999999999999645, -3.752776749732574135, -6.500000000000001776 ) ) ;
#92053=CARTESIAN_POINT ( 'NONE',  ( 6.692588830498425345, 3.932766476276028822, -6.892929031562515796 ) ) ;
#92055=ORIENTED_EDGE ( 'NONE', *, *, #72468, .F. ) ;
#92077=AXIS2_PLACEMENT_3D ( 'NONE', #39614, #72487, #63363 ) ;
#92082=VERTEX_POINT ( 'NONE', #85204 ) ;
#92091=PLANE ( 'NONE',  #106633 ) ;
#92134=DIRECTION ( 'NONE',  ( 0.000000000000000000, -1.000000000000000000, 0.000000000000000000 ) ) ;
#92151=ORIENTED_EDGE ( 'NONE', *, *, #5206, .T. ) ;
#92156=DIRECTION ( 'NONE',  ( 0.5735764363510491570, -0.8191520442889895781, 1.003171929053522035E-16 ) ) ;
#92182=EDGE_CURVE ( 'NONE', #40203, #60770, #12365, .T. ) ;
#92194=CARTESIAN_POINT ( 'NONE',  ( 7.500000000000001776, 0.000000000000000000, 0.000000000000000000 ) ) ;
#92196=CYLINDRICAL_SURFACE ( 'NONE', #86614, 4.000000000000000888 ) ;
#92199=EDGE_CURVE ( 'NONE', #3128, #65549, #20827, .T. ) ;
#92212=CONICAL_SURFACE ( 'NONE', #23356, 3.309500000000001663, 0.9599310885968770357 ) ;
#92215=ORIENTED_EDGE ( 'NONE', *, *, #70856, .T. ) ;
#92217=CONICAL_SURFACE ( 'NONE', #105999, 3.309500000000001663, 0.9599310885968770357 ) ;
#92230=ADVANCED_FACE ( 'NONE', ( #52294 ), #45346, .F. ) ;
#92246=CARTESIAN_POINT ( 'NONE',  ( 0.4037800551813745531, 7.199367570657607018, 0.5303295852573142177 ) ) ;
#92249=CARTESIAN_POINT ( 'NONE',  ( 0.000000000000000000, 0.000000000000000000, 0.000000000000000000 ) ) ;
#92281=AXIS2_PLACEMENT_3D ( 'NONE', #82377, #8485, #33323 ) ;
#92309=CARTESIAN_POINT ( 'NONE',  ( 14.83349330513380693, 1.593028355512270962E-15, 0.000000000000000000 ) ) ;
#92323=ADVANCED_FACE ( 'NONE', ( #43470 ), #24336, .T. ) ;
#92337=CARTESIAN_POINT ( 'NONE',  ( 5.947762761376480078, -6.880090707843049991, -1.083333333333332593 ) ) ;
#92357=ORIENTED_EDGE ( 'NONE', *, *, #4714, .T. ) ;
#92386=DIRECTION ( 'NONE',  ( 0.000000000000000000, 0.000000000000000000, 1.000000000000000000 ) ) ;
#92400=PLANE ( 'NONE',  #85591 ) ;
#92431=CARTESIAN_POINT ( 'NONE',  ( 23.09999999999999432, 1.533819458162526451E-15, 0.000000000000000000 ) ) ;
#92433=CARTESIAN_POINT ( 'NONE',  ( 33.09999999999999432, 1.533819458162526451E-15, 0.000000000000000000 ) ) ;
#92442=AXIS2_PLACEMENT_3D ( 'NONE', #72858, #97143, #55085 ) ;
#92449=FACE_OUTER_BOUND ( 'NONE', #18006, .T. ) ;
#92466=EDGE_CURVE ( 'NONE', #43607, #72268, #26061, .T. ) ;
#92470=ORIENTED_EDGE ( 'NONE', *, *, #19874, .F. ) ;
#92477=LINE ( 'NONE', #17554, #62339 ) ;
#92518=AXIS2_PLACEMENT_3D ( 'NONE', #66793, #48985, #72735 ) ;
#92531=AXIS2_PLACEMENT_3D ( 'NONE', #49913, #18108, #74713 ) ;
#92581=CARTESIAN_POINT ( 'NONE',  ( 29.34999999999999787, 1.533819458162526451E-15, 0.000000000000000000 ) ) ;
#92624=FACE_OUTER_BOUND ( 'NONE', #35416, .T. ) ;
#92667=FACE_OUTER_BOUND ( 'NONE', #37703, .T. ) ;
#92696=LINE ( 'NONE', #85141, #75111 ) ;
#92734=CARTESIAN_POINT ( 'NONE',  ( 9.833493305133805151, 4.000000000000003553, 0.000000000000000000 ) ) ;
#92740=AXIS2_PLACEMENT_3D ( 'NONE', #93973, #19596, #68649 ) ;
#92745=DIRECTION ( 'NONE',  ( -1.000000000000000000, -1.224606353822377258E-16, -0.000000000000000000 ) ) ;
#92769=ORIENTED_EDGE ( 'NONE', *, *, #62163, .F. ) ;
#92771=DIRECTION ( 'NONE',  ( -1.000000000000000000, -1.224606353822377258E-16, -0.000000000000000000 ) ) ;
#92773=VERTEX_POINT ( 'NONE', #51418 ) ;
#92776=CARTESIAN_POINT ( 'NONE',  ( 34.35000000000000142, 3.309500000000003439, 4.052968581778167743E-16 ) ) ;
#92789=ORIENTED_EDGE ( 'NONE', *, *, #41690, .T. ) ;
#92794=ORIENTED_EDGE ( 'NONE', *, *, #82546, .T. ) ;
#92799=FACE_OUTER_BOUND ( 'NONE', #12056, .T. ) ;
#92834=DIRECTION ( 'NONE',  ( -1.000000000000000000, -1.224606353822377258E-16, -0.000000000000000000 ) ) ;
#92843=CARTESIAN_POINT ( 'NONE',  ( 0.000000000000000000, 4.898587196589413815E-16, -4.000000000000000888 ) ) ;
#92847=EDGE_LOOP ( 'NONE', ( #73019, #25258, #83945, #29567, #100669 ) ) ;
#92848=EDGE_CURVE ( 'NONE', #38206, #42880, #34730, .T. ) ;
#92856=LINE ( 'NONE', #101495, #43372 ) ;
#92878=CARTESIAN_POINT ( 'NONE',  ( 16.84999999999999787, -3.309499999999999886, 0.000000000000000000 ) ) ;
#92891=ORIENTED_EDGE ( 'NONE', *, *, #9553, .F. ) ;
#92917=AXIS2_PLACEMENT_3D ( 'NONE', #20837, #103809, #61795 ) ;
#92976=FACE_OUTER_BOUND ( 'NONE', #55477, .T. ) ;
#92980=CARTESIAN_POINT ( 'NONE',  ( 10.59999999999999609, 1.533819458162526451E-15, 0.000000000000000000 ) ) ;
#92981=ORIENTED_EDGE ( 'NONE', *, *, #73938, .F. ) ;
#92992=AXIS2_PLACEMENT_3D ( 'NONE', #23403, #90238, #56247 ) ;
#93007=DIRECTION ( 'NONE',  ( 0.000000000000000000, 0.8660254037844381525, -0.5000000000000009992 ) ) ;
#93036=VECTOR ( 'NONE', #45806, 1000.000000000000000 ) ;
#93073=DIRECTION ( 'NONE',  ( -1.000000000000000000, -1.224606353822377258E-16, -0.000000000000000000 ) ) ;
#93097=EDGE_LOOP ( 'NONE', ( #67472, #79539, #38261, #63368, #5613 ) ) ;
#93115=AXIS2_PLACEMENT_3D ( 'NONE', #98198, #40501, #73378 ) ;
#93120=CARTESIAN_POINT ( 'NONE',  ( 0.000000000000000000, 0.000000000000000000, 0.000000000000000000 ) ) ;
#93143=ORIENTED_EDGE ( 'NONE', *, *, #73491, .F. ) ;
#93151=DIRECTION ( 'NONE',  ( -0.5735764363510494901, -0.8191520442889894671, 0.000000000000000000 ) ) ;
#93163=EDGE_CURVE ( 'NONE', #66061, #36374, #48458, .T. ) ;
#93202=VERTEX_POINT ( 'NONE', #90568 ) ;
#93209=DIRECTION ( 'NONE',  ( -1.000000000000000000, -0.000000000000000000, -0.000000000000000000 ) ) ;
#93219=CARTESIAN_POINT ( 'NONE',  ( 16.08349330513380337, -4.000000000000000888, 4.898587196589416773E-16 ) ) ;
#93222=ORIENTED_EDGE ( 'NONE', *, *, #45792, .F. ) ;
#93270=CARTESIAN_POINT ( 'NONE',  ( 27.61650669486618881, 4.898587196589413815E-16, -4.000000000000000888 ) ) ;
#93282=EDGE_CURVE ( 'NONE', #35207, #9118, #24422, .T. ) ;
#93323=FACE_OUTER_BOUND ( 'NONE', #84029, .T. ) ;
#93324=CARTESIAN_POINT ( 'NONE',  ( 13.58349330513380515, 1.593028355512270962E-15, 0.000000000000000000 ) ) ;
#93340=CARTESIAN_POINT ( 'NONE',  ( 36.84999999999999432, 1.533819458162526451E-15, 0.000000000000000000 ) ) ;
#93357=VERTEX_POINT ( 'NONE', #33416 ) ;
#93405=DIRECTION ( 'NONE',  ( 0.000000000000000000, -1.000000000000000000, 0.000000000000000000 ) ) ;
#93437=CARTESIAN_POINT ( 'NONE',  ( 6.683837171061806082, -3.955946848495971668, -6.851900933636991375 ) ) ;
#93440=DIRECTION ( 'NONE',  ( -1.000000000000000000, -1.224606353822377258E-16, -0.000000000000000000 ) ) ;
#93491=CARTESIAN_POINT ( 'NONE',  ( 34.83349330513380693, 1.593028355512270962E-15, 0.000000000000000000 ) ) ;
#93507=EDGE_CURVE ( 'NONE', #27343, #91446, #76113, .T. ) ;
#93535=FACE_OUTER_BOUND ( 'NONE', #56838, .T. ) ;
#93544=EDGE_CURVE ( 'NONE', #2998, #64476, #88201, .T. ) ;
#93557=EDGE_CURVE ( 'NONE', #32543, #52389, #41530, .T. ) ;
#93565=AXIS2_PLACEMENT_3D ( 'NONE', #104486, #16544, #56988 ) ;
#93596=ADVANCED_FACE ( 'NONE', ( #57928 ), #86463, .T. ) ;
#93666=VERTEX_POINT ( 'NONE', #106478 ) ;
#93688=VECTOR ( 'NONE', #55178, 1000.000000000000341 ) ;
#93757=EDGE_LOOP ( 'NONE', ( #19930, #4218, #67211, #87372, #14298 ) ) ;
#93772=CARTESIAN_POINT ( 'NONE',  ( 25.59999999999999787, 1.533819458162526451E-15, 0.000000000000000000 ) ) ;
#93800=ORIENTED_EDGE ( 'NONE', *, *, #100170, .F. ) ;
#93815=DIRECTION ( 'NONE',  ( 0.000000000000000000, -1.000000000000000000, 0.000000000000000000 ) ) ;
#93869=ORIENTED_EDGE ( 'NONE', *, *, #86675, .T. ) ;
#93870=CARTESIAN_POINT ( 'NONE',  ( 6.289692432696785573, -1.240526984323783911E-13, -6.828989928337169779 ) ) ;
#93880=ORIENTED_EDGE ( 'NONE', *, *, #20790, .F. ) ;
#93886=ADVANCED_FACE ( 'NONE', ( #30382 ), #50311, .T. ) ;
#93901=CARTESIAN_POINT ( 'NONE',  ( 13.58349330513380515, -3.851859888774471706E-31, 4.000000000000001776 ) ) ;
#93926=CONICAL_SURFACE ( 'NONE', #78434, 6.500000000000000000, 1.047197551196600296 ) ;
#93939=LINE ( 'NONE', #103613, #69035 ) ;
#93941=CARTESIAN_POINT ( 'NONE',  ( 6.281178480976146616, -3.752776749732560813, 6.500000000000004441 ) ) ;
#93973=CARTESIAN_POINT ( 'NONE',  ( 19.83349330513380693, 1.593028355512270962E-15, 0.000000000000000000 ) ) ;
#93994=FACE_OUTER_BOUND ( 'NONE', #80608, .T. ) ;
#94029=ORIENTED_EDGE ( 'NONE', *, *, #24415, .F. ) ;
#94044=ADVANCED_FACE ( 'NONE', ( #23894 ), #90722, .T. ) ;
#94081=CARTESIAN_POINT ( 'NONE',  ( 36.84999999999999432, 3.309500000000003439, 0.000000000000000000 ) ) ;
#94082=VECTOR ( 'NONE', #39906, 1000.000000000000341 ) ;
#94109=AXIS2_PLACEMENT_3D ( 'NONE', #101168, #27330, #60208 ) ;
#94116=CARTESIAN_POINT ( 'NONE',  ( 6.394343112843832166, 3.776352960569632877, 6.540835195019754522 ) ) ;
#94117=CARTESIAN_POINT ( 'NONE',  ( 36.08349330513379982, -3.851859888774471706E-31, 4.000000000000001776 ) ) ;
#94118=ORIENTED_EDGE ( 'NONE', *, *, #15713, .F. ) ;
#94121=CARTESIAN_POINT ( 'NONE',  ( 26.08349330513380693, 4.000000000000002665, 0.000000000000000000 ) ) ;
#94131=VERTEX_POINT ( 'NONE', #58348 ) ;
#94182=CIRCLE ( 'NONE', #33911, 4.000000000000000888 ) ;
#94194=ORIENTED_EDGE ( 'NONE', *, *, #38891, .F. ) ;
#94198=CARTESIAN_POINT ( 'NONE',  ( 36.08349330513379982, 4.898587196589411843E-16, -4.000000000000001776 ) ) ;
#94235=AXIS2_PLACEMENT_3D ( 'NONE', #36587, #4178, #86183 ) ;
#94244=DIRECTION ( 'NONE',  ( -1.000000000000000000, -1.224606353822377258E-16, -0.000000000000000000 ) ) ;
#94261=CARTESIAN_POINT ( 'NONE',  ( 24.83349330513380693, -4.000000000000000888, 4.898587196589416773E-16 ) ) ;
#94277=EDGE_CURVE ( 'NONE', #25041, #82621, #8965, .T. ) ;
#94299=ORIENTED_EDGE ( 'NONE', *, *, #6506, .F. ) ;
#94320=CARTESIAN_POINT ( 'NONE',  ( 26.84999999999999787, 3.309500000000003439, 0.000000000000000000 ) ) ;
#94334=AXIS2_PLACEMENT_3D ( 'NONE', #78098, #4215, #61944 ) ;
#94355=CYLINDRICAL_SURFACE ( 'NONE', #33173, 4.000000000000000888 ) ;
#94380=VERTEX_POINT ( 'NONE', #77483 ) ;
#94390=CARTESIAN_POINT ( 'NONE',  ( -3.321851460894552355E-15, 5.469921996229796690, -3.525817189091414949 ) ) ;
#94433=VERTEX_POINT ( 'NONE', #94198 ) ;
#94456=ORIENTED_EDGE ( 'NONE', *, *, #83081, .T. ) ;
#94462=DIRECTION ( 'NONE',  ( 0.000000000000000000, 0.000000000000000000, 1.000000000000000000 ) ) ;
#94473=DIRECTION ( 'NONE',  ( -1.000000000000000000, -1.224606353822377258E-16, -0.000000000000000000 ) ) ;
#94502=CARTESIAN_POINT ( 'NONE',  ( 18.86650669486618881, 1.474610560812782335E-15, 0.000000000000000000 ) ) ;
#94616=EDGE_LOOP ( 'NONE', ( #87915, #2088, #63777, #73861, #89000 ) ) ;
#94630=EDGE_CURVE ( 'NONE', #57770, #11179, #53467, .T. ) ;
#94632=SURFACE_STYLE_FILL_AREA ( #61190 ) ;
#94695=VERTEX_POINT ( 'NONE', #80909 ) ;
#94697=CARTESIAN_POINT ( 'NONE',  ( 24.83349330513380693, 1.593028355512270962E-15, 0.000000000000000000 ) ) ;
#94722=CARTESIAN_POINT ( 'NONE',  ( 0.06682554136338200723, -6.264794173742283867, -2.149058192116893196 ) ) ;
#94741=CIRCLE ( 'NONE', #8536, 3.309500000000001663 ) ;
#94744=ORIENTED_EDGE ( 'NONE', *, *, #81838, .F. ) ;
#94755=DIRECTION ( 'NONE',  ( 1.000000000000000000, 1.224606353822377258E-16, 0.000000000000000000 ) ) ;
#94759=ORIENTED_EDGE ( 'NONE', *, *, #55753, .T. ) ;
#94800=AXIS2_PLACEMENT_3D ( 'NONE', #10568, #50484, #83397 ) ;
#94819=VERTEX_POINT ( 'NONE', #40989 ) ;
#94850=ADVANCED_FACE ( 'NONE', ( #102420 ), #57389, .T. ) ;
#94873=ORIENTED_EDGE ( 'NONE', *, *, #54122, .F. ) ;
#94899=VECTOR ( 'NONE', #74974, 1000.000000000000000 ) ;
#94917=ORIENTED_EDGE ( 'NONE', *, *, #41698, .T. ) ;
#94924=DIRECTION ( 'NONE',  ( 0.000000000000000000, -1.000000000000000000, 0.000000000000000000 ) ) ;
#94982=ORIENTED_EDGE ( 'NONE', *, *, #44856, .F. ) ;
#94989=EDGE_LOOP ( 'NONE', ( #6599, #83821, #1370, #55077, #50998 ) ) ;
#95001=ORIENTED_EDGE ( 'NONE', *, *, #85532, .T. ) ;
#95017=CARTESIAN_POINT ( 'NONE',  ( 6.394343112843833055, -3.776352960569632433, 6.540835195019756299 ) ) ;
#95035=CARTESIAN_POINT ( 'NONE',  ( 33.09999999999999432, 1.533819458162526451E-15, 0.000000000000000000 ) ) ;
#95041=EDGE_LOOP ( 'NONE', ( #24355, #9843, #42127, #47200, #48344, #87397 ) ) ;
#95053=VECTOR ( 'NONE', #74097, 1000.000000000000000 ) ;
#95066=DIRECTION ( 'NONE',  ( -1.000000000000000000, -1.224606353822377258E-16, -0.000000000000000000 ) ) ;
#95085=ORIENTED_EDGE ( 'NONE', *, *, #81492, .T. ) ;
#95090=ORIENTED_EDGE ( 'NONE', *, *, #29825, .F. ) ;
#95093=DIRECTION ( 'NONE',  ( 0.000000000000000000, -1.000000000000000000, 0.000000000000000000 ) ) ;
#95098=FACE_OUTER_BOUND ( 'NONE', #57614, .T. ) ;
#95104=DIRECTION ( 'NONE',  ( -0.5735764363510494901, -0.8191520442889894671, 0.000000000000000000 ) ) ;
#95130=ORIENTED_EDGE ( 'NONE', *, *, #102050, .T. ) ;
#95160=CARTESIAN_POINT ( 'NONE',  ( 36.08349330513379982, -4.000000000000000888, 4.898587196589416773E-16 ) ) ;
#95183=CIRCLE ( 'NONE', #98613, 4.000000000000001776 ) ;
#95184=DIRECTION ( 'NONE',  ( 0.000000000000000000, -1.000000000000000000, 0.000000000000000000 ) ) ;
#95225=CARTESIAN_POINT ( 'NONE',  ( 17.33349330513380693, -4.000000000000000000, 4.898587196589415787E-16 ) ) ;
#95281=CARTESIAN_POINT ( 'NONE',  ( 23.58349330513380337, -4.000000000000000000, 4.898587196589415787E-16 ) ) ;
#95291=CARTESIAN_POINT ( 'NONE',  ( 17.61650669486618881, 4.898587196589413815E-16, -4.000000000000000888 ) ) ;
#95299=EDGE_CURVE ( 'NONE', #77629, #34409, #104809, .T. ) ;
#95317=CARTESIAN_POINT ( 'NONE',  ( 0.5805565836007650082, -3.752776749732574135, -6.500000000000001776 ) ) ;
#95326=ORIENTED_EDGE ( 'NONE', *, *, #95372, .F. ) ;
#95355=ORIENTED_EDGE ( 'NONE', *, *, #17216, .F. ) ;
#95372=EDGE_CURVE ( 'NONE', #29177, #100701, #81559, .T. ) ;
#95443=CARTESIAN_POINT ( 'NONE',  ( 21.36650669486618881, 1.474610560812782335E-15, 0.000000000000000000 ) ) ;
#95460=CARTESIAN_POINT ( 'NONE',  ( 31.36650669486618881, 1.474610560812782335E-15, 0.000000000000000000 ) ) ;
#95493=EDGE_CURVE ( 'NONE', #3065, #8034, #38561, .T. ) ;
#95518=CARTESIAN_POINT ( 'NONE',  ( 38.09999999999998721, 0.000000000000000000, 0.000000000000000000 ) ) ;
#95532=DIRECTION ( 'NONE',  ( 0.000000000000000000, -1.000000000000000000, 0.000000000000000000 ) ) ;
#95538=EDGE_LOOP ( 'NONE', ( #15993, #32509, #59525, #103972, #100687 ) ) ;
#95572=CARTESIAN_POINT ( 'NONE',  ( 18.86650669486618881, 4.000000000000003553, 4.898587196589414801E-16 ) ) ;
#95624=ORIENTED_EDGE ( 'NONE', *, *, #77037, .T. ) ;
#95626=FACE_OUTER_BOUND ( 'NONE', #8001, .T. ) ;
#95638=CARTESIAN_POINT ( 'NONE',  ( 0.5805565836007616776, 3.752776749732562589, -6.500000000000000888 ) ) ;
#95644=ADVANCED_FACE ( 'NONE', ( #29766 ), #79874, .T. ) ;
#95670=ORIENTED_EDGE ( 'NONE', *, *, #18487, .F. ) ;
#95673=EDGE_CURVE ( 'NONE', #17049, #7599, #41997, .T. ) ;
#95681=AXIS2_PLACEMENT_3D ( 'NONE', #81591, #40104, #96754 ) ;
#95720=ORIENTED_EDGE ( 'NONE', *, *, #89709, .F. ) ;
#95746=CARTESIAN_POINT ( 'NONE',  ( 0.000000000000000000, 0.000000000000000000, 0.000000000000000000 ) ) ;
#95771=EDGE_CURVE ( 'NONE', #8828, #40203, #7555, .T. ) ;
#95775=ORIENTED_EDGE ( 'NONE', *, *, #95493, .T. ) ;
#95785=CARTESIAN_POINT ( 'NONE',  ( 0.5805565836007616776, 3.752776749732562589, -6.500000000000000888 ) ) ;
#95816=DIRECTION ( 'NONE',  ( 0.000000000000000000, -1.000000000000000000, 0.000000000000000000 ) ) ;
#95834=EDGE_CURVE ( 'NONE', #83001, #90863, #58918, .T. ) ;
#95876=DIRECTION ( 'NONE',  ( 0.000000000000000000, -1.000000000000000000, 0.000000000000000000 ) ) ;
#95907=ADVANCED_FACE ( 'NONE', ( #101893 ), #92196, .T. ) ;
#95911=DIRECTION ( 'NONE',  ( 0.000000000000000000, -1.000000000000000000, 0.000000000000000000 ) ) ;
#95935=ADVANCED_FACE ( 'NONE', ( #35607 ), #94355, .T. ) ;
#95939=VECTOR ( 'NONE', #23722, 1000.000000000000341 ) ;
#95940=ORIENTED_EDGE ( 'NONE', *, *, #73180, .F. ) ;
#95974=CIRCLE ( 'NONE', #89294, 4.000000000000001776 ) ;
#95975=CARTESIAN_POINT ( 'NONE',  ( 6.585468679846623985, 7.640532685286893333, -0.2337908078075575935 ) ) ;
#95984=DIRECTION ( 'NONE',  ( -1.000000000000000000, -0.000000000000000000, -0.000000000000000000 ) ) ;
#96057=DIRECTION ( 'NONE',  ( -1.000000000000000000, -0.000000000000000000, -0.000000000000000000 ) ) ;
#96094=ORIENTED_EDGE ( 'NONE', *, *, #29745, .T. ) ;
#96106=CARTESIAN_POINT ( 'NONE',  ( 6.562874270078295602, 3.301808241302743863, 6.845811579416823278 ) ) ;
#96162=CIRCLE ( 'NONE', #20451, 4.000000000000001776 ) ;
#96173=CIRCLE ( 'NONE', #49638, 4.000000000000000888 ) ;
#96201=VERTEX_POINT ( 'NONE', #1323 ) ;
#96247=ADVANCED_FACE ( 'NONE', ( #83327 ), #64194, .T. ) ;
#96271=CARTESIAN_POINT ( 'NONE',  ( 21.36650669486618881, 1.474610560812782335E-15, 0.000000000000000000 ) ) ;
#96277=DIRECTION ( 'NONE',  ( -1.000000000000000000, -1.224606353822377258E-16, -0.000000000000000000 ) ) ;
#96282=AXIS2_PLACEMENT_3D ( 'NONE', #95460, #69079, #20580 ) ;
#96284=ORIENTED_EDGE ( 'NONE', *, *, #46803, .T. ) ;
#96297=DIRECTION ( 'NONE',  ( 0.000000000000000000, 1.000000000000000000, 0.000000000000000000 ) ) ;
#96329=ORIENTED_EDGE ( 'NONE', *, *, #105947, .F. ) ;
#96360=DIRECTION ( 'NONE',  ( -1.000000000000000000, -1.224606353822377258E-16, -0.000000000000000000 ) ) ;
#96395=DIRECTION ( 'NONE',  ( 0.000000000000000000, 1.000000000000000000, 0.000000000000000000 ) ) ;
#96401=VERTEX_POINT ( 'NONE', #34563 ) ;
#96420=ADVANCED_FACE ( 'NONE', ( #88647 ), #26418, .T. ) ;
#96439=ORIENTED_EDGE ( 'NONE', *, *, #36645, .T. ) ;
#96449=DIRECTION ( 'NONE',  ( 0.000000000000000000, 0.000000000000000000, 1.000000000000000000 ) ) ;
#96462=DIRECTION ( 'NONE',  ( -1.000000000000000000, -0.000000000000000000, -0.000000000000000000 ) ) ;
#96493=AXIS2_PLACEMENT_3D ( 'NONE', #44583, #68865, #26308 ) ;
#96509=CARTESIAN_POINT ( 'NONE',  ( 5.975663821520835306, 7.000939006314205848, 0.8740179403730332641 ) ) ;
#96534=CIRCLE ( 'NONE', #75894, 4.000000000000001776 ) ;
#96540=VERTEX_POINT ( 'NONE', #87338 ) ;
#96556=DIRECTION ( 'NONE',  ( 0.000000000000000000, -1.000000000000000000, 0.000000000000000000 ) ) ;
#96559=EDGE_LOOP ( 'NONE', ( #30199, #18182, #82883, #21995, #46797, #96439, #90006 ) ) ;
#96592=EDGE_CURVE ( 'NONE', #77164, #100664, #38485, .T. ) ;
#96624=VERTEX_POINT ( 'NONE', #34441 ) ;
#96629=DIRECTION ( 'NONE',  ( 0.000000000000000000, -1.000000000000000000, 0.000000000000000000 ) ) ;
#96682=DIRECTION ( 'NONE',  ( 0.000000000000000000, -1.000000000000000000, 0.000000000000000000 ) ) ;
#96684=AXIS2_PLACEMENT_3D ( 'NONE', #103175, #87525, #95093 ) ;
#96692=DIRECTION ( 'NONE',  ( 0.000000000000000000, -1.000000000000000000, 0.000000000000000000 ) ) ;
#96695=DIRECTION ( 'NONE',  ( 0.000000000000000000, -1.000000000000000000, 0.000000000000000000 ) ) ;
#96735=CARTESIAN_POINT ( 'NONE',  ( 6.683837171061806970, -7.911893696991936231, 5.688671339918660213E-17 ) ) ;
#96752=ORIENTED_EDGE ( 'NONE', *, *, #50152, .T. ) ;
#96754=DIRECTION ( 'NONE',  ( 0.000000000000000000, -1.000000000000000000, 0.000000000000000000 ) ) ;
#96762=CARTESIAN_POINT ( 'NONE',  ( 7.500000000000001776, 1.028703311283776783E-15, -8.400000000000000355 ) ) ;
#96783=FACE_OUTER_BOUND ( 'NONE', #33939, .T. ) ;
#96839=ORIENTED_EDGE ( 'NONE', *, *, #86640, .F. ) ;
#96914=EDGE_CURVE ( 'NONE', #72376, #77950, #19489, .T. ) ;
#96980=MECHANICAL_DESIGN_GEOMETRIC_PRESENTATION_REPRESENTATION('',(#102134),#62569);
#97010=EDGE_LOOP ( 'NONE', ( #8703, #19593, #31654, #61036, #23277 ) ) ;
#97021=LINE ( 'NONE', #63622, #27048 ) ;
#97028=FACE_OUTER_BOUND ( 'NONE', #24400, .T. ) ;
#97083=CARTESIAN_POINT ( 'NONE',  ( 11.08349330513380515, 1.593028355512270962E-15, 0.000000000000000000 ) ) ;
#97143=DIRECTION ( 'NONE',  ( -1.000000000000000000, -1.224606353822377258E-16, -0.000000000000000000 ) ) ;
#97177=DIRECTION ( 'NONE',  ( 0.000000000000000000, -1.000000000000000000, 0.000000000000000000 ) ) ;
#97201=CARTESIAN_POINT ( 'NONE',  ( 6.585468679846620432, -3.617797563910811753, 6.733790807807554124 ) ) ;
#97207=CARTESIAN_POINT ( 'NONE',  ( 5.996380728651201863, 2.731133088746455329, 6.499999999999997335 ) ) ;
#97228=EDGE_CURVE ( 'NONE', #25041, #38206, #50384, .T. ) ;
#97248=ADVANCED_FACE ( 'NONE', ( #93535 ), #62248, .T. ) ;
#97260=DIRECTION ( 'NONE',  ( -1.000000000000000000, -0.000000000000000000, -0.000000000000000000 ) ) ;
#97268=CARTESIAN_POINT ( 'NONE',  ( 8.099999999999999645, 3.752776749732562589, -6.500000000000000888 ) ) ;
#97303=CARTESIAN_POINT ( 'NONE',  ( 23.58349330513380337, 1.593028355512270962E-15, 0.000000000000000000 ) ) ;
#97311=EDGE_CURVE ( 'NONE', #83001, #25099, #3300, .T. ) ;
#97355=VERTEX_POINT ( 'NONE', #13113 ) ;
#97361=CARTESIAN_POINT ( 'NONE',  ( 6.936184427528457874, 0.000000000000000000, -8.605212085995399107 ) ) ;
#97374=CIRCLE ( 'NONE', #6073, 4.000000000000000888 ) ;
#97404=EDGE_CURVE ( 'NONE', #93202, #80922, #36916, .T. ) ;
#97452=AXIS2_PLACEMENT_3D ( 'NONE', #9869, #83761, #100482 ) ;
#97472=EDGE_CURVE ( 'NONE', #42880, #17716, #26483, .T. ) ;
#97475=DIRECTION ( 'NONE',  ( 0.000000000000000000, -1.000000000000000000, 0.000000000000000000 ) ) ;
#97510=CARTESIAN_POINT ( 'NONE',  ( 0.000000000000000000, 5.629165124598848102, 3.250000000000005329 ) ) ;
#97604=AXIS2_PLACEMENT_3D ( 'NONE', #3272, #35672, #91751 ) ;
#97624=DIRECTION ( 'NONE',  ( -1.000000000000000000, -1.224606353822377258E-16, -0.000000000000000000 ) ) ;
#97648=CIRCLE ( 'NONE', #47688, 4.000000000000001776 ) ;
#97681=ORIENTED_EDGE ( 'NONE', *, *, #87583, .F. ) ;
#97690=CARTESIAN_POINT ( 'NONE',  ( 27.61650669486618881, 1.474610560812782335E-15, 0.000000000000000000 ) ) ;
#97724=EDGE_CURVE ( 'NONE', #45785, #52343, #11031, .T. ) ;
#97739=DIRECTION ( 'NONE',  ( 0.000000000000000000, 1.000000000000000000, 0.000000000000000000 ) ) ;
#97771=CARTESIAN_POINT ( 'NONE',  ( 6.326592304916279552, -6.579439845142160515, -2.267162479624770022 ) ) ;
#97817=ADVANCED_FACE ( 'NONE', ( #37063 ), #78177, .T. ) ;
#97824=DIRECTION ( 'NONE',  ( 0.000000000000000000, -1.000000000000000000, 0.000000000000000000 ) ) ;
#97829=AXIS2_PLACEMENT_3D ( 'NONE', #284, #74206, #84448 ) ;
#97830=CARTESIAN_POINT ( 'NONE',  ( 6.289572920342627604, 6.243622107253692377, -2.843693100100564308 ) ) ;
#97863=B_SPLINE_CURVE_WITH_KNOTS ( 'NONE', 3,
 ( #105403, #56289, #63374, #46119, #13724, #14785 ),
 .UNSPECIFIED., .F., .F.,
 ( 4, 2, 4 ),
 ( 2.380733003144472638E-07, 0.001898835937927383305, 0.003797433802554452380 ),
 .UNSPECIFIED. ) ;
#97870=LINE ( 'NONE', #74116, #13859 ) ;
#97873=ORIENTED_EDGE ( 'NONE', *, *, #10028, .F. ) ;
#97883=ORIENTED_EDGE ( 'NONE', *, *, #44250, .T. ) ;
#97966=DIRECTION ( 'NONE',  ( 1.000000000000000000, 1.224606353822377258E-16, 0.000000000000000000 ) ) ;
#97987=AXIS2_PLACEMENT_3D ( 'NONE', #88365, #82379, #8487 ) ;
#98021=ORIENTED_EDGE ( 'NONE', *, *, #102050, .F. ) ;
#98032=DIRECTION ( 'NONE',  ( -1.000000000000000000, -0.000000000000000000, -0.000000000000000000 ) ) ;
#98074=CARTESIAN_POINT ( 'NONE',  ( 34.83349330513380693, -4.000000000000000888, 4.898587196589416773E-16 ) ) ;
#98079=VERTEX_POINT ( 'NONE', #9816 ) ;
#98081=EDGE_CURVE ( 'NONE', #7161, #39006, #17942, .T. ) ;
#98116=ORIENTED_EDGE ( 'NONE', *, *, #26587, .F. ) ;
#98128=CARTESIAN_POINT ( 'NONE',  ( 6.683837171061802529, 3.955946848495962787, 6.851900933636986935 ) ) ;
#98171=LINE ( 'NONE', #24325, #89497 ) ;
#98193=EDGE_LOOP ( 'NONE', ( #54987, #18584, #85114, #36836, #94456 ) ) ;
#98198=CARTESIAN_POINT ( 'NONE',  ( 26.36650669486618881, 1.474610560812782335E-15, 0.000000000000000000 ) ) ;
#98202=DIRECTION ( 'NONE',  ( 0.000000000000000000, 0.000000000000000000, 1.000000000000000000 ) ) ;
#98221=VERTEX_POINT ( 'NONE', #20647 ) ;
#98254=VECTOR ( 'NONE', #77474, 1000.000000000000227 ) ;
#98278=CARTESIAN_POINT ( 'NONE',  ( 6.585304040558099814, -4.021874164301465271, 6.499999999999999112 ) ) ;
#98293=DIRECTION ( 'NONE',  ( -1.000000000000000000, -1.224606353822377258E-16, -0.000000000000000000 ) ) ;
#98322=FACE_OUTER_BOUND ( 'NONE', #2468, .T. ) ;
#98324=ORIENTED_EDGE ( 'NONE', *, *, #91659, .T. ) ;
#98336=DIRECTION ( 'NONE',  ( -1.000000000000000000, -1.224606353822377258E-16, -0.000000000000000000 ) ) ;
#98362=VERTEX_POINT ( 'NONE', #47498 ) ;
#98375=DIRECTION ( 'NONE',  ( 0.000000000000000000, -1.000000000000000000, 0.000000000000000000 ) ) ;
#98496=LINE ( 'NONE', #33800, #81022 ) ;
#98527=ORIENTED_EDGE ( 'NONE', *, *, #15775, .T. ) ;
#98564=CARTESIAN_POINT ( 'NONE',  ( 33.86650669486618881, 1.474610560812782335E-15, 0.000000000000000000 ) ) ;
#98570=EDGE_CURVE ( 'NONE', #16221, #36441, #59414, .T. ) ;
#98613=AXIS2_PLACEMENT_3D ( 'NONE', #17476, #694, #33659 ) ;
#98614=DIRECTION ( 'NONE',  ( 0.000000000000000000, -1.000000000000000000, 0.000000000000000000 ) ) ;
#98662=VERTEX_POINT ( 'NONE', #78672 ) ;
#98671=ORIENTED_EDGE ( 'NONE', *, *, #8848, .F. ) ;
#98674=EDGE_CURVE ( 'NONE', #23216, #70045, #25003, .T. ) ;
#98690=VERTEX_POINT ( 'NONE', #78153 ) ;
#98691=AXIS2_PLACEMENT_3D ( 'NONE', #25977, #2159, #76589 ) ;
#98695=DIRECTION ( 'NONE',  ( 0.000000000000000000, -1.000000000000000000, 0.000000000000000000 ) ) ;
#98702=DIRECTION ( 'NONE',  ( -1.000000000000000000, -0.000000000000000000, -0.000000000000000000 ) ) ;
#98751=EDGE_CURVE ( 'NONE', #90863, #46570, #559, .T. ) ;
#98776=DIRECTION ( 'NONE',  ( -1.000000000000000000, -1.224606353822377258E-16, -0.000000000000000000 ) ) ;
#98815=EDGE_CURVE ( 'NONE', #87682, #92773, #54218, .T. ) ;
#98818=DIRECTION ( 'NONE',  ( 0.5735764363510491570, -0.8191520442889895781, 1.003171929053522035E-16 ) ) ;
#98872=CARTESIAN_POINT ( 'NONE',  ( 6.326445470157510798, 6.578717624163893163, -2.268395195563515543 ) ) ;
#98939=EDGE_LOOP ( 'NONE', ( #63638, #84050, #36307, #5241, #59721 ) ) ;
#98982=CIRCLE ( 'NONE', #11216, 4.000000000000001776 ) ;
#98983=CIRCLE ( 'NONE', #92077, 6.500000000000000000 ) ;
#98984=CIRCLE ( 'NONE', #66283, 4.000000000000000888 ) ;
#98996=EDGE_LOOP ( 'NONE', ( #85129, #76402, #85944, #72044, #70753 ) ) ;
#99020=EDGE_CURVE ( 'NONE', #1420, #51255, #9405, .T. ) ;
#99064=ORIENTED_EDGE ( 'NONE', *, *, #86267, .F. ) ;
#99071=AXIS2_PLACEMENT_3D ( 'NONE', #13038, #28763, #37905 ) ;
#99100=DIRECTION ( 'NONE',  ( 0.000000000000000000, -1.000000000000000000, 0.000000000000000000 ) ) ;
#99107=FACE_OUTER_BOUND ( 'NONE', #37844, .T. ) ;
#99148=ORIENTED_EDGE ( 'NONE', *, *, #97228, .F. ) ;
#99150=ADVANCED_FACE ( 'NONE', ( #28871 ), #30434, .T. ) ;
#99181=ORIENTED_EDGE ( 'NONE', *, *, #81838, .T. ) ;
#99186=ORIENTED_EDGE ( 'NONE', *, *, #37385, .F. ) ;
#99203=VERTEX_POINT ( 'NONE', #22879 ) ;
#99216=CIRCLE ( 'NONE', #23515, 4.000000000000001776 ) ;
#99217=AXIS2_PLACEMENT_3D ( 'NONE', #79412, #14653, #97177 ) ;
#99239=ORIENTED_EDGE ( 'NONE', *, *, #5986, .F. ) ;
#99242=EDGE_CURVE ( 'NONE', #4316, #16221, #45695, .T. ) ;
#99244=VECTOR ( 'NONE', #49281, 1000.000000000000000 ) ;
#99250=VERTEX_POINT ( 'NONE', #93437 ) ;
#99268=CIRCLE ( 'NONE', #68282, 4.000000000000000888 ) ;
#99272=CARTESIAN_POINT ( 'NONE',  ( 31.36650669486618881, 0.000000000000000000, 4.000000000000000888 ) ) ;
#99313=ORIENTED_EDGE ( 'NONE', *, *, #87722, .F. ) ;
#99321=CARTESIAN_POINT ( 'NONE',  ( 5.856349485908122432, 1.359279156792585930, 6.499999999999997335 ) ) ;
#99351=EDGE_CURVE ( 'NONE', #87241, #91829, #1187, .T. ) ;
#99406=AXIS2_PLACEMENT_3D ( 'NONE', #69626, #12422, #77177 ) ;
#99423=CARTESIAN_POINT ( 'NONE',  ( 0.000000000000000000, 0.000000000000000000, 0.000000000000000000 ) ) ;
#99440=ORIENTED_EDGE ( 'NONE', *, *, #20790, .T. ) ;
#99443=VERTEX_POINT ( 'NONE', #37883 ) ;
#99471=LINE ( 'NONE', #85440, #55949 ) ;
#99473=ORIENTED_EDGE ( 'NONE', *, *, #34811, .F. ) ;
#99477=DIRECTION ( 'NONE',  ( -1.000000000000000000, -1.224606353822377258E-16, -0.000000000000000000 ) ) ;
#99506=EDGE_LOOP ( 'NONE', ( #71430, #58186, #6749, #98324, #89912 ) ) ;
#99521=CYLINDRICAL_SURFACE ( 'NONE', #92531, 4.000000000000000888 ) ;
#99563=CARTESIAN_POINT ( 'NONE',  ( 33.86650669486618881, 1.474610560812782335E-15, 0.000000000000000000 ) ) ;
#99564=B_SPLINE_CURVE_WITH_KNOTS ( 'NONE', 3,
 ( #50285, #100964, #76152, #92337, #84258 ),
 .UNSPECIFIED., .F., .F.,
 ( 4, 1, 4 ),
 ( 0.000000000000000000, 0.003752776749732568331, 0.007505553499465136662 ),
 .UNSPECIFIED. ) ;
#99582=ADVANCED_FACE ( 'NONE', ( #2135 ), #47443, .T. ) ;
#99602=DIRECTION ( 'NONE',  ( 0.000000000000000000, 1.000000000000000000, 0.000000000000000000 ) ) ;
#99603=CIRCLE ( 'NONE', #99677, 4.000000000000000888 ) ;
#99619=ORIENTED_EDGE ( 'NONE', *, *, #97472, .T. ) ;
#99630=DIRECTION ( 'NONE',  ( -0.5735764363510497121, 0.8191520442889892450, 1.003171929053521665E-16 ) ) ;
#99650=AXIS2_PLACEMENT_3D ( 'NONE', #57199, #32441, #98202 ) ;
#99677=AXIS2_PLACEMENT_3D ( 'NONE', #96271, #23453, #81114 ) ;
#99683=CARTESIAN_POINT ( 'NONE',  ( 33.09999999999999432, -3.309499999999999886, 4.475777889183790779E-16 ) ) ;
#99694=DIRECTION ( 'NONE',  ( 0.000000000000000000, -1.000000000000000000, 0.000000000000000000 ) ) ;
#99703=LINE ( 'NONE', #25874, #35732 ) ;
#99736=VERTEX_POINT ( 'NONE', #32299 ) ;
#99766=ORIENTED_EDGE ( 'NONE', *, *, #54425, .F. ) ;
#99769=CARTESIAN_POINT ( 'NONE',  ( 31.84999999999999787, 1.533819458162526451E-15, 0.000000000000000000 ) ) ;
#99794=CARTESIAN_POINT ( 'NONE',  ( 19.34999999999999787, 3.309500000000003439, 4.052968581778167743E-16 ) ) ;
#99801=ORIENTED_EDGE ( 'NONE', *, *, #97228, .T. ) ;
#99823=FACE_OUTER_BOUND ( 'NONE', #22860, .T. ) ;
#99832=CARTESIAN_POINT ( 'NONE',  ( 28.58349330513380337, 1.593028355512270962E-15, 0.000000000000000000 ) ) ;
#99860=CARTESIAN_POINT ( 'NONE',  ( 34.83349330513380693, 1.593028355512270962E-15, 0.000000000000000000 ) ) ;
#99862=CARTESIAN_POINT ( 'NONE',  ( 0.000000000000000000, 0.000000000000000000, 0.000000000000000000 ) ) ;
#99873=DIRECTION ( 'NONE',  ( 0.000000000000000000, -1.000000000000000000, 0.000000000000000000 ) ) ;
#99908=AXIS2_PLACEMENT_3D ( 'NONE', #106401, #97260, #72971 ) ;
#99914=CARTESIAN_POINT ( 'NONE',  ( 35.11650669486618170, 1.474610560812782335E-15, 0.000000000000000000 ) ) ;
#99915=DIRECTION ( 'NONE',  ( 0.000000000000000000, 0.000000000000000000, -1.000000000000000000 ) ) ;
#99967=DIRECTION ( 'NONE',  ( 0.000000000000000000, 0.000000000000000000, 1.000000000000000000 ) ) ;
#99997=ORIENTED_EDGE ( 'NONE', *, *, #97472, .F. ) ;
#100011=CARTESIAN_POINT ( 'NONE',  ( 9.349999999999997868, 1.533819458162526451E-15, 0.000000000000000000 ) ) ;
#100025=CIRCLE ( 'NONE', #26018, 3.309499999999999886 ) ;
#100056=CARTESIAN_POINT ( 'NONE',  ( 0.000000000000000000, 4.898587196589413815E-16, -4.000000000000000888 ) ) ;
#100062=CONICAL_SURFACE ( 'NONE', #77671, 4.000000000000001776, 0.9599310885968774798 ) ;
#100103=CARTESIAN_POINT ( 'NONE',  ( 16.84999999999999787, -3.309499999999999886, 4.475777889183790779E-16 ) ) ;
#100113=CYLINDRICAL_SURFACE ( 'NONE', #94800, 4.000000000000000888 ) ;
#100135=ORIENTED_EDGE ( 'NONE', *, *, #67655, .F. ) ;
#100137=AXIS2_PLACEMENT_3D ( 'NONE', #20830, #4058, #22395 ) ;
#100145=CARTESIAN_POINT ( 'NONE',  ( 6.333820801331317973, 4.275724398227923828, -5.594228103109662342 ) ) ;
#100149=AXIS2_PLACEMENT_3D ( 'NONE', #8523, #58139, #41426 ) ;
#100170=EDGE_CURVE ( 'NONE', #16689, #63739, #75694, .T. ) ;
#100177=VECTOR ( 'NONE', #76054, 1000.000000000000000 ) ;
#100181=CARTESIAN_POINT ( 'NONE',  ( 18.86650669486618881, 1.474610560812782335E-15, 0.000000000000000000 ) ) ;
#100210=CARTESIAN_POINT ( 'NONE',  ( 0.4037800551813718331, -4.058962678540100733, 5.969670414742688003 ) ) ;
#100316=ADVANCED_FACE ( 'NONE', ( #12018 ), #12541, .T. ) ;
#100336=CARTESIAN_POINT ( 'NONE',  ( 12.33349330513380693, 1.593028355512270962E-15, 0.000000000000000000 ) ) ;
#100371=CARTESIAN_POINT ( 'NONE',  ( 32.33349330513380693, 1.593028355512270962E-15, 0.000000000000000000 ) ) ;
#100418=CARTESIAN_POINT ( 'NONE',  ( 24.83349330513380693, -4.000000000000000000, 4.898587196589415787E-16 ) ) ;
#100471=CONICAL_SURFACE ( 'NONE', #53964, 3.309500000000001663, 0.9599310885968770357 ) ;
#100482=DIRECTION ( 'NONE',  ( 0.000000000000000000, -1.000000000000000000, 0.000000000000000000 ) ) ;
#100532=ORIENTED_EDGE ( 'NONE', *, *, #8428, .F. ) ;
#100545=ORIENTED_EDGE ( 'NONE', *, *, #66819, .T. ) ;
#100555=EDGE_CURVE ( 'NONE', #31177, #37114, #83709, .T. ) ;
#100578=CARTESIAN_POINT ( 'NONE',  ( 27.33349330513380693, 4.898587196589411843E-16, -4.000000000000001776 ) ) ;
#100591=EDGE_CURVE ( 'NONE', #22641, #4198, #68249, .T. ) ;
#100624=CARTESIAN_POINT ( 'NONE',  ( 6.289692432696785573, -1.240526984323783911E-13, -6.828989928337169779 ) ) ;
#100646=CARTESIAN_POINT ( 'NONE',  ( 11.36650669486618881, 4.000000000000003553, 4.898587196589414801E-16 ) ) ;
#100664=VERTEX_POINT ( 'NONE', #89636 ) ;
#100669=ORIENTED_EDGE ( 'NONE', *, *, #39369, .F. ) ;
#100687=ORIENTED_EDGE ( 'NONE', *, *, #25730, .F. ) ;
#100697=VECTOR ( 'NONE', #3552, 1000.000000000000227 ) ;
#100701=VERTEX_POINT ( 'NONE', #66963 ) ;
#100782=DIRECTION ( 'NONE',  ( -1.000000000000000000, -0.000000000000000000, -0.000000000000000000 ) ) ;
#100783=ADVANCED_FACE ( 'NONE', ( #11895 ), #52841, .T. ) ;
#100806=ORIENTED_EDGE ( 'NONE', *, *, #66860, .F. ) ;
#100834=DIRECTION ( 'NONE',  ( 0.000000000000000000, -1.000000000000000000, 0.000000000000000000 ) ) ;
#100846=AXIS2_PLACEMENT_3D ( 'NONE', #91224, #17329, #50205 ) ;
#100866=DIRECTION ( 'NONE',  ( 0.000000000000000000, -1.000000000000000000, 0.000000000000000000 ) ) ;
#100891=ORIENTED_EDGE ( 'NONE', *, *, #2625, .F. ) ;
#100898=DIRECTION ( 'NONE',  ( 0.000000000000000000, 1.000000000000000000, 0.000000000000000000 ) ) ;
#100903=DIRECTION ( 'NONE',  ( 0.000000000000000000, -1.000000000000000000, 0.000000000000000000 ) ) ;
#100937=EDGE_CURVE ( 'NONE', #3128, #47612, #11759, .T. ) ;
#100958=CIRCLE ( 'NONE', #11403, 3.309500000000001663 ) ;
#100964=CARTESIAN_POINT ( 'NONE',  ( 5.947762761376476526, -4.378239541354667530, -5.416666666666668739 ) ) ;
#100980=APPLICATION_CONTEXT ( 'automotive_design' ) ;
#100997=CARTESIAN_POINT ( 'NONE',  ( 26.84999999999999787, 1.533819458162526451E-15, 0.000000000000000000 ) ) ;
#101046=FACE_OUTER_BOUND ( 'NONE', #54780, .T. ) ;
#101063=ADVANCED_FACE ( 'NONE', ( #23077 ), #68337, .T. ) ;
#101079=AXIS2_PLACEMENT_3D ( 'NONE', #68523, #101415, #80295 ) ;
#101081=AXIS2_PLACEMENT_3D ( 'NONE', #46111, #38048, #5635 ) ;
#101168=CARTESIAN_POINT ( 'NONE',  ( 12.61650669486618881, 1.474610560812782335E-15, 0.000000000000000000 ) ) ;
#101180=DIRECTION ( 'NONE',  ( 0.000000000000000000, -1.000000000000000000, 0.000000000000000000 ) ) ;
#101183=LINE ( 'NONE', #27344, #102326 ) ;
#101228=ADVANCED_FACE ( 'NONE', ( #6880 ), #44307, .T. ) ;
#101287=EDGE_LOOP ( 'NONE', ( #32652, #38513, #63530, #102489, #12263 ) ) ;
#101320=ORIENTED_EDGE ( 'NONE', *, *, #22621, .T. ) ;
#101335=ORIENTED_EDGE ( 'NONE', *, *, #71742, .T. ) ;
#101373=CARTESIAN_POINT ( 'NONE',  ( 5.947762761376474749, 6.880090707843042885, -1.083333333333333037 ) ) ;
#101394=DIRECTION ( 'NONE',  ( -1.000000000000000000, -0.000000000000000000, -0.000000000000000000 ) ) ;
#101396=FACE_OUTER_BOUND ( 'NONE', #92847, .T. ) ;
#101408=AXIS2_PLACEMENT_3D ( 'NONE', #7567, #57706, #39964 ) ;
#101412=AXIS2_PLACEMENT_3D ( 'NONE', #36254, #27093, #75049 ) ;
#101415=DIRECTION ( 'NONE',  ( 1.000000000000000000, 0.000000000000000000, 0.000000000000000000 ) ) ;
#101417=DIRECTION ( 'NONE',  ( -0.5735764363510497121, 0.8191520442889892450, 1.003171929053521665E-16 ) ) ;
#101426=VERTEX_POINT ( 'NONE', #47212 ) ;
#101455=DIRECTION ( 'NONE',  ( 0.000000000000000000, 0.000000000000000000, -1.000000000000000000 ) ) ;
#101465=CARTESIAN_POINT ( 'NONE',  ( 5.947762761376472973, 4.378239541354660425, 5.416666666666664298 ) ) ;
#101495=CARTESIAN_POINT ( 'NONE',  ( 9.349999999999997868, 3.309500000000003439, 4.052968581778167743E-16 ) ) ;
#101499=VERTEX_POINT ( 'NONE', #70453 ) ;
#101517=DIRECTION ( 'NONE',  ( 0.000000000000000000, -1.000000000000000000, 0.000000000000000000 ) ) ;
#101543=FACE_OUTER_BOUND ( 'NONE', #73736, .T. ) ;
#101631=CARTESIAN_POINT ( 'NONE',  ( 14.34999999999999787, 3.309500000000003439, 0.000000000000000000 ) ) ;
#101644=VECTOR ( 'NONE', #4564, 1000.000000000000000 ) ;
#101690=CARTESIAN_POINT ( 'NONE',  ( 10.11650669486618881, 1.474610560812782335E-15, 0.000000000000000000 ) ) ;
#101701=ORIENTED_EDGE ( 'NONE', *, *, #25927, .F. ) ;
#101706=DIRECTION ( 'NONE',  ( -1.000000000000000000, -0.000000000000000000, -0.000000000000000000 ) ) ;
#101723=CARTESIAN_POINT ( 'NONE',  ( 0.5805565836007664515, -7.505553499465142053, -1.357586595304856736E-16 ) ) ;
#101731=ADVANCED_FACE ( 'NONE', ( #92449 ), #18605, .T. ) ;
#101747=EDGE_LOOP ( 'NONE', ( #7760, #67672, #40388, #11909, #94299 ) ) ;
#101755=ORIENTED_EDGE ( 'NONE', *, *, #8679, .F. ) ;
#101855=AXIS2_PLACEMENT_3D ( 'NONE', #30529, #20349, #102804 ) ;
#101880=AXIS2_PLACEMENT_3D ( 'NONE', #91597, #65181, #17708 ) ;
#101887=AXIS2_PLACEMENT_3D ( 'NONE', #70528, #3132, #2585 ) ;
#101893=FACE_OUTER_BOUND ( 'NONE', #10939, .T. ) ;
#101928=LINE ( 'NONE', #92776, #100177 ) ;
#101931=ORIENTED_EDGE ( 'NONE', *, *, #50288, .F. ) ;
#101945=ORIENTED_EDGE ( 'NONE', *, *, #55874, .T. ) ;
#102013=CARTESIAN_POINT ( 'NONE',  ( 11.84999999999999787, 1.533819458162526451E-15, 0.000000000000000000 ) ) ;
#102029=ORIENTED_EDGE ( 'NONE', *, *, #78695, .F. ) ;
#102050=EDGE_CURVE ( 'NONE', #8349, #81897, #46828, .T. ) ;
#102068=ORIENTED_EDGE ( 'NONE', *, *, #47265, .F. ) ;
#102090=EDGE_LOOP ( 'NONE', ( #623, #53194, #81183, #86198, #90676, #10544 ) ) ;
#102099=CARTESIAN_POINT ( 'NONE',  ( 31.84999999999999787, -3.309499999999999886, 0.000000000000000000 ) ) ;
#102118=CARTESIAN_POINT ( 'NONE',  ( 28.58349330513380337, 1.593028355512270962E-15, 0.000000000000000000 ) ) ;
#102134=STYLED_ITEM ( 'NONE', ( #12604 ), #38340 ) ;
#102163=FILL_AREA_STYLE_COLOUR ( '', #36738 ) ;
#102209=AXIS2_PLACEMENT_3D ( 'NONE', #47117, #32028, #72461 ) ;
#102261=AXIS2_PLACEMENT_3D ( 'NONE', #13849, #97966, #96395 ) ;
#102264=AXIS2_PLACEMENT_3D ( 'NONE', #36728, #62560, #79787 ) ;
#102294=CONICAL_SURFACE ( 'NONE', #64420, 3.309500000000001663, 0.9599310885968770357 ) ;
#102299=AXIS2_PLACEMENT_3D ( 'NONE', #55049, #30285, #72310 ) ;
#102326=VECTOR ( 'NONE', #19260, 1000.000000000000000 ) ;
#102328=ORIENTED_EDGE ( 'NONE', *, *, #95372, .T. ) ;
#102347=CARTESIAN_POINT ( 'NONE',  ( 38.09999999999998721, 0.000000000000000000, 3.309499999999999886 ) ) ;
#102351=ORIENTED_EDGE ( 'NONE', *, *, #4690, .F. ) ;
#102359=AXIS2_PLACEMENT_3D ( 'NONE', #84650, #26449, #42581 ) ;
#102420=FACE_OUTER_BOUND ( 'NONE', #11490, .T. ) ;
#102424=CARTESIAN_POINT ( 'NONE',  ( 13.09999999999999787, -3.309499999999999886, 4.475777889183790779E-16 ) ) ;
#102455=DIRECTION ( 'NONE',  ( 0.000000000000000000, -1.000000000000000000, 0.000000000000000000 ) ) ;
#102465=CIRCLE ( 'NONE', #35283, 4.000000000000000888 ) ;
#102471=CARTESIAN_POINT ( 'NONE',  ( 6.333820801330125150, 4.275724398227219503, 5.594228103108966010 ) ) ;
#102480=CIRCLE ( 'NONE', #31812, 4.000000000000001776 ) ;
#102489=ORIENTED_EDGE ( 'NONE', *, *, #67903, .F. ) ;
#102553=CIRCLE ( 'NONE', #55998, 3.309500000000001663 ) ;
#102583=DIRECTION ( 'NONE',  ( -1.000000000000000000, -1.224606353822377258E-16, -0.000000000000000000 ) ) ;
#102640=VECTOR ( 'NONE', #2855, 1000.000000000000341 ) ;
#102643=DIRECTION ( 'NONE',  ( -1.000000000000000000, -0.000000000000000000, -0.000000000000000000 ) ) ;
#102714=EDGE_LOOP ( 'NONE', ( #6058, #39672, #2659 ) ) ;
#102730=ADVANCED_FACE ( 'NONE', ( #92976 ), #32672, .T. ) ;
#102734=CARTESIAN_POINT ( 'NONE',  ( 9.349999999999997868, -3.309499999999999886, 4.475777889183790779E-16 ) ) ;
#102737=CIRCLE ( 'NONE', #73459, 4.000000000000001776 ) ;
#102739=ORIENTED_EDGE ( 'NONE', *, *, #53322, .T. ) ;
#102754=DIRECTION ( 'NONE',  ( -1.000000000000000000, -0.000000000000000000, -0.000000000000000000 ) ) ;
#102768=VERTEX_POINT ( 'NONE', #106214 ) ;
#102770=CARTESIAN_POINT ( 'NONE',  ( 0.000000000000000000, 0.000000000000000000, 0.000000000000000000 ) ) ;
#102783=ORIENTED_EDGE ( 'NONE', *, *, #48925, .F. ) ;
#102804=DIRECTION ( 'NONE',  ( 0.000000000000000000, -1.000000000000000000, 0.000000000000000000 ) ) ;
#102807=EDGE_CURVE ( 'NONE', #72268, #43607, #15389, .T. ) ;
#102816=DIRECTION ( 'NONE',  ( 0.000000000000000000, -1.000000000000000000, 0.000000000000000000 ) ) ;
#102864=DIRECTION ( 'NONE',  ( 0.000000000000000000, -1.000000000000000000, 0.000000000000000000 ) ) ;
#102883=CARTESIAN_POINT ( 'NONE',  ( 8.866506694866188809, 4.898587196589413815E-16, -4.000000000000000888 ) ) ;
#102889=ORIENTED_EDGE ( 'NONE', *, *, #62048, .T. ) ;
#102917=EDGE_LOOP ( 'NONE', ( #95090, #67881, #55186, #56703, #65963 ) ) ;
#102930=CIRCLE ( 'NONE', #87463, 4.000000000000000888 ) ;
#102999=CARTESIAN_POINT ( 'NONE',  ( 33.58349330513380693, 1.593028355512270962E-15, 0.000000000000000000 ) ) ;
#103044=DIRECTION ( 'NONE',  ( -1.000000000000000000, -1.224606353822377258E-16, -0.000000000000000000 ) ) ;
#103090=DIRECTION ( 'NONE',  ( 0.000000000000000000, -1.000000000000000000, 0.000000000000000000 ) ) ;
#103114=CIRCLE ( 'NONE', #4951, 4.000000000000001776 ) ;
#103134=DIRECTION ( 'NONE',  ( 0.000000000000000000, -1.000000000000000000, 0.000000000000000000 ) ) ;
#103175=CARTESIAN_POINT ( 'NONE',  ( 33.58349330513380693, 1.593028355512270962E-15, 0.000000000000000000 ) ) ;
#103186=DIRECTION ( 'NONE',  ( -1.000000000000000000, -0.000000000000000000, -0.000000000000000000 ) ) ;
#103210=AXIS2_PLACEMENT_3D ( 'NONE', #51485, #83855, #91951 ) ;
#103232=EDGE_CURVE ( 'NONE', #78825, #56180, #60445, .T. ) ;
#103234=SURFACE_STYLE_USAGE ( .BOTH. , #77363 ) ;
#103262=DIRECTION ( 'NONE',  ( -1.000000000000000000, -1.224606353822377258E-16, -0.000000000000000000 ) ) ;
#103276=EDGE_CURVE ( 'NONE', #6482, #4006, #13900, .T. ) ;
#103284=ADVANCED_FACE ( 'NONE', ( #64088 ), #36301, .T. ) ;
#103320=EDGE_LOOP ( 'NONE', ( #30421, #68950, #34080, #48395, #83918 ) ) ;
#103338=ORIENTED_EDGE ( 'NONE', *, *, #40959, .T. ) ;
#103361=DIRECTION ( 'NONE',  ( -1.000000000000000000, -1.224606353822377258E-16, -0.000000000000000000 ) ) ;
#103364=CARTESIAN_POINT ( 'NONE',  ( 28.58349330513380337, 4.898587196589411843E-16, -4.000000000000001776 ) ) ;
#103366=ORIENTED_EDGE ( 'NONE', *, *, #82408, .F. ) ;
#103375=DIRECTION ( 'NONE',  ( 0.000000000000000000, -1.000000000000000000, 0.000000000000000000 ) ) ;
#103378=CARTESIAN_POINT ( 'NONE',  ( 15.11650669486618881, -3.999999999999998224, 0.000000000000000000 ) ) ;
#103393=ORIENTED_EDGE ( 'NONE', *, *, #41266, .F. ) ;
#103406=ORIENTED_EDGE ( 'NONE', *, *, #28115, .T. ) ;
#103409=EDGE_CURVE ( 'NONE', #32377, #75403, #67360, .T. ) ;
#103414=AXIS2_PLACEMENT_3D ( 'NONE', #25091, #47206, #55808 ) ;
#103427=DIRECTION ( 'NONE',  ( -1.000000000000000000, -1.224606353822377258E-16, -0.000000000000000000 ) ) ;
#103461=CARTESIAN_POINT ( 'NONE',  ( 30.59999999999999787, 1.533819458162526451E-15, 0.000000000000000000 ) ) ;
#103496=AXIS2_PLACEMENT_3D ( 'NONE', #63161, #81431, #46953 ) ;
#103508=CARTESIAN_POINT ( 'NONE',  ( 15.59999999999999787, 1.533819458162526451E-15, 0.000000000000000000 ) ) ;
#103612=AXIS2_PLACEMENT_3D ( 'NONE', #76041, #51221, #102455 ) ;
#103613=CARTESIAN_POINT ( 'NONE',  ( 0.000000000000000000, 4.898587196589413815E-16, -4.000000000000000888 ) ) ;
#103620=ORIENTED_EDGE ( 'NONE', *, *, #28390, .F. ) ;
#103630=DIRECTION ( 'NONE',  ( -1.000000000000000000, -1.224606353822377258E-16, -0.000000000000000000 ) ) ;
#103672=LINE ( 'NONE', #62696, #30576 ) ;
#103711=CARTESIAN_POINT ( 'NONE',  ( 6.169949891408089471, -4.949864754179694515, 4.426582755167080663 ) ) ;
#103712=ADVANCED_FACE ( 'NONE', ( #38629 ), #40190, .T. ) ;
#103729=ADVANCED_FACE ( 'NONE', ( #6220 ), #100062, .T. ) ;
#103809=DIRECTION ( 'NONE',  ( -1.000000000000000000, -1.224606353822377258E-16, -0.000000000000000000 ) ) ;
#103836=EDGE_CURVE ( 'NONE', #36200, #52034, #51932, .T. ) ;
#103881=ADVANCED_FACE ( 'NONE', ( #59585 ), #38203, .T. ) ;
#103913=CARTESIAN_POINT ( 'NONE',  ( 21.08349330513380693, 4.898587196589411843E-16, -4.000000000000001776 ) ) ;
#103972=ORIENTED_EDGE ( 'NONE', *, *, #78158, .T. ) ;
#103982=ORIENTED_EDGE ( 'NONE', *, *, #29125, .F. ) ;
#104032=CONICAL_SURFACE ( 'NONE', #45554, 4.000000000000001776, 0.9599310885968774798 ) ;
#104043=VECTOR ( 'NONE', #34132, 1000.000000000000227 ) ;
#104046=ADVANCED_FACE ( 'NONE', ( #72980 ), #47650, .F. ) ;
#104048=CARTESIAN_POINT ( 'NONE',  ( 6.222742520105473574, 7.673830019007162662, -0.2914634815676393487 ) ) ;
#104115=CIRCLE ( 'NONE', #5948, 3.309500000000001663 ) ;
#104149=ORIENTED_EDGE ( 'NONE', *, *, #51284, .T. ) ;
#104156=AXIS2_PLACEMENT_3D ( 'NONE', #60052, #11988, #75119 ) ;
#104170=DIRECTION ( 'NONE',  ( 0.000000000000000000, -1.000000000000000000, 0.000000000000000000 ) ) ;
#104173=EDGE_CURVE ( 'NONE', #77164, #8054, #43680, .T. ) ;
#104187=DIRECTION ( 'NONE',  ( 0.000000000000000000, -1.000000000000000000, 0.000000000000000000 ) ) ;
#104200=EDGE_LOOP ( 'NONE', ( #23341, #66703, #89805, #41651, #89278, #72707 ) ) ;
#104207=ADVANCED_FACE ( 'NONE', ( #101396 ), #43326, .T. ) ;
#104250=ORIENTED_EDGE ( 'NONE', *, *, #80456, .F. ) ;
#104300=LINE ( 'NONE', #80023, #13408 ) ;
#104312=CARTESIAN_POINT ( 'NONE',  ( 31.36650669486618881, 1.474610560812782335E-15, 0.000000000000000000 ) ) ;
#104323=CARTESIAN_POINT ( 'NONE',  ( 8.866506694866188809, 1.474610560812782335E-15, 0.000000000000000000 ) ) ;
#104345=DIRECTION ( 'NONE',  ( 0.000000000000000000, -2.311253228826401127E-16, -1.000000000000000000 ) ) ;
#104348=ADVANCED_FACE ( 'NONE', ( #82423 ), #105306, .T. ) ;
#104383=CARTESIAN_POINT ( 'NONE',  ( 38.09999999999998721, 0.000000000000000000, 0.000000000000000000 ) ) ;
#104402=DIRECTION ( 'NONE',  ( 0.000000000000000000, -1.000000000000000000, 0.000000000000000000 ) ) ;
#104404=EDGE_CURVE ( 'NONE', #90141, #30305, #79508, .T. ) ;
#104461=CIRCLE ( 'NONE', #11443, 4.000000000000000888 ) ;
#104479=CARTESIAN_POINT ( 'NONE',  ( 6.338255145480260921, 2.729868969643340471, -6.500000000000002665 ) ) ;
#104486=CARTESIAN_POINT ( 'NONE',  ( 28.58349330513380337, 1.593028355512270962E-15, 0.000000000000000000 ) ) ;
#104487=PRODUCT ( 'hex flange bolt_din_DIN 6921 - M8 x 30 x 30-S', 'hex flange bolt_din_DIN 6921 - M8 x 30 x 30-S', '', ( #15287 ) ) ;
#104506=ORIENTED_EDGE ( 'NONE', *, *, #12881, .T. ) ;
#104536=CIRCLE ( 'NONE', #92518, 4.000000000000000888 ) ;
#104544=VERTEX_POINT ( 'NONE', #65045 ) ;
#104569=CARTESIAN_POINT ( 'NONE',  ( 6.692588830498428010, -3.932766476276041256, -6.892929031562517572 ) ) ;
#104570=LINE ( 'NONE', #71145, #12473 ) ;
#104579=CARTESIAN_POINT ( 'NONE',  ( 6.222742520105470021, 3.584500230190543313, 6.791463481567635796 ) ) ;
#104629=CARTESIAN_POINT ( 'NONE',  ( -9.994988777600744001E-16, -0.6346842323187741330, 6.499999999999998224 ) ) ;
#104636=CARTESIAN_POINT ( 'NONE',  ( 29.83349330513380693, -3.851859888774471706E-31, 4.000000000000001776 ) ) ;
#104639=CIRCLE ( 'NONE', #34079, 3.309500000000001663 ) ;
#104677=ORIENTED_EDGE ( 'NONE', *, *, #32330, .F. ) ;
#104696=CARTESIAN_POINT ( 'NONE',  ( 13.86650669486618881, 4.000000000000003553, 4.898587196589414801E-16 ) ) ;
#104707=FACE_OUTER_BOUND ( 'NONE', #42641, .T. ) ;
#104744=DIRECTION ( 'NONE',  ( -1.000000000000000000, -1.224606353822377258E-16, -0.000000000000000000 ) ) ;
#104747=DIRECTION ( 'NONE',  ( 0.000000000000000000, -1.000000000000000000, 0.000000000000000000 ) ) ;
#104754=EDGE_CURVE ( 'NONE', #47192, #19669, #81262, .T. ) ;
#104766=CONICAL_SURFACE ( 'NONE', #6590, 3.309500000000001663, 0.9599310885968770357 ) ;
#104772=CARTESIAN_POINT ( 'NONE',  ( 6.222742520105474462, -7.673830019007166214, -0.2914634815676421797 ) ) ;
#104809=LINE ( 'NONE', #22859, #93688 ) ;
#104848=DIRECTION ( 'NONE',  ( -1.000000000000000000, -0.000000000000000000, -0.000000000000000000 ) ) ;
#104913=CLOSED_SHELL ( 'NONE', ( #61100, #51253, #56334, #79916, #61999, #45788, #37095, #23856, #16370, #14978, #31419, #48112, #26978, #71449, #99582, #62823, #80126, #38379, #18314, #99150, #23488, #97817, #34878, #46374, #85335, #28886, #58390, #5751, #10229, #84424, #66333, #83465, #45798, #92323, #94044, #19861, #19338, #105615, #84896, #103729, #97248, #60927, #9691, #91316, #101063, #22867, #105611, #96420, #33801, #19829, #93886, #33865, #89651, #52670, #4059, #67686, #66172, #63035, #27666, #59712, #22435, #71749, #67849, #64499, #30246, #21155, #100783, #95907, #103881, #29414, #77217, #91539, #75265, #29194, #100316, #1619, #12353, #6226, #80383, #25721, #82700, #61318, #62960, #63667, #104046, #59489, #11423, #71062, #22117, #74618, #30236, #44252, #72595, #1027, #8383, #92230, #8810, #40377, #31835, #12777, #93596, #58551, #95644, #72855, #76431, #105441, #87340, #5743, #42817, #86974, #95935, #70819, #104207, #80803, #35957, #67778, #103712, #62035, #8606, #15517, #23558, #103284, #41947, #106013, #60561, #86726, #31467, #6214, #50651, #74850, #102730, #14248, #45937, #76160, #20906, #22396, #47248, #46462, #84952, #25238, #76069, #35801, #75939, #36765, #40294, #66384, #101731, #89647, #101228, #54413, #30995, #20002, #4062, #94850, #104348, #63253, #105777, #96247, #2086, #37763, #10760, #16542, #18096, #56589, #75285, #10901, #77558 ) ) ;
#104932=ORIENTED_EDGE ( 'NONE', *, *, #86010, .T. ) ;
#104971=LINE ( 'NONE', #81196, #71388 ) ;
#104988=VERTEX_POINT ( 'NONE', #77267 ) ;
#104998=FACE_OUTER_BOUND ( 'NONE', #86052, .T. ) ;
#105023=CARTESIAN_POINT ( 'NONE',  ( 6.172076129340783091, 1.395179846520576694, -6.500000000000001776 ) ) ;
#105056=CARTESIAN_POINT ( 'NONE',  ( 0.000000000000000000, 4.898587196589413815E-16, -4.000000000000000888 ) ) ;
#105057=CARTESIAN_POINT ( 'NONE',  ( 25.11650669486618881, 1.474610560812782335E-15, 0.000000000000000000 ) ) ;
#105071=CIRCLE ( 'NONE', #12048, 6.500000000000000888 ) ;
#105074=CARTESIAN_POINT ( 'NONE',  ( 33.58349330513380693, 1.593028355512270962E-15, 0.000000000000000000 ) ) ;
#105075=ORIENTED_EDGE ( 'NONE', *, *, #81408, .T. ) ;
#105092=EDGE_CURVE ( 'NONE', #88621, #98079, #86304, .T. ) ;
#105116=CIRCLE ( 'NONE', #75863, 4.000000000000000888 ) ;
#105120=AXIS2_PLACEMENT_3D ( 'NONE', #3887, #11418, #20113 ) ;
#105205=DIRECTION ( 'NONE',  ( 0.000000000000000000, -1.000000000000000000, 0.000000000000000000 ) ) ;
#105229=DIRECTION ( 'NONE',  ( -1.000000000000000000, -1.224606353822377258E-16, -0.000000000000000000 ) ) ;
#105245=CARTESIAN_POINT ( 'NONE',  ( 9.349999999999997868, 1.533819458162526451E-15, 0.000000000000000000 ) ) ;
#105253=LINE ( 'NONE', #45965, #17029 ) ;
#105306=CONICAL_SURFACE ( 'NONE', #100149, 3.309500000000001663, 0.9599310885968770357 ) ;
#105346=CARTESIAN_POINT ( 'NONE',  ( 17.61650669486618881, 1.474610560812782335E-15, 0.000000000000000000 ) ) ;
#105349=CARTESIAN_POINT ( 'NONE',  ( 6.683837171061806082, -3.955946848495971668, -6.851900933636991375 ) ) ;
#105391=ORIENTED_EDGE ( 'NONE', *, *, #12881, .F. ) ;
#105403=CARTESIAN_POINT ( 'NONE',  ( 0.5805565836007658964, 7.505553499465141165, -3.996997974842411264E-16 ) ) ;
#105438=DIRECTION ( 'NONE',  ( 0.000000000000000000, 1.000000000000000000, 0.000000000000000000 ) ) ;
#105441=ADVANCED_FACE ( 'NONE', ( #104998 ), #77745, .T. ) ;
#105443=ORIENTED_EDGE ( 'NONE', *, *, #4151, .T. ) ;
#105470=DIRECTION ( 'NONE',  ( -1.000000000000000000, -0.000000000000000000, -0.000000000000000000 ) ) ;
#105549=CARTESIAN_POINT ( 'NONE',  ( 34.83349330513380693, 1.593028355512270962E-15, 0.000000000000000000 ) ) ;
#105560=ORIENTED_EDGE ( 'NONE', *, *, #82735, .F. ) ;
#105576=ORIENTED_EDGE ( 'NONE', *, *, #76562, .F. ) ;
#105581=DIRECTION ( 'NONE',  ( -1.000000000000000000, -0.000000000000000000, -0.000000000000000000 ) ) ;
#105611=ADVANCED_FACE ( 'NONE', ( #16508 ), #7345, .T. ) ;
#105615=ADVANCED_FACE ( 'NONE', ( #89351 ), #15442, .T. ) ;
#105628=CARTESIAN_POINT ( 'NONE',  ( 6.333820801332779915, -6.982605850969665795, -0.9057718968909265200 ) ) ;
#105669=DIRECTION ( 'NONE',  ( -0.5735764363510494901, -0.8191520442889894671, 0.000000000000000000 ) ) ;
#105689=ORIENTED_EDGE ( 'NONE', *, *, #42271, .F. ) ;
#105690=ORIENTED_EDGE ( 'NONE', *, *, #22741, .T. ) ;
#105719=CARTESIAN_POINT ( 'NONE',  ( 20.59999999999999787, 1.533819458162526451E-15, 0.000000000000000000 ) ) ;
#105759=CONICAL_SURFACE ( 'NONE', #73030, 4.000000000000001776, 0.9599310885968774798 ) ;
#105766=DIRECTION ( 'NONE',  ( -1.000000000000000000, -0.000000000000000000, -0.000000000000000000 ) ) ;
#105772=CIRCLE ( 'NONE', #64462, 4.000000000000001776 ) ;
#105777=ADVANCED_FACE ( 'NONE', ( #71423 ), #58808, .T. ) ;
#105780=CONICAL_SURFACE ( 'NONE', #69621, 4.000000000000001776, 0.9599310885968774798 ) ;
#105786=CARTESIAN_POINT ( 'NONE',  ( 12.61650669486618881, -3.999999999999998224, 0.000000000000000000 ) ) ;
#105824=FACE_OUTER_BOUND ( 'NONE', #52713, .T. ) ;
#105838=CARTESIAN_POINT ( 'NONE',  ( 32.33349330513380693, 1.593028355512270962E-15, 0.000000000000000000 ) ) ;
#105861=ORIENTED_EDGE ( 'NONE', *, *, #94630, .T. ) ;
#105867=CARTESIAN_POINT ( 'NONE',  ( 6.562974947121713143, -7.579827465851456836, -0.5629870116737628605 ) ) ;
#105907=CARTESIAN_POINT ( 'NONE',  ( 13.09999999999999787, 1.533819458162526451E-15, 0.000000000000000000 ) ) ;
#105918=ORIENTED_EDGE ( 'NONE', *, *, #103276, .F. ) ;
#105922=AXIS2_PLACEMENT_3D ( 'NONE', #22557, #14400, #6312 ) ;
#105942=DIRECTION ( 'NONE',  ( 0.000000000000000000, -1.000000000000000000, 0.000000000000000000 ) ) ;
#105947=EDGE_CURVE ( 'NONE', #82322, #81756, #60582, .T. ) ;
#105951=CARTESIAN_POINT ( 'NONE',  ( 13.58349330513380515, 1.593028355512270962E-15, 0.000000000000000000 ) ) ;
#105961=AXIS2_PLACEMENT_3D ( 'NONE', #99914, #76166, #26607 ) ;
#105999=AXIS2_PLACEMENT_3D ( 'NONE', #27383, #60263, #86129 ) ;
#106013=ADVANCED_FACE ( 'NONE', ( #47549 ), #36518, .T. ) ;
#106047=ORIENTED_EDGE ( 'NONE', *, *, #41000, .T. ) ;
#106082=CIRCLE ( 'NONE', #81981, 4.000000000000001776 ) ;
#106113=CARTESIAN_POINT ( 'NONE',  ( 21.08349330513380693, 4.000000000000003553, 0.000000000000000000 ) ) ;
#106125=ORIENTED_EDGE ( 'NONE', *, *, #98081, .F. ) ;
#106134=CARTESIAN_POINT ( 'NONE',  ( 33.58349330513380693, -4.000000000000000000, 4.898587196589415787E-16 ) ) ;
#106166=CIRCLE ( 'NONE', #30391, 4.000000000000001776 ) ;
#106209=AXIS2_PLACEMENT_3D ( 'NONE', #87631, #37519, #36464 ) ;
#106214=CARTESIAN_POINT ( 'NONE',  ( 20.59999999999999787, -3.309499999999999886, 4.475777889183790779E-16 ) ) ;
#106235=ORIENTED_EDGE ( 'NONE', *, *, #64471, .F. ) ;
#106257=AXIS2_PLACEMENT_3D ( 'NONE', #103461, #38227, #62482 ) ;
#106258=DIRECTION ( 'NONE',  ( -1.000000000000000000, -1.224606353822377258E-16, -0.000000000000000000 ) ) ;
#106287=CARTESIAN_POINT ( 'NONE',  ( 19.83349330513380693, -3.851859888774471706E-31, 4.000000000000001776 ) ) ;
#106299=VECTOR ( 'NONE', #84607, 1000.000000000000000 ) ;
#106327=CARTESIAN_POINT ( 'NONE',  ( 8.866506694866188809, 4.000000000000003553, 4.898587196589414801E-16 ) ) ;
#106340=FACE_OUTER_BOUND ( 'NONE', #65314, .T. ) ;
#106352=CARTESIAN_POINT ( 'NONE',  ( 6.288680569791143427, 0.6514782672944290365, 6.828922012436084543 ) ) ;
#106358=AXIS2_PLACEMENT_3D ( 'NONE', #55708, #15277, #8241 ) ;
#106401=CARTESIAN_POINT ( 'NONE',  ( 8.099999999999999645, 0.000000000000000000, 0.000000000000000000 ) ) ;
#106418=VECTOR ( 'NONE', #61010, 1000.000000000000227 ) ;
#106443=CIRCLE ( 'NONE', #15223, 4.000000000000000888 ) ;
#106469=EDGE_LOOP ( 'NONE', ( #53150, #12131, #5910, #46164, #74447 ) ) ;
#106478=CARTESIAN_POINT ( 'NONE',  ( 0.000000000000000000, -5.629165124598850767, -3.249999999999999556 ) ) ;
#106487=VECTOR ( 'NONE', #47333, 1000.000000000000000 ) ;
#106534=CARTESIAN_POINT ( 'NONE',  ( 0.000000000000000000, 5.629165124598848102, 3.250000000000005329 ) ) ;
#106551=EDGE_CURVE ( 'NONE', #96401, #54339, #25319, .T. ) ;
#106558=AXIS2_PLACEMENT_3D ( 'NONE', #42117, #24902, #83113 ) ;
#106630=ORIENTED_EDGE ( 'NONE', *, *, #25927, .T. ) ;
#106633=AXIS2_PLACEMENT_3D ( 'NONE', #9567, #82411, #74309 ) ;
#106639=DIRECTION ( 'NONE',  ( -1.000000000000000000, -1.224606353822377258E-16, -0.000000000000000000 ) ) ;
#106644=CARTESIAN_POINT ( 'NONE',  ( 21.84999999999999787, 3.309500000000003439, 0.000000000000000000 ) ) ;
#106656=DIRECTION ( 'NONE',  ( 0.000000000000000000, -1.000000000000000000, 0.000000000000000000 ) ) ;
#106669=DIRECTION ( 'NONE',  ( 1.000000000000000000, 1.224606353822377258E-16, 0.000000000000000000 ) ) ;
#106697=CARTESIAN_POINT ( 'NONE',  ( 11.08349330513380515, 4.000000000000003553, 0.000000000000000000 ) ) ;
#106715=DIRECTION ( 'NONE',  ( -1.000000000000000000, -1.224606353822377258E-16, -0.000000000000000000 ) ) ;
ENDSEC;
END-ISO-10303-21;
